ISO-10303-21;
HEADER;
/* Generated by software containing ST-Developer
 * from STEP Tools, Inc. (www.steptools.com) 
 */

FILE_DESCRIPTION(
/* description */ ('STEP AP214'),
/* implementation_level */ '2;1');

FILE_NAME(
/* name */ 'PRT-TQ-1012-03.step',
/* time_stamp */ '2026-10-07T12:49:37-07:00',
/* author */ (''),
/* organization */ (''),
/* preprocessor_version */ 'ST-DEVELOPER v20.2',
/* originating_system */ 'Autodesk Translation Framework v15.15.0.0',
/* authorisation */ '');

FILE_SCHEMA (('AUTOMOTIVE_DESIGN { 1 0 10303 214 3 1 1 }'));
ENDSEC;

DATA;
#10=MECHANICAL_DESIGN_GEOMETRIC_PRESENTATION_REPRESENTATION('',(#310),#33016);
#252=SHAPE_REPRESENTATION_RELATIONSHIP('SRR','None',#33147,#279);
#279=ADVANCED_BREP_SHAPE_REPRESENTATION('',(#337),#33008);
#310=STYLED_ITEM('',(#33284),#337);
#337=MANIFOLD_SOLID_BREP('Body1',#9961);
#360=CONICAL_SURFACE('',#10976,13.,0.0282533494021236);
#361=CONICAL_SURFACE('',#10986,16.,0.785398163397441);
#362=CONICAL_SURFACE('',#10997,13.5,0.785398163397453);
#393=TOROIDAL_SURFACE('',#11026,4.98804347826086,0.5);
#394=TOROIDAL_SURFACE('',#11030,4.98804347826086,0.5);
#395=TOROIDAL_SURFACE('',#11033,4.98804347826086,0.5);
#396=TOROIDAL_SURFACE('',#11037,4.98804347826086,0.5);
#397=TOROIDAL_SURFACE('',#11040,4.98804347826086,0.5);
#398=TOROIDAL_SURFACE('',#11044,4.98804347826086,0.5);
#399=TOROIDAL_SURFACE('',#11048,4.98804347826086,0.5);
#400=TOROIDAL_SURFACE('',#11051,4.98804347826086,0.5);
#401=TOROIDAL_SURFACE('',#11055,4.98804347826086,0.5);
#402=TOROIDAL_SURFACE('',#11058,4.98804347826087,0.5);
#410=ELLIPSE('',#11023,0.568348249767833,0.502762642635108);
#411=ELLIPSE('',#11027,0.568387932752179,0.502812488556745);
#412=ELLIPSE('',#11034,0.568387933440688,0.502812489527255);
#413=ELLIPSE('',#11041,0.568348249819522,0.502762642708099);
#414=ELLIPSE('',#11045,0.568387932758158,0.502812488561987);
#415=ELLIPSE('',#11052,0.568387932787414,0.502812488608016);
#460=(
BOUNDED_SURFACE()
B_SPLINE_SURFACE(3,2,((#30126,#30127,#30128),(#30129,#30130,#30131),(#30132,
#30133,#30134),(#30135,#30136,#30137),(#30138,#30139,#30140),(#30141,#30142,
#30143),(#30144,#30145,#30146),(#30147,#30148,#30149),(#30150,#30151,#30152),
(#30153,#30154,#30155),(#30156,#30157,#30158),(#30159,#30160,#30161),(#30162,
#30163,#30164),(#30165,#30166,#30167),(#30168,#30169,#30170),(#30171,#30172,
#30173),(#30174,#30175,#30176),(#30177,#30178,#30179),(#30180,#30181,#30182),
(#30183,#30184,#30185),(#30186,#30187,#30188),(#30189,#30190,#30191)),
 .UNSPECIFIED.,.F.,.F.,.F.)
B_SPLINE_SURFACE_WITH_KNOTS((4,2,2,2,2,2,2,2,2,2,4),(3,3),(0.00618007368741724,
0.00707169626481771,0.00796331884221818,0.00885494141961865,0.00930075270831889,
0.00974656399701912,0.0101923752857194,0.0106381865744196,0.0115298091518201,
0.0124214317292205,0.013313054306621),(0.,1.),.UNSPECIFIED.)
GEOMETRIC_REPRESENTATION_ITEM()
RATIONAL_B_SPLINE_SURFACE(((1.,0.858045858703177,1.),(1.,0.866904822687482,
1.),(1.,0.875299209011426,1.),(1.,0.890836089594423,1.),(1.,0.898040712548752,
1.),(1.,0.910117038219606,1.),(1.,0.915056450314983,1.),(1.,0.920263585253285,
1.),(1.,0.921616129399948,1.),(1.,0.923410100119622,1.),(1.,0.923869223474666,
1.),(1.,0.923889498575711,1.),(1.,0.92344256786583,1.),(1.,0.921656854892037,
1.),(1.,0.920333354099966,1.),(1.,0.9152042866524,1.),(1.,0.910157237148985,
1.),(1.,0.898027307649231,1.),(1.,0.890964714100696,1.),(1.,0.875368043550207,
1.),(1.,0.86682243570435,1.),(1.,0.85805265757134,1.)))
REPRESENTATION_ITEM('')
SURFACE()
);
#461=(
BOUNDED_SURFACE()
B_SPLINE_SURFACE(3,2,((#30228,#30229,#30230),(#30231,#30232,#30233),(#30234,
#30235,#30236),(#30237,#30238,#30239),(#30240,#30241,#30242),(#30243,#30244,
#30245),(#30246,#30247,#30248),(#30249,#30250,#30251),(#30252,#30253,#30254),
(#30255,#30256,#30257),(#30258,#30259,#30260),(#30261,#30262,#30263),(#30264,
#30265,#30266),(#30267,#30268,#30269),(#30270,#30271,#30272),(#30273,#30274,
#30275),(#30276,#30277,#30278),(#30279,#30280,#30281),(#30282,#30283,#30284),
(#30285,#30286,#30287),(#30288,#30289,#30290),(#30291,#30292,#30293)),
 .UNSPECIFIED.,.F.,.F.,.F.)
B_SPLINE_SURFACE_WITH_KNOTS((4,2,2,2,2,2,2,2,2,2,4),(3,3),(0.00463173145868099,
0.0055550496708318,0.00644833560515975,0.00689497857232373,0.0073416215394877,
0.00823490747381566,0.00868155044097963,0.00912819340814361,0.0100214793424716,
0.0109147652767995,0.011838209828059),(-9.16721149006242E-5,1.00007252857048),
 .UNSPECIFIED.)
GEOMETRIC_REPRESENTATION_ITEM()
RATIONAL_B_SPLINE_SURFACE(((1.00002619145898,0.857135625077539,1.00002072159804),
(1.00002451884082,0.866259116387597,1.0000193982918),(1.00002289154787,
0.875135376031697,1.00001811084498),(1.00001998551899,0.890986650264669,
1.00001581171524),(1.00001868879555,0.898059779870719,1.00001478580134),
(1.00001701652053,0.90718139945745,1.00001346276657),(1.00001650323434,
0.909981178978598,1.00001305667579),(1.00001560966983,0.914855231051331,
1.00001234972454),(1.00001522637194,0.916945974201243,1.00001204647512),
(1.00001428784851,0.922065259968938,1.00001130395424),(1.00001395123475,
0.923901359098063,1.00001103763936),(1.0000139608147,0.923849104111275,
1.00001104521863),(1.00001404571456,0.923386007914237,1.00001111238788),
(1.00001437612857,0.921583726099594,1.00001137379776),(1.00001462510049,
0.920225679629222,1.00001157077404),(1.00001558266984,0.915002505660967,
1.00001232836327),(1.00001648988299,0.910054005470624,1.00001304611276),
(1.00001870584049,0.897966806240844,1.00001479928659),(1.000020028908,0.890749979859378,
1.00001584604283),(1.00002292411145,0.87495775415132,1.00001813660794),
(1.00002451487478,0.866280749609431,1.00001939515403),(1.00002619181141,
0.857133702726523,1.00002072187687)))
REPRESENTATION_ITEM('')
SURFACE()
);
#462=(
BOUNDED_SURFACE()
B_SPLINE_SURFACE(3,2,((#30330,#30331,#30332),(#30333,#30334,#30335),(#30336,
#30337,#30338),(#30339,#30340,#30341),(#30342,#30343,#30344),(#30345,#30346,
#30347),(#30348,#30349,#30350),(#30351,#30352,#30353),(#30354,#30355,#30356),
(#30357,#30358,#30359),(#30360,#30361,#30362),(#30363,#30364,#30365),(#30366,
#30367,#30368),(#30369,#30370,#30371),(#30372,#30373,#30374),(#30375,#30376,
#30377),(#30378,#30379,#30380),(#30381,#30382,#30383)),.UNSPECIFIED.,.F.,
 .F.,.F.)
B_SPLINE_SURFACE_WITH_KNOTS((4,2,2,2,2,2,2,2,4),(3,3),(0.00330583080240976,
0.0050987612729038,0.00599522650815083,0.00689169174339785,0.00733992436102137,
0.00778815697864488,0.0086846222138919,0.00958108744913893,0.010477552684386),
(0.,1.),.UNSPECIFIED.)
GEOMETRIC_REPRESENTATION_ITEM()
RATIONAL_B_SPLINE_SURFACE(((1.,0.858051573205352,1.),(1.,0.875590740245255,
1.),(1.,0.891984535276897,1.),(1.,0.910123535489779,1.),(1.,0.915171726878822,
1.),(1.,0.922080092984598,1.),(1.,0.923887406776032,1.),(1.,0.923875556180348,
1.),(1.,0.923415662237232,1.),(1.,0.921609909018457,1.),(1.,0.920278779497026,
1.),(1.,0.91513274798944,1.),(1.,0.910082531829078,1.),(1.,0.897961000925969,
1.),(1.,0.890907866965291,1.),(1.,0.875336477322621,1.),(1.,0.866807510696487,
1.),(1.,0.858055143785041,1.)))
REPRESENTATION_ITEM('')
SURFACE()
);
#463=(
BOUNDED_SURFACE()
B_SPLINE_SURFACE(3,2,((#30435,#30436,#30437),(#30438,#30439,#30440),(#30441,
#30442,#30443),(#30444,#30445,#30446),(#30447,#30448,#30449),(#30450,#30451,
#30452),(#30453,#30454,#30455),(#30456,#30457,#30458),(#30459,#30460,#30461),
(#30462,#30463,#30464),(#30465,#30466,#30467),(#30468,#30469,#30470),(#30471,
#30472,#30473),(#30474,#30475,#30476),(#30477,#30478,#30479),(#30480,#30481,
#30482),(#30483,#30484,#30485),(#30486,#30487,#30488),(#30489,#30490,#30491),
(#30492,#30493,#30494),(#30495,#30496,#30497),(#30498,#30499,#30500)),
 .UNSPECIFIED.,.F.,.F.,.F.)
B_SPLINE_SURFACE_WITH_KNOTS((4,2,2,2,2,2,2,2,2,2,4),(3,3),(0.00463173145912357,
0.0055550496708318,0.00644833560515975,0.00689497857232373,0.0073416215394877,
0.00823490747381566,0.00868155044097963,0.00912819340814361,0.0100214793424716,
0.0109147652767995,0.0118382098276163),(-9.16721145407206E-5,1.00007252857004),
 .UNSPECIFIED.)
GEOMETRIC_REPRESENTATION_ITEM()
RATIONAL_B_SPLINE_SURFACE(((1.00002619145888,0.857135625090785,1.00002072159791),
(1.00002451884072,0.866259116396099,1.00001939829168),(1.00002289154778,
0.875135376035797,1.00001811084487),(1.00001998551891,0.890986650264622,
1.00001581171514),(1.00001868879548,0.898059779870952,1.00001478580125),
(1.00001701652046,0.907181399457448,1.00001346276649),(1.00001650323428,
0.909981178978704,1.00001305667571),(1.00001560966977,0.914855231051366,
1.00001234972447),(1.00001522637188,0.916945974201386,1.00001204647505),
(1.00001428784846,0.922065259968851,1.00001130395417),(1.00001395123469,
0.923901359098042,1.0000110376393),(1.00001396081465,0.923849104111378,
1.00001104521856),(1.00001404571451,0.923386007914241,1.00001111238781),
(1.00001437612851,0.921583726099716,1.00001137379769),(1.00001462510043,
0.920225679629301,1.00001157077397),(1.00001558266978,0.915002505661001,
1.00001232836319),(1.00001648988293,0.910054005470596,1.00001304611268),
(1.00001870584042,0.897966806241025,1.0000147992865),(1.00002002890792,
0.890749979859465,1.00001584604273),(1.00002292411136,0.874957754155268,
1.00001813660783),(1.00002451487468,0.866280749617856,1.00001939515391),
(1.0000261918113,0.857133702739791,1.00002072187674)))
REPRESENTATION_ITEM('')
SURFACE()
);
#464=(
BOUNDED_SURFACE()
B_SPLINE_SURFACE(3,2,((#30537,#30538,#30539),(#30540,#30541,#30542),(#30543,
#30544,#30545),(#30546,#30547,#30548),(#30549,#30550,#30551),(#30552,#30553,
#30554),(#30555,#30556,#30557),(#30558,#30559,#30560),(#30561,#30562,#30563),
(#30564,#30565,#30566),(#30567,#30568,#30569),(#30570,#30571,#30572),(#30573,
#30574,#30575),(#30576,#30577,#30578),(#30579,#30580,#30581),(#30582,#30583,
#30584),(#30585,#30586,#30587),(#30588,#30589,#30590)),.UNSPECIFIED.,.F.,
 .F.,.F.)
B_SPLINE_SURFACE_WITH_KNOTS((4,2,2,2,2,2,2,2,4),(3,3),(0.0033058308024097,
0.00509876127290375,0.00599522650815077,0.00689169174339779,0.0073399243610213,
0.00778815697864482,0.00868462221389184,0.00958108744913886,0.0104775526843859),
(0.,1.),.UNSPECIFIED.)
GEOMETRIC_REPRESENTATION_ITEM()
RATIONAL_B_SPLINE_SURFACE(((1.,0.858051573205352,1.),(1.,0.875590740245157,
1.),(1.,0.891984535277027,1.),(1.,0.91012353548971,1.),(1.,0.915171726878704,
1.),(1.,0.922080092984716,1.),(1.,0.923887406776032,1.),(1.,0.923875556180348,
1.),(1.,0.923415662237307,1.),(1.,0.921609909018382,1.),(1.,0.920278779497094,
1.),(1.,0.915132747989309,1.),(1.,0.910082531829295,1.),(1.,0.897961000925752,
1.),(1.,0.890907866965658,1.),(1.,0.875336477322253,1.),(1.,0.866807510696761,
1.),(1.,0.858055143785041,1.)))
REPRESENTATION_ITEM('')
SURFACE()
);
#465=(
BOUNDED_SURFACE()
B_SPLINE_SURFACE(3,2,((#30642,#30643,#30644),(#30645,#30646,#30647),(#30648,
#30649,#30650),(#30651,#30652,#30653),(#30654,#30655,#30656),(#30657,#30658,
#30659),(#30660,#30661,#30662),(#30663,#30664,#30665),(#30666,#30667,#30668),
(#30669,#30670,#30671),(#30672,#30673,#30674),(#30675,#30676,#30677),(#30678,
#30679,#30680),(#30681,#30682,#30683),(#30684,#30685,#30686),(#30687,#30688,
#30689),(#30690,#30691,#30692),(#30693,#30694,#30695),(#30696,#30697,#30698),
(#30699,#30700,#30701),(#30702,#30703,#30704),(#30705,#30706,#30707)),
 .UNSPECIFIED.,.F.,.F.,.F.)
B_SPLINE_SURFACE_WITH_KNOTS((4,2,2,2,2,2,2,2,2,2,4),(3,3),(0.00618007368741721,
0.00707169626481767,0.00796331884221814,0.00885494141961861,0.00930075270831885,
0.00974656399701908,0.0101923752857193,0.0106381865744195,0.01152980915182,
0.0124214317292205,0.013313054306621),(0.,1.),.UNSPECIFIED.)
GEOMETRIC_REPRESENTATION_ITEM()
RATIONAL_B_SPLINE_SURFACE(((1.,0.858045858703177,1.),(1.,0.86690482268742,
1.),(1.,0.875299209011509,1.),(1.,0.890836089594339,1.),(1.,0.898040712548885,
1.),(1.,0.910117038219473,1.),(1.,0.915056450314664,1.),(1.,0.920263585253445,
1.),(1.,0.921616129400065,1.),(1.,0.923410100119505,1.),(1.,0.923869223474666,
1.),(1.,0.923889498575711,1.),(1.,0.923442567865973,1.),(1.,0.921656854891893,
1.),(1.,0.92033335410005,1.),(1.,0.915204286652234,1.),(1.,0.910157237148985,
1.),(1.,0.898027307649231,1.),(1.,0.890964714100597,1.),(1.,0.875368043550308,
1.),(1.,0.866822435704274,1.),(1.,0.85805265757134,1.)))
REPRESENTATION_ITEM('')
SURFACE()
);
#466=(
BOUNDED_SURFACE()
B_SPLINE_SURFACE(3,2,((#30744,#30745,#30746),(#30747,#30748,#30749),(#30750,
#30751,#30752),(#30753,#30754,#30755),(#30756,#30757,#30758),(#30759,#30760,
#30761),(#30762,#30763,#30764),(#30765,#30766,#30767),(#30768,#30769,#30770),
(#30771,#30772,#30773),(#30774,#30775,#30776),(#30777,#30778,#30779),(#30780,
#30781,#30782),(#30783,#30784,#30785),(#30786,#30787,#30788),(#30789,#30790,
#30791),(#30792,#30793,#30794),(#30795,#30796,#30797),(#30798,#30799,#30800),
(#30801,#30802,#30803),(#30804,#30805,#30806),(#30807,#30808,#30809)),
 .UNSPECIFIED.,.F.,.F.,.F.)
B_SPLINE_SURFACE_WITH_KNOTS((4,2,2,2,2,2,2,2,2,2,4),(3,3),(0.00463173145890188,
0.0055550496708318,0.00644833560515975,0.00689497857232372,0.0073416215394877,
0.00823490747381565,0.00868155044097963,0.00912819340814361,0.0100214793424716,
0.0109147652767995,0.0118382098278381),(-9.16721146127048E-5,1.00007252857026),
 .UNSPECIFIED.)
GEOMETRIC_REPRESENTATION_ITEM()
RATIONAL_B_SPLINE_SURFACE(((1.0000261914589,0.857135625084157,1.00002072159798),
(1.00002451884074,0.86625911639194,1.00001939829174),(1.0000228915478,0.875135376033654,
1.00001811084493),(1.00001998551893,0.890986650264758,1.00001581171519),
(1.00001868879549,0.89805977987109,1.00001478580129),(1.00001701652048,
0.907181399457338,1.00001346276653),(1.00001650323429,0.909981178978669,
1.00001305667575),(1.00001560966978,0.914855231051349,1.00001234972451),
(1.0000152263719,0.916945974201319,1.00001204647509),(1.00001428784847,
0.922065259968911,1.0000113039542),(1.00001395123471,0.923901359098102,
1.00001103763933),(1.00001396081466,0.923849104111314,1.00001104521859),
(1.00001404571452,0.923386007914268,1.00001111238785),(1.00001437612852,
0.921583726099643,1.00001137379773),(1.00001462510045,0.920225679629262,
1.00001157077401),(1.00001558266979,0.915002505661011,1.00001232836323),
(1.00001648988294,0.910054005470637,1.00001304611272),(1.00001870584043,
0.897966806240929,1.00001479928655),(1.00002002890793,0.890749979859433,
1.00001584604278),(1.00002292411138,0.874957754153303,1.00001813660789),
(1.0000245148747,0.866280749613647,1.00001939515397),(1.00002619181133,
0.857133702733158,1.0000207218768)))
REPRESENTATION_ITEM('')
SURFACE()
);
#467=(
BOUNDED_SURFACE()
B_SPLINE_SURFACE(3,2,((#30846,#30847,#30848),(#30849,#30850,#30851),(#30852,
#30853,#30854),(#30855,#30856,#30857),(#30858,#30859,#30860),(#30861,#30862,
#30863),(#30864,#30865,#30866),(#30867,#30868,#30869),(#30870,#30871,#30872),
(#30873,#30874,#30875),(#30876,#30877,#30878),(#30879,#30880,#30881),(#30882,
#30883,#30884),(#30885,#30886,#30887),(#30888,#30889,#30890),(#30891,#30892,
#30893),(#30894,#30895,#30896),(#30897,#30898,#30899)),.UNSPECIFIED.,.F.,
 .F.,.F.)
B_SPLINE_SURFACE_WITH_KNOTS((4,2,2,2,2,2,2,2,4),(3,3),(0.00330583080240973,
0.00509876127290377,0.0059952265081508,0.00689169174339782,0.00733992436102133,
0.00778815697864484,0.00868462221389187,0.00958108744913889,0.0104775526843859),
(0.,1.),.UNSPECIFIED.)
GEOMETRIC_REPRESENTATION_ITEM()
RATIONAL_B_SPLINE_SURFACE(((1.,0.858051573205352,1.),(1.,0.875590740245257,
1.),(1.,0.891984535276895,1.),(1.,0.910123535489777,1.),(1.,0.915171726878671,
1.),(1.,0.92208009298475,1.),(1.,0.923887406775965,1.),(1.,0.923875556180381,
1.),(1.,0.923415662237265,1.),(1.,0.921609909018423,1.),(1.,0.920278779497103,
1.),(1.,0.915132747989292,1.),(1.,0.910082531829227,1.),(1.,0.897961000925819,
1.),(1.,0.890907866965258,1.),(1.,0.875336477322655,1.),(1.,0.86680751069646,
1.),(1.,0.858055143785041,1.)))
REPRESENTATION_ITEM('')
SURFACE()
);
#468=(
BOUNDED_SURFACE()
B_SPLINE_SURFACE(3,2,((#30951,#30952,#30953),(#30954,#30955,#30956),(#30957,
#30958,#30959),(#30960,#30961,#30962),(#30963,#30964,#30965),(#30966,#30967,
#30968),(#30969,#30970,#30971),(#30972,#30973,#30974),(#30975,#30976,#30977),
(#30978,#30979,#30980),(#30981,#30982,#30983),(#30984,#30985,#30986),(#30987,
#30988,#30989),(#30990,#30991,#30992),(#30993,#30994,#30995),(#30996,#30997,
#30998),(#30999,#31000,#31001),(#31002,#31003,#31004),(#31005,#31006,#31007),
(#31008,#31009,#31010),(#31011,#31012,#31013),(#31014,#31015,#31016)),
 .UNSPECIFIED.,.F.,.F.,.F.)
B_SPLINE_SURFACE_WITH_KNOTS((4,2,2,2,2,2,2,2,2,2,4),(3,3),(0.00463173145913793,
0.0055550496708318,0.00644833560515975,0.00689497857232373,0.0073416215394877,
0.00823490747381566,0.00868155044097963,0.00912819340814361,0.0100214793424716,
0.0109147652767995,0.011838209827602),(-9.1672114921884E-5,1.00007252857003),
 .UNSPECIFIED.)
GEOMETRIC_REPRESENTATION_ITEM()
RATIONAL_B_SPLINE_SURFACE(((1.00002619145899,0.857135625091139,1.00002072159791),
(1.00002451884082,0.866259116396527,1.00001939829167),(1.00002289154787,
0.875135376035635,1.00001811084487),(1.000019985519,0.890986650264817,1.00001581171514),
(1.00001868879555,0.898059779870914,1.00001478580124),(1.00001701652053,
0.907181399457414,1.00001346276649),(1.00001650323435,0.909981178978654,
1.00001305667571),(1.00001560966984,0.914855231051352,1.00001234972447),
(1.00001522637195,0.91694597420133,1.00001204647505),(1.00001428784852,
0.922065259968872,1.00001130395417),(1.00001395123475,0.923901359098063,
1.00001103763929),(1.00001396081471,0.923849104111325,1.00001104521856),
(1.00001404571456,0.923386007914212,1.00001111238781),(1.00001437612857,
0.921583726099687,1.00001137379769),(1.00001462510049,0.92022567962924,
1.00001157077397),(1.00001558266985,0.915002505661038,1.00001232836319),
(1.000016489883,0.910054005470647,1.00001304611267),(1.0000187058405,0.897966806240904,
1.0000147992865),(1.000020028908,0.890749979859459,1.00001584604273),(1.00002292411146,
0.874957754155313,1.00001813660783),(1.00002451487478,0.866280749618104,
1.00001939515391),(1.00002619181141,0.857133702740162,1.00002072187673)))
REPRESENTATION_ITEM('')
SURFACE()
);
#469=(
BOUNDED_SURFACE()
B_SPLINE_SURFACE(3,2,((#31053,#31054,#31055),(#31056,#31057,#31058),(#31059,
#31060,#31061),(#31062,#31063,#31064),(#31065,#31066,#31067),(#31068,#31069,
#31070),(#31071,#31072,#31073),(#31074,#31075,#31076),(#31077,#31078,#31079),
(#31080,#31081,#31082),(#31083,#31084,#31085),(#31086,#31087,#31088),(#31089,
#31090,#31091),(#31092,#31093,#31094),(#31095,#31096,#31097),(#31098,#31099,
#31100),(#31101,#31102,#31103),(#31104,#31105,#31106)),.UNSPECIFIED.,.F.,
 .F.,.F.)
B_SPLINE_SURFACE_WITH_KNOTS((4,2,2,2,2,2,2,2,4),(3,3),(0.00330583080240977,
0.00509876127290382,0.00599522650815085,0.00689169174339787,0.00733992436102138,
0.0077881569786449,0.00868462221389192,0.00958108744913895,0.010477552684386),
(0.,1.),.UNSPECIFIED.)
GEOMETRIC_REPRESENTATION_ITEM()
RATIONAL_B_SPLINE_SURFACE(((1.,0.858051573205352,1.),(1.,0.875590740245157,
1.),(1.,0.891984535277027,1.),(1.,0.91012353548971,1.),(1.,0.915171726878721,
1.),(1.,0.922080092984699,1.),(1.,0.923887406775799,1.),(1.,0.923875556180464,
1.),(1.,0.923415662237299,1.),(1.,0.92160990901839,1.),(1.,0.920278779497093,
1.),(1.,0.915132747989307,1.),(1.,0.910082531829311,1.),(1.,0.897961000925736,
1.),(1.,0.890907866965291,1.),(1.,0.875336477322621,1.),(1.,0.866807510696485,
1.),(1.,0.858055143785041,1.)))
REPRESENTATION_ITEM('')
SURFACE()
);
#527=FACE_BOUND('',#2028,.T.);
#528=FACE_BOUND('',#2033,.T.);
#529=FACE_BOUND('',#2036,.T.);
#530=FACE_BOUND('',#2037,.T.);
#531=FACE_BOUND('',#2038,.T.);
#532=FACE_BOUND('',#2039,.T.);
#533=FACE_BOUND('',#2040,.T.);
#534=FACE_BOUND('',#2042,.T.);
#535=FACE_BOUND('',#2046,.T.);
#536=FACE_BOUND('',#2048,.T.);
#537=FACE_BOUND('',#2049,.T.);
#538=FACE_BOUND('',#2050,.T.);
#539=FACE_BOUND('',#2051,.T.);
#540=FACE_BOUND('',#2052,.T.);
#541=FACE_BOUND('',#2061,.T.);
#542=FACE_BOUND('',#2064,.T.);
#639=B_SPLINE_CURVE_WITH_KNOTS('',3,(#28035,#28036,#28037,#28038,#28039,
#28040,#28041,#28042),.UNSPECIFIED.,.F.,.F.,(4,2,2,4),(-0.269775582616464,
-0.253421285918584,-0.22590943032474,-0.222790814239488),.UNSPECIFIED.);
#640=B_SPLINE_CURVE_WITH_KNOTS('',3,(#28046,#28047,#28048,#28049,#28050,
#28051),.UNSPECIFIED.,.F.,.F.,(4,2,4),(-0.0146617576038819,-0.00732399879407159,
0.),.UNSPECIFIED.);
#641=B_SPLINE_CURVE_WITH_KNOTS('',3,(#28055,#28056,#28057,#28058,#28059,
#28060),.UNSPECIFIED.,.F.,.F.,(4,2,4),(-0.0146584345608506,-0.00733705776971509,
-2.0365131182774E-6),.UNSPECIFIED.);
#642=B_SPLINE_CURVE_WITH_KNOTS('',3,(#28063,#28064,#28065,#28066,#28067,
#28068),.UNSPECIFIED.,.F.,.F.,(4,2,4),(-0.131101349644823,-0.108436635501131,
-0.0855680085348876),.UNSPECIFIED.);
#643=B_SPLINE_CURVE_WITH_KNOTS('',3,(#28074,#28075,#28076,#28077,#28078,
#28079),.UNSPECIFIED.,.F.,.F.,(4,2,4),(-0.131101349644766,-0.108436635501081,
-0.0855680085348502),.UNSPECIFIED.);
#644=B_SPLINE_CURVE_WITH_KNOTS('',3,(#28083,#28084,#28085,#28086,#28087,
#28088,#28089,#28090),.UNSPECIFIED.,.F.,.F.,(4,2,2,4),(-0.269775582616478,
-0.253421285918598,-0.225909430324752,-0.222790814239499),.UNSPECIFIED.);
#645=B_SPLINE_CURVE_WITH_KNOTS('',3,(#28094,#28095,#28096,#28097,#28098,
#28099),.UNSPECIFIED.,.F.,.F.,(4,2,4),(-0.0146618387590922,-0.00732404409132206,
-1.5273897580742E-8),.UNSPECIFIED.);
#646=B_SPLINE_CURVE_WITH_KNOTS('',3,(#28102,#28103,#28104,#28105,#28106,
#28107),.UNSPECIFIED.,.F.,.F.,(4,2,4),(-0.0146570227865704,-0.00733642775269209,
-9.89091544272014E-7),.UNSPECIFIED.);
#647=B_SPLINE_CURVE_WITH_KNOTS('',3,(#28113,#28114,#28115,#28116,#28117,
#28118),.UNSPECIFIED.,.F.,.F.,(4,2,4),(-0.131101349644767,-0.108436635501072,
-0.0855680085348483),.UNSPECIFIED.);
#648=B_SPLINE_CURVE_WITH_KNOTS('',3,(#28122,#28123,#28124,#28125,#28126,
#28127,#28128,#28129),.UNSPECIFIED.,.F.,.F.,(4,2,2,4),(-0.269775582616373,
-0.253421285918502,-0.225909430324671,-0.222790814239419),.UNSPECIFIED.);
#649=B_SPLINE_CURVE_WITH_KNOTS('',3,(#28133,#28134,#28135,#28136,#28137,
#28138),.UNSPECIFIED.,.F.,.F.,(4,2,4),(-0.0146618152090308,-0.00732403346802824,
-1.542284065216E-8),.UNSPECIFIED.);
#650=B_SPLINE_CURVE_WITH_KNOTS('',3,(#28141,#28142,#28143,#28144,#28145,
#28146),.UNSPECIFIED.,.F.,.F.,(4,2,4),(-0.0146570266562873,-0.00733642653042715,
-9.88349770934815E-7),.UNSPECIFIED.);
#651=B_SPLINE_CURVE_WITH_KNOTS('',3,(#28152,#28153,#28154,#28155,#28156,
#28157),.UNSPECIFIED.,.F.,.F.,(4,2,4),(-0.131101349644736,-0.108436635501052,
-0.0855680085348304),.UNSPECIFIED.);
#652=B_SPLINE_CURVE_WITH_KNOTS('',3,(#28161,#28162,#28163,#28164,#28165,
#28166,#28167,#28168),.UNSPECIFIED.,.F.,.F.,(4,2,2,4),(-0.269775582616424,
-0.25342128591855,-0.225909430324718,-0.222790814239467),.UNSPECIFIED.);
#653=B_SPLINE_CURVE_WITH_KNOTS('',3,(#28172,#28173,#28174,#28175,#28176,
#28177),.UNSPECIFIED.,.F.,.F.,(4,2,4),(-0.01466175760385,-0.00732399879408571,
0.),.UNSPECIFIED.);
#654=B_SPLINE_CURVE_WITH_KNOTS('',3,(#28182,#28183,#28184,#28185,#28186,
#28187),.UNSPECIFIED.,.F.,.F.,(4,2,4),(-0.0146584345606624,-0.00733705776964583,
-2.03651308581504E-6),.UNSPECIFIED.);
#655=B_SPLINE_CURVE_WITH_KNOTS('',3,(#28193,#28194,#28195,#28196,#28197,
#28198,#28199,#28200),.UNSPECIFIED.,.F.,.F.,(4,2,2,4),(-0.269775582616442,
-0.253421285918564,-0.225909430324722,-0.22279081423947),.UNSPECIFIED.);
#656=B_SPLINE_CURVE_WITH_KNOTS('',3,(#28204,#28205,#28206,#28207,#28208,
#28209),.UNSPECIFIED.,.F.,.F.,(4,2,4),(-0.0146618387596521,-0.0073240440914945,
-1.52738934607738E-8),.UNSPECIFIED.);
#657=B_SPLINE_CURVE_WITH_KNOTS('',3,(#28213,#28214,#28215,#28216,#28217,
#28218),.UNSPECIFIED.,.F.,.F.,(4,2,4),(-0.0146570266563023,-0.00733642653042518,
-9.88349766483515E-7),.UNSPECIFIED.);
#658=B_SPLINE_CURVE_WITH_KNOTS('',3,(#28221,#28222,#28223,#28224,#28225,
#28226),.UNSPECIFIED.,.F.,.F.,(4,2,4),(-0.131101349644881,-0.108436635501189,
-0.0855680085349263),.UNSPECIFIED.);
#659=B_SPLINE_CURVE_WITH_KNOTS('',3,(#28232,#28233,#28234,#28235,#28236,
#28237),.UNSPECIFIED.,.F.,.F.,(4,2,4),(-0.131101349644726,-0.108436635501036,
-0.0855680085348208),.UNSPECIFIED.);
#660=B_SPLINE_CURVE_WITH_KNOTS('',3,(#28241,#28242,#28243,#28244,#28245,
#28246,#28247,#28248),.UNSPECIFIED.,.F.,.F.,(4,2,2,4),(-0.26977558261646,
-0.253421285918579,-0.225909430324732,-0.222790814239478),.UNSPECIFIED.);
#661=B_SPLINE_CURVE_WITH_KNOTS('',3,(#28252,#28253,#28254,#28255,#28256,
#28257),.UNSPECIFIED.,.F.,.F.,(4,2,4),(-0.01466175760387,-0.0073239987940538,
0.),.UNSPECIFIED.);
#662=B_SPLINE_CURVE_WITH_KNOTS('',3,(#28260,#28261,#28262,#28263,#28264,
#28265),.UNSPECIFIED.,.F.,.F.,(4,2,4),(-0.0146584345608046,-0.00733705776969051,
-2.03651309724679E-6),.UNSPECIFIED.);
#663=B_SPLINE_CURVE_WITH_KNOTS('',3,(#28271,#28272,#28273,#28274,#28275,
#28276),.UNSPECIFIED.,.F.,.F.,(4,2,4),(-0.131101349644819,-0.108436635501123,
-0.0855680085348801),.UNSPECIFIED.);
#664=B_SPLINE_CURVE_WITH_KNOTS('',3,(#28280,#28281,#28282,#28283,#28284,
#28285,#28286,#28287),.UNSPECIFIED.,.F.,.F.,(4,2,2,4),(-0.269775582616506,
-0.253421285918626,-0.225909430324778,-0.222790814239526),.UNSPECIFIED.);
#665=B_SPLINE_CURVE_WITH_KNOTS('',3,(#28291,#28292,#28293,#28294,#28295,
#28296),.UNSPECIFIED.,.F.,.F.,(4,2,4),(-0.0146618387590248,-0.00732404409122351,
-1.52738976744171E-8),.UNSPECIFIED.);
#666=B_SPLINE_CURVE_WITH_KNOTS('',3,(#28299,#28300,#28301,#28302,#28303,
#28304),.UNSPECIFIED.,.F.,.F.,(4,2,4),(-0.0146570227863867,-0.00733642775264506,
-9.89091543862619E-7),.UNSPECIFIED.);
#667=B_SPLINE_CURVE_WITH_KNOTS('',3,(#28310,#28311,#28312,#28313,#28314,
#28315),.UNSPECIFIED.,.F.,.F.,(4,2,4),(-0.131101349644802,-0.108436635501105,
-0.0855680085348711),.UNSPECIFIED.);
#668=B_SPLINE_CURVE_WITH_KNOTS('',3,(#28319,#28320,#28321,#28322,#28323,
#28324,#28325,#28326),.UNSPECIFIED.,.F.,.F.,(4,2,2,4),(-0.269775582616408,
-0.253421285918538,-0.225909430324714,-0.222790814239463),.UNSPECIFIED.);
#669=B_SPLINE_CURVE_WITH_KNOTS('',3,(#28330,#28331,#28332,#28333,#28334,
#28335),.UNSPECIFIED.,.F.,.F.,(4,2,4),(-0.0146618152087878,-0.00732403346791597,
-1.54228420676944E-8),.UNSPECIFIED.);
#670=B_SPLINE_CURVE_WITH_KNOTS('',3,(#28338,#28339,#28340,#28341,#28342,
#28343),.UNSPECIFIED.,.F.,.F.,(4,2,4),(-0.0146570266560919,-0.00733642653037241,
-9.88349764358479E-7),.UNSPECIFIED.);
#671=B_SPLINE_CURVE_WITH_KNOTS('',3,(#28349,#28350,#28351,#28352,#28353,
#28354),.UNSPECIFIED.,.F.,.F.,(4,2,4),(-0.131101349644797,-0.108436635501117,
-0.0855680085348727),.UNSPECIFIED.);
#672=B_SPLINE_CURVE_WITH_KNOTS('',3,(#28358,#28359,#28360,#28361,#28362,
#28363,#28364,#28365),.UNSPECIFIED.,.F.,.F.,(4,2,2,4),(-0.269775582616456,
-0.253421285918579,-0.225909430324743,-0.222790814239492),.UNSPECIFIED.);
#673=B_SPLINE_CURVE_WITH_KNOTS('',3,(#28369,#28370,#28371,#28372,#28373,
#28374),.UNSPECIFIED.,.F.,.F.,(4,2,4),(-0.0146617576042861,-0.00732399879426565,
0.),.UNSPECIFIED.);
#674=B_SPLINE_CURVE_WITH_KNOTS('',3,(#28377,#28378,#28379,#28380,#28381,
#28382),.UNSPECIFIED.,.F.,.F.,(4,2,4),(-0.0146584345607558,-0.00733705776967299,
-2.03651308879836E-6),.UNSPECIFIED.);
#675=B_SPLINE_CURVE_WITH_KNOTS('',3,(#28415,#28416,#28417,#28418,#28419,
#28420),.UNSPECIFIED.,.F.,.F.,(4,2,4),(-0.131101349644817,-0.108436635501125,
-0.085568008534881),.UNSPECIFIED.);
#676=B_SPLINE_CURVE_WITH_KNOTS('',3,(#28422,#28423,#28424,#28425,#28426,
#28427,#28428,#28429),.UNSPECIFIED.,.F.,.F.,(4,2,2,4),(-0.269775582616367,
-0.253421285918495,-0.225909430324662,-0.222790814239412),.UNSPECIFIED.);
#677=B_SPLINE_CURVE_WITH_KNOTS('',3,(#28433,#28434,#28435,#28436,#28437,
#28438),.UNSPECIFIED.,.F.,.F.,(4,2,4),(-0.0146618387595114,-0.00732404409148471,
-1.52738936567975E-8),.UNSPECIFIED.);
#678=B_SPLINE_CURVE_WITH_KNOTS('',3,(#28441,#28442,#28443,#28444,#28445,
#28446),.UNSPECIFIED.,.F.,.F.,(4,2,4),(-0.0146570266563214,-0.00733642653043949,
-9.88349770927877E-7),.UNSPECIFIED.);
#679=B_SPLINE_CURVE_WITH_KNOTS('',3,(#28464,#28465,#28466,#28467,#28468,
#28469,#28470,#28471,#28472,#28473,#28474,#28475,#28476,#28477,#28478,#28479,
#28480,#28481),.UNSPECIFIED.,.F.,.F.,(4,2,2,2,2,2,2,2,4),(-1.13175700460039,
-1.06102166552592,-0.99028632645144,-0.919552039950867,-0.848817753450294,
-0.77808346694972,-0.707349180449147,-0.636613841374672,-0.565878502300197),
 .UNSPECIFIED.);
#680=B_SPLINE_CURVE_WITH_KNOTS('',3,(#28482,#28483,#28484,#28485,#28486,
#28487,#28488,#28489,#28490,#28491,#28492,#28493,#28494,#28495,#28496,#28497,
#28498,#28499),.UNSPECIFIED.,.F.,.F.,(4,2,2,2,2,2,2,2,4),(-0.565878502300197,
-0.495143163225721,-0.424407824151245,-0.353673537650672,-0.282939251150098,
-0.212204964649525,-0.141470678148952,-0.0707353390744758,0.),
 .UNSPECIFIED.);
#681=B_SPLINE_CURVE_WITH_KNOTS('',3,(#28502,#28503,#28504,#28505,#28506,
#28507,#28508,#28509,#28510,#28511,#28512,#28513,#28514,#28515,#28516,#28517,
#28518,#28519),.UNSPECIFIED.,.F.,.F.,(4,2,2,2,2,2,2,2,4),(-1.13175700460039,
-1.06102166552592,-0.990286326451441,-0.919552039950867,-0.848817753450294,
-0.778083466949721,-0.707349180449147,-0.636613841374672,-0.565878502300197),
 .UNSPECIFIED.);
#682=B_SPLINE_CURVE_WITH_KNOTS('',3,(#28520,#28521,#28522,#28523,#28524,
#28525,#28526,#28527,#28528,#28529,#28530,#28531,#28532,#28533,#28534,#28535,
#28536,#28537),.UNSPECIFIED.,.F.,.F.,(4,2,2,2,2,2,2,2,4),(-0.565878502300197,
-0.495143163225721,-0.424407824151246,-0.353673537650672,-0.282939251150099,
-0.212204964649525,-0.141470678148952,-0.070735339074476,0.),
 .UNSPECIFIED.);
#683=B_SPLINE_CURVE_WITH_KNOTS('',3,(#28540,#28541,#28542,#28543,#28544,
#28545,#28546,#28547,#28548,#28549,#28550,#28551,#28552,#28553,#28554,#28555,
#28556,#28557),.UNSPECIFIED.,.F.,.F.,(4,2,2,2,2,2,2,2,4),(-1.13175700460039,
-1.06102166552592,-0.990286326451441,-0.919552039950867,-0.848817753450294,
-0.77808346694972,-0.707349180449147,-0.636613841374672,-0.565878502300197),
 .UNSPECIFIED.);
#684=B_SPLINE_CURVE_WITH_KNOTS('',3,(#28558,#28559,#28560,#28561,#28562,
#28563,#28564,#28565,#28566,#28567,#28568,#28569,#28570,#28571,#28572,#28573,
#28574,#28575),.UNSPECIFIED.,.F.,.F.,(4,2,2,2,2,2,2,2,4),(-0.565878502300197,
-0.495143163225721,-0.424407824151245,-0.353673537650672,-0.282939251150098,
-0.212204964649525,-0.141470678148952,-0.0707353390744758,0.),
 .UNSPECIFIED.);
#685=B_SPLINE_CURVE_WITH_KNOTS('',3,(#28578,#28579,#28580,#28581,#28582,
#28583,#28584,#28585,#28586,#28587,#28588,#28589,#28590,#28591,#28592,#28593,
#28594,#28595),.UNSPECIFIED.,.F.,.F.,(4,2,2,2,2,2,2,2,4),(-1.1317570046004,
-1.06102166552592,-0.990286326451445,-0.919552039950871,-0.848817753450298,
-0.778083466949725,-0.707349180449151,-0.636613841374674,-0.565878502300198),
 .UNSPECIFIED.);
#686=B_SPLINE_CURVE_WITH_KNOTS('',3,(#28596,#28597,#28598,#28599,#28600,
#28601,#28602,#28603,#28604,#28605,#28606,#28607,#28608,#28609,#28610,#28611,
#28612,#28613),.UNSPECIFIED.,.F.,.F.,(4,2,2,2,2,2,2,2,4),(-0.565878502300198,
-0.495143163225722,-0.424407824151246,-0.353673537650672,-0.282939251150099,
-0.212204964649525,-0.141470678148952,-0.0707353390744759,0.),
 .UNSPECIFIED.);
#687=B_SPLINE_CURVE_WITH_KNOTS('',3,(#28616,#28617,#28618,#28619,#28620,
#28621,#28622,#28623,#28624,#28625,#28626,#28627,#28628,#28629,#28630,#28631,
#28632,#28633),.UNSPECIFIED.,.F.,.F.,(4,2,2,2,2,2,2,2,4),(-0.848817753450289,
-0.778083466949716,-0.707349180449143,-0.636613841374668,-0.565878502300194,
-0.495143163225718,-0.424407824151242,-0.353673537650669,-0.282939251150097),
 .UNSPECIFIED.);
#688=B_SPLINE_CURVE_WITH_KNOTS('',3,(#28634,#28635,#28636,#28637,#28638,
#28639,#28640,#28641,#28642,#28643,#28644,#28645,#28646,#28647,#28648,#28649,
#28650,#28651,#28652),.UNSPECIFIED.,.F.,.F.,(4,2,2,2,3,2,2,2,4),(-0.282939251150097,
-0.212204964649524,-0.141470678148952,-0.0707353390744758,0.,0.0707353390744749,
0.14147067814895,0.212204964649523,0.282939251150096),.UNSPECIFIED.);
#689=B_SPLINE_CURVE_WITH_KNOTS('',3,(#28663,#28664,#28665,#28666,#28667,
#28668,#28669,#28670,#28671,#28672,#28673,#28674,#28675,#28676,#28677,#28678,
#28679,#28680,#28681,#28682,#28683,#28684),.UNSPECIFIED.,.F.,.F.,(4,2,2,
2,2,2,2,2,2,2,4),(1.03259187272008E-9,0.000910225950447462,0.00182045190089492,
0.00227556487611866,0.00273067785134239,0.00364090380178987,0.00409601677701361,
0.00455112975223734,0.00546135570268482,0.0063715816531323,0.00728180748389903),
 .UNSPECIFIED.);
#690=B_SPLINE_CURVE_WITH_KNOTS('',3,(#28685,#28686,#28687,#28688,#28689,
#28690,#28691,#28692,#28693,#28694,#28695,#28696,#28697,#28698,#28699,#28700,
#28701,#28702,#28703,#28704,#28705,#28706,#28707,#28708,#28709,#28710,#28711,
#28712,#28713,#28714,#28715,#28716,#28717,#28718,#28719,#28720,#28721,#28722,
#28723,#28724,#28725,#28726,#28727,#28728,#28729,#28730,#28731,#28732,#28733,
#28734,#28735,#28736,#28737,#28738,#28739,#28740,#28741,#28742,#28743,#28744,
#28745,#28746,#28747,#28748,#28749,#28750,#28751,#28752,#28753,#28754,#28755,
#28756,#28757,#28758,#28759,#28760,#28761,#28762,#28763,#28764,#28765,#28766,
#28767,#28768,#28769),.UNSPECIFIED.,.F.,.F.,(4,3,3,3,3,3,3,3,3,3,3,3,3,
3,3,3,3,3,3,3,3,3,3,3,3,3,3,3,4),(1.27326789064134E-9,0.000305183030961356,
0.000618697405666451,0.000865973237167131,0.000907586176443212,0.00143258173570116,
0.00178321767141052,0.00181517235288642,0.00233679237650043,0.00270521777421962,
0.00272275852932964,0.0031677449805063,0.00317655161755125,0.00351188758019002,
0.00363034470577285,0.00363091529585842,0.00404743389245343,0.00446889752821537,
0.00453793088221607,0.00455651100281011,0.00512035053921118,0.00544551705865929,
0.00547872254023125,0.00584209036189708,0.00622546925989105,0.00635310323510251,
0.00664528416315127,0.00695298625517416,0.00726068834719705),
 .UNSPECIFIED.);
#691=B_SPLINE_CURVE_WITH_KNOTS('',3,(#28770,#28771,#28772,#28773,#28774,
#28775,#28776,#28777,#28778,#28779,#28780,#28781,#28782,#28783,#28784,#28785,
#28786,#28787,#28788,#28789,#28790,#28791),.UNSPECIFIED.,.F.,.F.,(4,2,2,
2,2,2,2,2,2,2,4),(1.03259179694757E-9,0.000910225950447464,0.00182045190089493,
0.00227556487611866,0.0027306778513424,0.00364090380178987,0.00409601677701361,
0.00455112975223735,0.00546135570268482,0.00637158165313229,0.00728180748389901),
 .UNSPECIFIED.);
#692=B_SPLINE_CURVE_WITH_KNOTS('',3,(#28792,#28793,#28794,#28795,#28796,
#28797,#28798,#28799,#28800,#28801,#28802,#28803,#28804,#28805,#28806,#28807,
#28808,#28809,#28810,#28811,#28812,#28813,#28814,#28815,#28816,#28817,#28818,
#28819,#28820,#28821,#28822,#28823,#28824,#28825,#28826,#28827,#28828,#28829,
#28830,#28831,#28832,#28833,#28834,#28835,#28836,#28837,#28838,#28839,#28840,
#28841,#28842,#28843,#28844,#28845,#28846,#28847,#28848,#28849,#28850,#28851,
#28852,#28853,#28854,#28855,#28856,#28857,#28858,#28859,#28860,#28861,#28862,
#28863,#28864,#28865,#28866,#28867,#28868,#28869,#28870,#28871,#28872,#28873),
 .UNSPECIFIED.,.F.,.F.,(4,3,3,3,3,3,3,3,3,3,3,3,3,3,3,3,3,3,3,3,3,3,3,3,
3,3,3,4),(1.28482073593457E-9,0.000305235153235769,0.000618823755187696,
0.000867705358119334,0.000909427513427647,0.00143855251726445,0.00178678626263729,
0.00181885502685529,0.00234189634471885,0.00271063977086651,0.00272828254028294,
0.00317414461806316,0.00358630275067258,0.00363771005371059,0.00363819037736454,
0.00409242381042441,0.00410208104893608,0.00444871693184629,0.00454713756713824,
0.0045656013242579,0.00518563856811733,0.00545656508056589,0.00548920795128179,
0.00599393750643838,0.00636599259399354,0.0064075598747639,0.00686713671046424,
0.00727541997337556),.UNSPECIFIED.);
#693=B_SPLINE_CURVE_WITH_KNOTS('',3,(#28874,#28875,#28876,#28877,#28878,
#28879,#28880,#28881,#28882,#28883,#28884,#28885,#28886,#28887,#28888,#28889,
#28890,#28891,#28892,#28893,#28894,#28895,#28896,#28897,#28898,#28899,#28900,
#28901,#28902,#28903,#28904,#28905,#28906,#28907,#28908,#28909,#28910,#28911,
#28912,#28913,#28914,#28915,#28916,#28917,#28918,#28919,#28920,#28921,#28922,
#28923,#28924,#28925,#28926,#28927,#28928,#28929,#28930,#28931,#28932,#28933,
#28934,#28935,#28936,#28937,#28938,#28939,#28940,#28941,#28942,#28943,#28944,
#28945,#28946,#28947,#28948,#28949,#28950,#28951,#28952,#28953,#28954,#28955,
#28956,#28957,#28958),.UNSPECIFIED.,.F.,.F.,(4,3,3,3,3,3,3,3,3,3,3,3,3,
3,3,3,3,3,3,3,3,3,3,3,3,3,3,3,4),(1.27326809408661E-9,0.00030518303086706,
0.000618697405474252,0.000865973237167092,0.000907586176443212,0.0014325817372093,
0.0017832176714105,0.00181517235288642,0.00233679237665264,0.00270521777421962,
0.00272275852932964,0.0031677449805063,0.00317655161755124,0.00351188758016664,
0.00363034470577285,0.00363091529585842,0.00404743389252427,0.00446889752836537,
0.00453793088221607,0.0045565110028101,0.00512035053941143,0.00544551705865929,
0.00547872254023127,0.00584209036189159,0.00622546925988722,0.00635310323510251,
0.00664528416314683,0.00695298625517191,0.007260688347197),
 .UNSPECIFIED.);
#694=B_SPLINE_CURVE_WITH_KNOTS('',3,(#28959,#28960,#28961,#28962,#28963,
#28964,#28965,#28966,#28967,#28968,#28969,#28970,#28971,#28972,#28973,#28974,
#28975,#28976,#28977,#28978,#28979,#28980),.UNSPECIFIED.,.F.,.F.,(4,2,2,
2,2,2,2,2,2,2,4),(1.03259185302256E-9,0.000910225950447462,0.00182045190089492,
0.00227556487611866,0.00273067785134239,0.00364090380178986,0.0040960167770136,
0.00455112975223734,0.00546135570268482,0.00637158165313229,0.00728180748389903),
 .UNSPECIFIED.);
#695=B_SPLINE_CURVE_WITH_KNOTS('',3,(#28981,#28982,#28983,#28984,#28985,
#28986,#28987,#28988,#28989,#28990,#28991,#28992,#28993,#28994,#28995,#28996,
#28997,#28998,#28999,#29000,#29001,#29002,#29003,#29004,#29005,#29006,#29007,
#29008,#29009,#29010,#29011,#29012,#29013,#29014,#29015,#29016,#29017,#29018,
#29019,#29020,#29021,#29022,#29023,#29024,#29025,#29026,#29027,#29028,#29029,
#29030,#29031,#29032,#29033,#29034,#29035,#29036,#29037,#29038,#29039,#29040,
#29041,#29042,#29043,#29044,#29045,#29046,#29047,#29048,#29049,#29050,#29051,
#29052,#29053,#29054,#29055,#29056,#29057,#29058,#29059,#29060,#29061,#29062,
#29063,#29064,#29065),.UNSPECIFIED.,.F.,.F.,(4,3,3,3,3,3,3,3,3,3,3,3,3,
3,3,3,3,3,3,3,3,3,3,3,3,3,3,3,4),(1.27326788952501E-9,0.000305183030980495,
0.000618697405702965,0.000865973237167141,0.00090758617644321,0.00143258173545336,
0.00178321767141052,0.00181517235288642,0.00233679237666166,0.00270521777421961,
0.00272275852932963,0.0031677449805063,0.00317655161755124,0.00351188757989355,
0.00363034470577285,0.00363091529585842,0.00404743389254553,0.00446889752840383,
0.00453793088221607,0.0045565110028101,0.00512035054042042,0.00544551705865929,
0.00547872254023124,0.00584209036187272,0.00622546925982432,0.00635310323510251,
0.00664528416315582,0.00695298625517646,0.0072606883471971),
 .UNSPECIFIED.);
#696=B_SPLINE_CURVE_WITH_KNOTS('',3,(#29067,#29068,#29069,#29070,#29071,
#29072,#29073,#29074,#29075,#29076,#29077,#29078,#29079,#29080,#29081,#29082,
#29083,#29084,#29085,#29086,#29087,#29088),.UNSPECIFIED.,.F.,.F.,(4,2,2,
2,2,2,2,2,2,2,4),(1.03259182419686E-9,0.000910225950447465,0.00182045190089493,
0.00227556487611866,0.0027306778513424,0.00364090380178987,0.00409601677701361,
0.00455112975223735,0.00546135570268482,0.00637158165313229,0.00728180748389904),
 .UNSPECIFIED.);
#697=B_SPLINE_CURVE_WITH_KNOTS('',3,(#29089,#29090,#29091,#29092,#29093,
#29094,#29095,#29096,#29097,#29098,#29099,#29100,#29101,#29102,#29103,#29104,
#29105,#29106,#29107,#29108,#29109,#29110,#29111,#29112,#29113,#29114,#29115,
#29116,#29117,#29118,#29119,#29120,#29121,#29122,#29123,#29124,#29125,#29126,
#29127,#29128,#29129,#29130,#29131,#29132,#29133,#29134,#29135,#29136,#29137,
#29138,#29139,#29140,#29141,#29142,#29143,#29144,#29145,#29146,#29147,#29148,
#29149,#29150,#29151,#29152,#29153,#29154,#29155,#29156,#29157,#29158,#29159,
#29160,#29161,#29162,#29163,#29164,#29165,#29166,#29167,#29168,#29169,#29170),
 .UNSPECIFIED.,.F.,.F.,(4,3,3,3,3,3,3,3,3,3,3,3,3,3,3,3,3,3,3,3,3,3,3,3,
3,3,3,4),(1.28482065261636E-9,0.000305235153155936,0.000618823755024699,
0.000867705358119319,0.000909427513427649,0.00143855251661484,0.00178678626263731,
0.0018188550268553,0.00234189634486621,0.0027106397708665,0.00272828254028295,
0.00317414461806298,0.00358630275051328,0.0036377100537106,0.00363819037736455,
0.00409242381042442,0.0041020810489361,0.0044487169314161,0.00454713756713825,
0.00456560132425793,0.00518563856945916,0.00545656508056589,0.00548920795128181,
0.00599393750639588,0.00636599259399354,0.00640755987476391,0.00686713671060239,
0.00727541997337555),.UNSPECIFIED.);
#698=B_SPLINE_CURVE_WITH_KNOTS('',3,(#29171,#29172,#29173,#29174,#29175,
#29176,#29177,#29178,#29179,#29180,#29181,#29182,#29183,#29184,#29185,#29186,
#29187,#29188,#29189,#29190,#29191,#29192,#29193,#29194,#29195,#29196,#29197,
#29198,#29199,#29200,#29201,#29202,#29203,#29204,#29205,#29206,#29207,#29208,
#29209,#29210,#29211,#29212,#29213,#29214,#29215,#29216,#29217,#29218,#29219,
#29220,#29221,#29222,#29223,#29224,#29225,#29226,#29227,#29228,#29229,#29230,
#29231,#29232,#29233,#29234,#29235,#29236,#29237,#29238,#29239,#29240,#29241,
#29242,#29243,#29244,#29245,#29246,#29247,#29248,#29249,#29250,#29251,#29252,
#29253,#29254,#29255),.UNSPECIFIED.,.F.,.F.,(4,3,3,3,3,3,3,3,3,3,3,3,3,
3,3,3,3,3,3,3,3,3,3,3,3,3,3,3,4),(1.273268146625E-9,0.000305183030965793,
0.000618697405662781,0.000865973237167115,0.000907586176443213,0.0014325817358511,
0.00178321767141051,0.00181517235288642,0.002336792376541,0.00270521777421962,
0.00272275852932964,0.0031677449805063,0.00317655161755125,0.00351188757997544,
0.00363034470577286,0.00363091529585842,0.00404743389236458,0.00446889752799985,
0.00453793088221608,0.00455651100281012,0.005120350539528,0.0054455170586593,
0.00547872254023126,0.00584209036187464,0.00622546925983902,0.00635310323510253,
0.00664528416314504,0.00695298625517104,0.00726068834719704),
 .UNSPECIFIED.);
#699=B_SPLINE_CURVE_WITH_KNOTS('',3,(#29263,#29264,#29265,#29266,#29267,
#29268,#29269,#29270,#29271,#29272,#29273,#29274,#29275,#29276,#29277,#29278,
#29279,#29280),.UNSPECIFIED.,.F.,.F.,(4,2,2,2,2,2,2,2,4),(0.,0.0707692450882043,
0.141538490176409,0.212305911681142,0.283073333185875,0.353840754690609,
0.424608176195343,0.495377421283547,0.566146666371752),.UNSPECIFIED.);
#700=B_SPLINE_CURVE_WITH_KNOTS('',3,(#29281,#29282,#29283,#29284,#29285,
#29286,#29287,#29288,#29289,#29290,#29291,#29292,#29293,#29294,#29295,#29296,
#29297,#29298),.UNSPECIFIED.,.F.,.F.,(4,2,2,2,2,2,2,2,4),(0.566146666371752,
0.636915911459956,0.70768515654816,0.778452578052894,0.849219999557628,
0.919987421062361,0.990754842567095,1.0615240876553,1.1322933327435),
 .UNSPECIFIED.);
#701=B_SPLINE_CURVE_WITH_KNOTS('',3,(#29301,#29302,#29303,#29304,#29305,
#29306,#29307,#29308,#29309,#29310,#29311,#29312,#29313,#29314,#29315,#29316,
#29317,#29318),.UNSPECIFIED.,.F.,.F.,(4,2,2,2,2,2,2,2,4),(0.,0.0707692450882054,
0.141538490176411,0.212305911681144,0.283073333185877,0.35384075469061,
0.424608176195344,0.495377421283548,0.566146666371752),.UNSPECIFIED.);
#702=B_SPLINE_CURVE_WITH_KNOTS('',3,(#29319,#29320,#29321,#29322,#29323,
#29324,#29325,#29326,#29327,#29328,#29329,#29330,#29331,#29332,#29333,#29334,
#29335,#29336),.UNSPECIFIED.,.F.,.F.,(4,2,2,2,2,2,2,2,4),(0.566146666371752,
0.636915911459956,0.70768515654816,0.778452578052894,0.849219999557627,
0.91998742106236,0.990754842567093,1.0615240876553,1.1322933327435),
 .UNSPECIFIED.);
#703=B_SPLINE_CURVE_WITH_KNOTS('',3,(#29339,#29340,#29341,#29342,#29343,
#29344,#29345,#29346,#29347,#29348,#29349,#29350,#29351,#29352,#29353,#29354,
#29355,#29356),.UNSPECIFIED.,.F.,.F.,(4,2,2,2,2,2,2,2,4),(0.,0.0707692450882044,
0.141538490176409,0.212305911681142,0.283073333185876,0.353840754690609,
0.424608176195343,0.495377421283547,0.566146666371752),.UNSPECIFIED.);
#704=B_SPLINE_CURVE_WITH_KNOTS('',3,(#29357,#29358,#29359,#29360,#29361,
#29362,#29363,#29364,#29365,#29366,#29367,#29368,#29369,#29370,#29371,#29372,
#29373,#29374),.UNSPECIFIED.,.F.,.F.,(4,2,2,2,2,2,2,2,4),(0.566146666371752,
0.636915911459956,0.707685156548161,0.778452578052894,0.849219999557628,
0.919987421062361,0.990754842567095,1.0615240876553,1.1322933327435),
 .UNSPECIFIED.);
#705=B_SPLINE_CURVE_WITH_KNOTS('',3,(#29377,#29378,#29379,#29380,#29381,
#29382,#29383,#29384,#29385,#29386,#29387,#29388,#29389,#29390,#29391,#29392,
#29393,#29394),.UNSPECIFIED.,.F.,.F.,(4,2,2,2,2,2,2,2,4),(0.,0.0707692450882054,
0.141538490176411,0.212305911681144,0.283073333185877,0.353840754690611,
0.424608176195344,0.495377421283549,0.566146666371754),.UNSPECIFIED.);
#706=B_SPLINE_CURVE_WITH_KNOTS('',3,(#29395,#29396,#29397,#29398,#29399,
#29400,#29401,#29402,#29403,#29404,#29405,#29406,#29407,#29408,#29409,#29410,
#29411,#29412),.UNSPECIFIED.,.F.,.F.,(4,2,2,2,2,2,2,2,4),(0.566146666371754,
0.63691591145996,0.707685156548165,0.778452578052898,0.849219999557631,
0.919987421062365,0.990754842567098,1.0615240876553,1.13229333274351),
 .UNSPECIFIED.);
#707=B_SPLINE_CURVE_WITH_KNOTS('',3,(#29415,#29416,#29417,#29418,#29419,
#29420,#29421,#29422,#29423,#29424,#29425,#29426,#29427,#29428,#29429,#29430,
#29431,#29432,#29433),.UNSPECIFIED.,.F.,.F.,(4,2,2,2,3,2,2,2,4),(0.849219999557622,
0.919987421062355,0.990754842567088,1.06152408765529,1.1322933327435,1.2030625778317,
1.27383182291991,1.34459924442464,1.41536666592937),.UNSPECIFIED.);
#708=B_SPLINE_CURVE_WITH_KNOTS('',3,(#29434,#29435,#29436,#29437,#29438,
#29439,#29440,#29441,#29442,#29443,#29444,#29445,#29446,#29447,#29448,#29449,
#29450,#29451),.UNSPECIFIED.,.F.,.F.,(4,2,2,2,2,2,2,2,4),(1.41536666592937,
1.4861340874341,1.55690150893884,1.62767075402704,1.69843999911525,1.76920924420345,
1.83997848929165,1.91074591079639,1.98151333230112),.UNSPECIFIED.);
#709=B_SPLINE_CURVE_WITH_KNOTS('',3,(#29484,#29485,#29486,#29487,#29488,
#29489,#29490,#29491,#29492,#29493,#29494,#29495,#29496,#29497,#29498,#29499,
#29500,#29501),.UNSPECIFIED.,.F.,.F.,(4,2,2,2,2,2,2,2,4),(4.77682283355534E-9,
0.00075938273231847,0.00151876546463694,0.00227814819695541,0.00303753092927388,
0.00379691366159235,0.00455629639391082,0.00531567912622929,0.00607506185854776),
 .UNSPECIFIED.);
#710=B_SPLINE_CURVE_WITH_KNOTS('',3,(#29510,#29511,#29512,#29513,#29514,
#29515,#29516,#29517,#29518,#29519,#29520,#29521,#29522,#29523,#29524,#29525,
#29526,#29527,#29528,#29529,#29530,#29531,#29532,#29533,#29534,#29535,#29536,
#29537,#29538,#29539,#29540,#29541,#29542,#29543,#29544,#29545,#29546,#29547,
#29548,#29549,#29550,#29551,#29552,#29553,#29554,#29555,#29556,#29557,#29558,
#29559,#29560,#29561,#29562,#29563,#29564,#29565,#29566,#29567,#29568,#29569,
#29570,#29571,#29572,#29573,#29574,#29575,#29576,#29577,#29578,#29579,#29580,
#29581,#29582,#29583,#29584,#29585,#29586,#29587,#29588,#29589,#29590,#29591),
 .UNSPECIFIED.,.F.,.F.,(4,3,3,3,3,3,3,3,3,3,3,3,3,3,3,3,3,3,3,3,3,3,3,3,
3,3,3,4),(0.,0.0004211704095861,0.000817473654555697,0.00118439929991323,
0.00140274866617539,0.00152429215349839,0.00189673183671225,0.00222892904096502,
0.00228643823024759,0.00259994712936789,0.00290784220121708,0.00304730469033869,
0.00304858430699679,0.00332638406781091,0.00345576304453128,0.00374859930974991,
0.00381073038374598,0.00386547246148279,0.00412567953064968,0.00419180342212058,
0.00453614859577863,0.00457287646049518,0.00469199913147008,0.0050854186274231,
0.00533502253724438,0.00552937120160224,0.00586539666303883,0.00609716861399357),
 .UNSPECIFIED.);
#711=B_SPLINE_CURVE_WITH_KNOTS('',3,(#29600,#29601,#29602,#29603,#29604,
#29605,#29606,#29607,#29608,#29609,#29610,#29611,#29612,#29613,#29614,#29615,
#29616,#29617),.UNSPECIFIED.,.F.,.F.,(4,2,2,2,2,2,2,2,4),(4.77682273112898E-9,
0.00075938273231847,0.00151876546463694,0.00227814819695541,0.00303753092927388,
0.00379691366159235,0.00455629639391082,0.00531567912622929,0.00607506185854776),
 .UNSPECIFIED.);
#712=B_SPLINE_CURVE_WITH_KNOTS('',3,(#29626,#29627,#29628,#29629,#29630,
#29631,#29632,#29633,#29634,#29635,#29636,#29637,#29638,#29639,#29640,#29641,
#29642,#29643,#29644,#29645,#29646,#29647,#29648,#29649,#29650,#29651,#29652,
#29653,#29654,#29655,#29656,#29657,#29658,#29659,#29660,#29661,#29662,#29663,
#29664,#29665,#29666,#29667,#29668,#29669,#29670,#29671,#29672,#29673,#29674,
#29675,#29676,#29677,#29678,#29679,#29680,#29681,#29682,#29683,#29684,#29685,
#29686,#29687,#29688,#29689,#29690,#29691,#29692,#29693,#29694,#29695,#29696,
#29697,#29698,#29699,#29700,#29701,#29702,#29703,#29704,#29705,#29706,#29707,
#29708,#29709,#29710),.UNSPECIFIED.,.F.,.F.,(4,3,3,3,3,3,3,3,3,3,3,3,3,
3,3,3,3,3,3,3,3,3,3,3,3,3,3,3,4),(0.,0.000450053972194884,0.00056431495950664,
0.000759601302696842,0.00117337414957987,0.001397743801198,0.00151920260539368,
0.00184099933344668,0.00214827687898448,0.00222197528808396,0.00227880390809053,
0.00263007039899105,0.00303752617006762,0.00303840521078737,0.00331462895684914,
0.00344451241700138,0.00373559439233855,0.00379800651348421,0.00385273052115206,
0.00411271653974196,0.00417780716483263,0.00451675956026997,0.00455760781618105,
0.004676243259529,0.00506171900842959,0.0053172091188779,0.00551058612136977,
0.00584478941941549,0.00607681042157474),.UNSPECIFIED.);
#713=B_SPLINE_CURVE_WITH_KNOTS('',3,(#29719,#29720,#29721,#29722,#29723,
#29724,#29725,#29726,#29727,#29728,#29729,#29730,#29731,#29732,#29733,#29734,
#29735,#29736,#29737,#29738,#29739,#29740,#29741,#29742,#29743,#29744,#29745,
#29746,#29747,#29748,#29749,#29750,#29751,#29752,#29753,#29754,#29755,#29756,
#29757,#29758,#29759,#29760,#29761,#29762,#29763,#29764,#29765,#29766,#29767,
#29768,#29769,#29770,#29771,#29772,#29773,#29774,#29775,#29776,#29777,#29778,
#29779,#29780,#29781,#29782,#29783,#29784,#29785,#29786,#29787,#29788,#29789,
#29790,#29791,#29792,#29793,#29794,#29795,#29796,#29797,#29798,#29799,#29800),
 .UNSPECIFIED.,.F.,.F.,(4,3,3,3,3,3,3,3,3,3,3,3,3,3,3,3,3,3,3,3,3,3,3,3,
3,3,3,4),(0.,0.000421170409560706,0.000817473654507556,0.00118439929984293,
0.00140274866617529,0.00152429215349839,0.00189673183664917,0.00222892904096503,
0.00228643823024759,0.00259994712938916,0.00290784220125873,0.00304730469033868,
0.00304858430699679,0.0033263840678449,0.00345576304453138,0.00374859930978851,
0.00381073038374598,0.00386547246148282,0.00412567953064846,0.00419180342212058,
0.00453614859565633,0.00457287646049518,0.00469199913147023,0.00508541862720809,
0.00533502253724438,0.00552937120160261,0.00586539666311319,0.00609716861399357),
 .UNSPECIFIED.);
#714=B_SPLINE_CURVE_WITH_KNOTS('',3,(#29804,#29805,#29806,#29807,#29808,
#29809,#29810,#29811,#29812,#29813,#29814,#29815,#29816,#29817,#29818,#29819,
#29820,#29821),.UNSPECIFIED.,.F.,.F.,(4,2,2,2,2,2,2,2,4),(4.77682281082537E-9,
0.000759382732318467,0.00151876546463693,0.0022781481969554,0.00303753092927387,
0.00379691366159234,0.0045562963939108,0.00531567912622927,0.00607506185854774),
 .UNSPECIFIED.);
#715=B_SPLINE_CURVE_WITH_KNOTS('',3,(#29835,#29836,#29837,#29838,#29839,
#29840,#29841,#29842,#29843,#29844,#29845,#29846,#29847,#29848,#29849,#29850,
#29851,#29852,#29853,#29854,#29855,#29856,#29857,#29858,#29859,#29860,#29861,
#29862,#29863,#29864,#29865,#29866,#29867,#29868,#29869,#29870,#29871,#29872,
#29873,#29874,#29875,#29876,#29877,#29878,#29879,#29880,#29881,#29882,#29883,
#29884,#29885,#29886,#29887,#29888,#29889,#29890,#29891,#29892,#29893,#29894,
#29895,#29896,#29897,#29898,#29899,#29900,#29901,#29902,#29903,#29904,#29905,
#29906,#29907,#29908,#29909,#29910,#29911,#29912,#29913,#29914,#29915,#29916),
 .UNSPECIFIED.,.F.,.F.,(4,3,3,3,3,3,3,3,3,3,3,3,3,3,3,3,3,3,3,3,3,3,3,3,
3,3,3,4),(0.,0.00042117040958297,0.000817473654550321,0.00118439929990684,
0.00140274866617551,0.00152429215349839,0.00189673183686581,0.00222892904096507,
0.00228643823024759,0.00259994712942609,0.00290784220133854,0.00304730469033868,
0.00304858430699679,0.00332638406787497,0.00345576304453135,0.00374859930981913,
0.00381073038374599,0.00386547246148282,0.00412567953059812,0.00419180342212059,
0.00453614859568482,0.00457287646049519,0.00469199913147008,0.00508541862749306,
0.00533502253724438,0.00552937120160218,0.00586539666303646,0.00609716861399358),
 .UNSPECIFIED.);
#716=B_SPLINE_CURVE_WITH_KNOTS('',3,(#29925,#29926,#29927,#29928,#29929,
#29930,#29931,#29932,#29933,#29934,#29935,#29936,#29937,#29938,#29939,#29940,
#29941,#29942),.UNSPECIFIED.,.F.,.F.,(4,2,2,2,2,2,2,2,4),(4.77682282016954E-9,
0.00075938273231847,0.00151876546463694,0.00227814819695541,0.00303753092927388,
0.00379691366159235,0.00455629639391082,0.00531567912622929,0.00607506185854776),
 .UNSPECIFIED.);
#717=B_SPLINE_CURVE_WITH_KNOTS('',3,(#29951,#29952,#29953,#29954,#29955,
#29956,#29957,#29958,#29959,#29960,#29961,#29962,#29963,#29964,#29965,#29966,
#29967,#29968,#29969,#29970,#29971,#29972,#29973,#29974,#29975,#29976,#29977,
#29978,#29979,#29980,#29981,#29982,#29983,#29984,#29985,#29986,#29987,#29988,
#29989,#29990,#29991,#29992,#29993,#29994,#29995,#29996,#29997,#29998,#29999,
#30000,#30001,#30002,#30003,#30004,#30005,#30006,#30007,#30008,#30009,#30010,
#30011,#30012,#30013,#30014,#30015,#30016,#30017,#30018,#30019,#30020,#30021,
#30022,#30023,#30024,#30025,#30026,#30027,#30028,#30029,#30030,#30031,#30032,
#30033,#30034,#30035),.UNSPECIFIED.,.F.,.F.,(4,3,3,3,3,3,3,3,3,3,3,3,3,
3,3,3,3,3,3,3,3,3,3,3,3,3,3,3,4),(0.,0.000450053972178455,0.000564314959506638,
0.000759601302696842,0.00117337414953125,0.001397743801198,0.00151920260539368,
0.00184099933344431,0.00214827687897479,0.0022219752880839,0.00227880390809053,
0.00263007039899095,0.00303752617006762,0.00303840521078737,0.00331462895687695,
0.00344451241700149,0.00373559439236671,0.00379800651348421,0.00385273052115206,
0.00411271653966241,0.00417780716483263,0.00451675956044004,0.00455760781618105,
0.00467624325952877,0.00506171900826484,0.0053172091188779,0.00551058612137,
0.00584478941937396,0.00607681042157474),.UNSPECIFIED.);
#718=B_SPLINE_CURVE_WITH_KNOTS('',3,(#30044,#30045,#30046,#30047,#30048,
#30049,#30050,#30051,#30052,#30053,#30054,#30055,#30056,#30057,#30058,#30059,
#30060,#30061,#30062,#30063,#30064,#30065,#30066,#30067,#30068,#30069,#30070,
#30071,#30072,#30073,#30074,#30075,#30076,#30077,#30078,#30079,#30080,#30081,
#30082,#30083,#30084,#30085,#30086,#30087,#30088,#30089,#30090,#30091,#30092,
#30093,#30094,#30095,#30096,#30097,#30098,#30099,#30100,#30101,#30102,#30103,
#30104,#30105,#30106,#30107,#30108,#30109,#30110,#30111,#30112,#30113,#30114,
#30115,#30116,#30117,#30118,#30119,#30120,#30121,#30122,#30123,#30124,#30125),
 .UNSPECIFIED.,.F.,.F.,(4,3,3,3,3,3,3,3,3,3,3,3,3,3,3,3,3,3,3,3,3,3,3,3,
3,3,3,4),(0.,0.000421170409563676,0.000817473654515121,0.00118439929985521,
0.0014027486661753,0.0015242921534984,0.00189673183663668,0.00222892904096502,
0.0022864382302476,0.00259994712935677,0.00290784220118465,0.00304730469033869,
0.0030485843069968,0.0033263840678324,0.00345576304453135,0.00374859930976709,
0.003810730383746,0.00386547246148282,0.00412567953061791,0.00419180342212059,
0.00453614859574039,0.00457287646049519,0.00469199913147009,0.00508541862740153,
0.00533502253724439,0.00552937120160227,0.0058653966630742,0.00609716861399359),
 .UNSPECIFIED.);
#719=B_SPLINE_CURVE_WITH_KNOTS('',3,(#30192,#30193,#30194,#30195,#30196,
#30197,#30198,#30199,#30200,#30201,#30202,#30203,#30204,#30205,#30206,#30207),
 .UNSPECIFIED.,.F.,.F.,(4,3,3,3,3,4),(-4.96552337022927E-6,0.00010764588910917,
0.000210094846213861,0.000303745134247416,0.000388498757831818,0.000430337104598325),
 .UNSPECIFIED.);
#720=B_SPLINE_CURVE_WITH_KNOTS('',3,(#30210,#30211,#30212,#30213,#30214,
#30215,#30216,#30217),.UNSPECIFIED.,.F.,.F.,(4,2,2,4),(-0.000433447002133302,
0.,0.0387852866187773,0.0560629149274059),.UNSPECIFIED.);
#721=B_SPLINE_CURVE_WITH_KNOTS('',3,(#30219,#30220,#30221,#30222,#30223,
#30224,#30225,#30226),.UNSPECIFIED.,.F.,.F.,(4,2,2,4),(0.137724521771023,
0.151853084795163,0.183569264620213,0.183923710449112),.UNSPECIFIED.);
#722=B_SPLINE_CURVE_WITH_KNOTS('',3,(#30294,#30295,#30296,#30297,#30298,
#30299,#30300,#30301,#30302,#30303,#30304,#30305,#30306,#30307,#30308,#30309),
 .UNSPECIFIED.,.F.,.F.,(4,3,3,3,3,4),(-4.96552472797221E-6,0.000107645888232349,
0.00021009484556578,0.000303745133732349,0.000388498757401816,0.000430337104597686),
 .UNSPECIFIED.);
#723=B_SPLINE_CURVE_WITH_KNOTS('',3,(#30312,#30313,#30314,#30315,#30316,
#30317,#30318,#30319),.UNSPECIFIED.,.F.,.F.,(4,2,2,4),(-0.000433447001819931,
0.,0.0387852865238832,0.0560629147500476),.UNSPECIFIED.);
#724=B_SPLINE_CURVE_WITH_KNOTS('',3,(#30321,#30322,#30323,#30324,#30325,
#30326,#30327,#30328),.UNSPECIFIED.,.F.,.F.,(4,2,2,4),(0.137724521771001,
0.151853084794259,0.183569264683853,0.183923710514055),.UNSPECIFIED.);
#725=B_SPLINE_CURVE_WITH_KNOTS('',3,(#30384,#30385,#30386,#30387,#30388,
#30389,#30390,#30391,#30392,#30393,#30394,#30395,#30396,#30397,#30398,#30399),
 .UNSPECIFIED.,.F.,.F.,(4,3,3,3,3,4),(-4.9655233990862E-6,0.000107645889303446,
0.000210094846471236,0.000303745134532124,0.000388498758142231,0.000430337104598325),
 .UNSPECIFIED.);
#726=B_SPLINE_CURVE_WITH_KNOTS('',3,(#30400,#30401,#30402,#30403,#30404,
#30405,#30406,#30407,#30408,#30409,#30410,#30411,#30412,#30413,#30414,#30415),
 .UNSPECIFIED.,.F.,.F.,(4,3,3,3,3,4),(0.,8.57266868340804E-5,0.00017997859326195,
0.000281094481442682,0.000399483842647333,0.000429651352273076),
 .UNSPECIFIED.);
#727=B_SPLINE_CURVE_WITH_KNOTS('',3,(#30417,#30418,#30419,#30420,#30421,
#30422,#30423,#30424),.UNSPECIFIED.,.F.,.F.,(4,2,2,4),(-0.000433447002036394,
3.69027725044546E-14,0.0387852865738777,0.0560629148434446),
 .UNSPECIFIED.);
#728=B_SPLINE_CURVE_WITH_KNOTS('',3,(#30426,#30427,#30428,#30429,#30430,
#30431,#30432,#30433),.UNSPECIFIED.,.F.,.F.,(4,2,2,4),(0.137724521770918,
0.151853084794576,0.183569264655288,0.183923710484895),.UNSPECIFIED.);
#729=B_SPLINE_CURVE_WITH_KNOTS('',3,(#30501,#30502,#30503,#30504,#30505,
#30506,#30507,#30508,#30509,#30510,#30511,#30512,#30513,#30514,#30515,#30516),
 .UNSPECIFIED.,.F.,.F.,(4,3,3,3,3,4),(-4.96552472794879E-6,0.000107645887808995,
0.000210094845026632,0.00030374513314452,0.000388498756766525,0.000430337104597696),
 .UNSPECIFIED.);
#730=B_SPLINE_CURVE_WITH_KNOTS('',3,(#30519,#30520,#30521,#30522,#30523,
#30524,#30525,#30526),.UNSPECIFIED.,.F.,.F.,(4,2,2,4),(-0.000433447002159874,
0.,0.0387852866200758,0.0560629149297987),.UNSPECIFIED.);
#731=B_SPLINE_CURVE_WITH_KNOTS('',3,(#30528,#30529,#30530,#30531,#30532,
#30533,#30534,#30535),.UNSPECIFIED.,.F.,.F.,(4,2,2,4),(0.137724521771109,
0.151853084795218,0.183569264621138,0.183923710450037),.UNSPECIFIED.);
#732=B_SPLINE_CURVE_WITH_KNOTS('',3,(#30591,#30592,#30593,#30594,#30595,
#30596,#30597,#30598,#30599,#30600,#30601,#30602,#30603,#30604,#30605,#30606),
 .UNSPECIFIED.,.F.,.F.,(4,3,3,3,3,4),(-4.9655233990868E-6,0.000107645889377711,
0.000210094846565806,0.000303745134635254,0.000388498758253666,0.000430337104598325),
 .UNSPECIFIED.);
#733=B_SPLINE_CURVE_WITH_KNOTS('',3,(#30607,#30608,#30609,#30610,#30611,
#30612,#30613,#30614,#30615,#30616,#30617,#30618,#30619,#30620,#30621,#30622),
 .UNSPECIFIED.,.F.,.F.,(4,3,3,3,3,4),(8.67361737988404E-19,8.57266868355843E-5,
0.000179978593251411,0.000281094481402461,0.00039948384249144,0.000429651352272726),
 .UNSPECIFIED.);
#734=B_SPLINE_CURVE_WITH_KNOTS('',3,(#30624,#30625,#30626,#30627,#30628,
#30629,#30630,#30631),.UNSPECIFIED.,.F.,.F.,(4,2,2,4),(-0.000433447001866445,
0.,0.0387852865654643,0.0560629148277019),.UNSPECIFIED.);
#735=B_SPLINE_CURVE_WITH_KNOTS('',3,(#30633,#30634,#30635,#30636,#30637,
#30638,#30639,#30640),.UNSPECIFIED.,.F.,.F.,(4,2,2,4),(0.13772452177113,
0.151853084794678,0.183569264665514,0.183923710495293),.UNSPECIFIED.);
#736=B_SPLINE_CURVE_WITH_KNOTS('',3,(#30708,#30709,#30710,#30711,#30712,
#30713,#30714,#30715,#30716,#30717,#30718,#30719,#30720,#30721,#30722,#30723),
 .UNSPECIFIED.,.F.,.F.,(4,3,3,3,3,4),(-4.9655233702401E-6,0.000107645889063516,
0.000210094846155721,0.000303745134184041,0.000388498757763316,0.000430337104598318),
 .UNSPECIFIED.);
#737=B_SPLINE_CURVE_WITH_KNOTS('',3,(#30726,#30727,#30728,#30729,#30730,
#30731,#30732,#30733),.UNSPECIFIED.,.F.,.F.,(4,2,2,4),(-0.00043344700214138,
0.,0.0387852866057272,0.0560629149029756),.UNSPECIFIED.);
#738=B_SPLINE_CURVE_WITH_KNOTS('',3,(#30735,#30736,#30737,#30738,#30739,
#30740,#30741,#30742),.UNSPECIFIED.,.F.,.F.,(4,2,2,4),(0.137724521771185,
0.151853084795333,0.183569264617388,0.183923710446234),.UNSPECIFIED.);
#739=B_SPLINE_CURVE_WITH_KNOTS('',3,(#30810,#30811,#30812,#30813,#30814,
#30815,#30816,#30817,#30818,#30819,#30820,#30821,#30822,#30823,#30824,#30825),
 .UNSPECIFIED.,.F.,.F.,(4,3,3,3,3,4),(-4.96552472796978E-6,0.000107645888261097,
0.000210094845602384,0.000303745133772396,0.000388498757445142,0.000430337104597697),
 .UNSPECIFIED.);
#740=B_SPLINE_CURVE_WITH_KNOTS('',3,(#30828,#30829,#30830,#30831,#30832,
#30833,#30834,#30835),.UNSPECIFIED.,.F.,.F.,(4,2,2,4),(-0.00043344700187696,
0.,0.0387852865361233,0.0560629147728757),.UNSPECIFIED.);
#741=B_SPLINE_CURVE_WITH_KNOTS('',3,(#30837,#30838,#30839,#30840,#30841,
#30842,#30843,#30844),.UNSPECIFIED.,.F.,.F.,(4,2,2,4),(0.137724521771103,
0.151853084794522,0.183569264674518,0.183923710504536),.UNSPECIFIED.);
#742=B_SPLINE_CURVE_WITH_KNOTS('',3,(#30900,#30901,#30902,#30903,#30904,
#30905,#30906,#30907,#30908,#30909,#30910,#30911,#30912,#30913,#30914,#30915),
 .UNSPECIFIED.,.F.,.F.,(4,3,3,3,3,4),(-4.96552339908152E-6,0.000107645889444403,
0.000210094846650772,0.000303745134727905,0.000388498758353848,0.000430337104598325),
 .UNSPECIFIED.);
#743=B_SPLINE_CURVE_WITH_KNOTS('',3,(#30916,#30917,#30918,#30919,#30920,
#30921,#30922,#30923,#30924,#30925,#30926,#30927,#30928,#30929,#30930,#30931),
 .UNSPECIFIED.,.F.,.F.,(4,3,3,3,3,4),(4.33680868994202E-19,8.57266868349673E-5,
0.000179978593250927,0.000281094481403179,0.000399483842498987,0.000429651352273256),
 .UNSPECIFIED.);
#744=B_SPLINE_CURVE_WITH_KNOTS('',3,(#30933,#30934,#30935,#30936,#30937,
#30938,#30939,#30940),.UNSPECIFIED.,.F.,.F.,(4,2,2,4),(-0.00043344700190692,
0.,0.0387852865487993,0.0560629147965774),.UNSPECIFIED.);
#745=B_SPLINE_CURVE_WITH_KNOTS('',3,(#30942,#30943,#30944,#30945,#30946,
#30947,#30948,#30949),.UNSPECIFIED.,.F.,.F.,(4,2,2,4),(0.137724521770992,
0.151853084794507,0.183569264670678,0.183923710500586),.UNSPECIFIED.);
#746=B_SPLINE_CURVE_WITH_KNOTS('',3,(#31017,#31018,#31019,#31020,#31021,
#31022,#31023,#31024,#31025,#31026,#31027,#31028,#31029,#31030,#31031,#31032),
 .UNSPECIFIED.,.F.,.F.,(4,3,3,3,3,4),(-4.96552472798547E-6,0.000107645888160522,
0.000210094845474309,0.000303745133632723,0.000388498757294183,0.000430337104597689),
 .UNSPECIFIED.);
#747=B_SPLINE_CURVE_WITH_KNOTS('',3,(#31035,#31036,#31037,#31038,#31039,
#31040,#31041,#31042),.UNSPECIFIED.,.F.,.F.,(4,2,2,4),(-0.000433447001961007,
0.,0.0387852865485228,0.0560629147960515),.UNSPECIFIED.);
#748=B_SPLINE_CURVE_WITH_KNOTS('',3,(#31044,#31045,#31046,#31047,#31048,
#31049,#31050,#31051),.UNSPECIFIED.,.F.,.F.,(4,2,2,4),(0.137724521771081,
0.151853084794498,0.183569264679235,0.183923710509208),.UNSPECIFIED.);
#749=B_SPLINE_CURVE_WITH_KNOTS('',3,(#31107,#31108,#31109,#31110,#31111,
#31112,#31113,#31114,#31115,#31116,#31117,#31118,#31119,#31120,#31121,#31122),
 .UNSPECIFIED.,.F.,.F.,(4,3,3,3,3,4),(-4.96552339908991E-6,0.000107645889258478,
0.000210094846413965,0.000303745134469702,0.00038849875807473,0.000430337104598321),
 .UNSPECIFIED.);
#750=B_SPLINE_CURVE_WITH_KNOTS('',3,(#31123,#31124,#31125,#31126,#31127,
#31128,#31129,#31130,#31131,#31132,#31133,#31134,#31135,#31136,#31137,#31138),
 .UNSPECIFIED.,.F.,.F.,(4,3,3,3,3,4),(4.33680868994202E-19,8.57266868340056E-5,
0.000179978593272076,0.000281094481476539,0.000399483842768878,0.000429651352272027),
 .UNSPECIFIED.);
#751=B_SPLINE_CURVE_WITH_KNOTS('',3,(#31140,#31141,#31142,#31143,#31144,
#31145,#31146,#31147),.UNSPECIFIED.,.F.,.F.,(4,2,2,4),(-0.000433447002021717,
0.,0.0387852865801805,0.0560629148552472),.UNSPECIFIED.);
#752=B_SPLINE_CURVE_WITH_KNOTS('',3,(#31149,#31150,#31151,#31152,#31153,
#31154,#31155,#31156),.UNSPECIFIED.,.F.,.F.,(4,2,2,4),(0.137724521771083,
0.151853084794822,0.183569264651922,0.183923710481445),.UNSPECIFIED.);
#969=PLANE('',#10952);
#970=PLANE('',#10973);
#971=PLANE('',#10981);
#972=PLANE('',#10987);
#973=PLANE('',#10998);
#974=PLANE('',#11002);
#1409=FACE_OUTER_BOUND('',#2018,.T.);
#1410=FACE_OUTER_BOUND('',#2019,.T.);
#1411=FACE_OUTER_BOUND('',#2020,.T.);
#1412=FACE_OUTER_BOUND('',#2021,.T.);
#1413=FACE_OUTER_BOUND('',#2022,.T.);
#1414=FACE_OUTER_BOUND('',#2023,.T.);
#1415=FACE_OUTER_BOUND('',#2024,.T.);
#1416=FACE_OUTER_BOUND('',#2025,.T.);
#1417=FACE_OUTER_BOUND('',#2026,.T.);
#1418=FACE_OUTER_BOUND('',#2027,.T.);
#1419=FACE_OUTER_BOUND('',#2029,.T.);
#1420=FACE_OUTER_BOUND('',#2030,.T.);
#1421=FACE_OUTER_BOUND('',#2031,.T.);
#1422=FACE_OUTER_BOUND('',#2032,.T.);
#1423=FACE_OUTER_BOUND('',#2034,.T.);
#1424=FACE_OUTER_BOUND('',#2035,.T.);
#1425=FACE_OUTER_BOUND('',#2041,.T.);
#1426=FACE_OUTER_BOUND('',#2043,.T.);
#1427=FACE_OUTER_BOUND('',#2044,.T.);
#1428=FACE_OUTER_BOUND('',#2045,.T.);
#1429=FACE_OUTER_BOUND('',#2047,.T.);
#1430=FACE_OUTER_BOUND('',#2053,.T.);
#1431=FACE_OUTER_BOUND('',#2054,.T.);
#1432=FACE_OUTER_BOUND('',#2055,.T.);
#1433=FACE_OUTER_BOUND('',#2056,.T.);
#1434=FACE_OUTER_BOUND('',#2057,.T.);
#1435=FACE_OUTER_BOUND('',#2058,.T.);
#1436=FACE_OUTER_BOUND('',#2059,.T.);
#1437=FACE_OUTER_BOUND('',#2060,.T.);
#1438=FACE_OUTER_BOUND('',#2062,.T.);
#1439=FACE_OUTER_BOUND('',#2063,.T.);
#1440=FACE_OUTER_BOUND('',#2065,.T.);
#1441=FACE_OUTER_BOUND('',#2066,.T.);
#1442=FACE_OUTER_BOUND('',#2067,.T.);
#1443=FACE_OUTER_BOUND('',#2068,.T.);
#1444=FACE_OUTER_BOUND('',#2069,.T.);
#1445=FACE_OUTER_BOUND('',#2070,.T.);
#1446=FACE_OUTER_BOUND('',#2071,.T.);
#1447=FACE_OUTER_BOUND('',#2072,.T.);
#1448=FACE_OUTER_BOUND('',#2073,.T.);
#1449=FACE_OUTER_BOUND('',#2074,.T.);
#1450=FACE_OUTER_BOUND('',#2075,.T.);
#1451=FACE_OUTER_BOUND('',#2076,.T.);
#1452=FACE_OUTER_BOUND('',#2077,.T.);
#1453=FACE_OUTER_BOUND('',#2078,.T.);
#1454=FACE_OUTER_BOUND('',#2079,.T.);
#1455=FACE_OUTER_BOUND('',#2080,.T.);
#1456=FACE_OUTER_BOUND('',#2081,.T.);
#1457=FACE_OUTER_BOUND('',#2082,.T.);
#1458=FACE_OUTER_BOUND('',#2083,.T.);
#1459=FACE_OUTER_BOUND('',#2084,.T.);
#1460=FACE_OUTER_BOUND('',#2085,.T.);
#1461=FACE_OUTER_BOUND('',#2086,.T.);
#1462=FACE_OUTER_BOUND('',#2087,.T.);
#1463=FACE_OUTER_BOUND('',#2088,.T.);
#1464=FACE_OUTER_BOUND('',#2089,.T.);
#1465=FACE_OUTER_BOUND('',#2090,.T.);
#1466=FACE_OUTER_BOUND('',#2091,.T.);
#1467=FACE_OUTER_BOUND('',#2092,.T.);
#1468=FACE_OUTER_BOUND('',#2093,.T.);
#1469=FACE_OUTER_BOUND('',#2094,.T.);
#1470=FACE_OUTER_BOUND('',#2095,.T.);
#1471=FACE_OUTER_BOUND('',#2096,.T.);
#1472=FACE_OUTER_BOUND('',#2097,.T.);
#1473=FACE_OUTER_BOUND('',#2098,.T.);
#1474=FACE_OUTER_BOUND('',#2099,.T.);
#1475=FACE_OUTER_BOUND('',#2100,.T.);
#1476=FACE_OUTER_BOUND('',#2101,.T.);
#1477=FACE_OUTER_BOUND('',#2102,.T.);
#1478=FACE_OUTER_BOUND('',#2103,.T.);
#1479=FACE_OUTER_BOUND('',#2104,.T.);
#1480=FACE_OUTER_BOUND('',#2105,.T.);
#1481=FACE_OUTER_BOUND('',#2106,.T.);
#1482=FACE_OUTER_BOUND('',#2107,.T.);
#1483=FACE_OUTER_BOUND('',#2108,.T.);
#1484=FACE_OUTER_BOUND('',#2109,.T.);
#1485=FACE_OUTER_BOUND('',#2110,.T.);
#1486=FACE_OUTER_BOUND('',#2111,.T.);
#1487=FACE_OUTER_BOUND('',#2112,.T.);
#1488=FACE_OUTER_BOUND('',#2113,.T.);
#1489=FACE_OUTER_BOUND('',#2114,.T.);
#2018=EDGE_LOOP('',(#8342,#8343,#8344,#8345,#8346,#8347,#8348,#8349));
#2019=EDGE_LOOP('',(#8350,#8351,#8352,#8353,#8354,#8355,#8356,#8357));
#2020=EDGE_LOOP('',(#8358,#8359,#8360,#8361,#8362,#8363,#8364,#8365));
#2021=EDGE_LOOP('',(#8366,#8367,#8368,#8369,#8370,#8371,#8372,#8373,#8374));
#2022=EDGE_LOOP('',(#8375,#8376,#8377,#8378,#8379,#8380,#8381,#8382));
#2023=EDGE_LOOP('',(#8383,#8384,#8385,#8386,#8387,#8388,#8389,#8390));
#2024=EDGE_LOOP('',(#8391,#8392,#8393,#8394,#8395,#8396,#8397,#8398));
#2025=EDGE_LOOP('',(#8399,#8400,#8401,#8402,#8403,#8404,#8405,#8406));
#2026=EDGE_LOOP('',(#8407,#8408,#8409,#8410,#8411,#8412,#8413,#8414));
#2027=EDGE_LOOP('',(#8415,#8416,#8417,#8418,#8419,#8420,#8421,#8422,#8423,
#8424,#8425,#8426,#8427,#8428,#8429,#8430,#8431,#8432,#8433,#8434));
#2028=EDGE_LOOP('',(#8435));
#2029=EDGE_LOOP('',(#8436,#8437,#8438,#8439));
#2030=EDGE_LOOP('',(#8440,#8441,#8442,#8443));
#2031=EDGE_LOOP('',(#8444,#8445,#8446,#8447,#8448,#8449,#8450,#8451));
#2032=EDGE_LOOP('',(#8452));
#2033=EDGE_LOOP('',(#8453));
#2034=EDGE_LOOP('',(#8454,#8455,#8456,#8457,#8458));
#2035=EDGE_LOOP('',(#8459,#8460,#8461,#8462,#8463));
#2036=EDGE_LOOP('',(#8464,#8465));
#2037=EDGE_LOOP('',(#8466,#8467));
#2038=EDGE_LOOP('',(#8468,#8469));
#2039=EDGE_LOOP('',(#8470,#8471));
#2040=EDGE_LOOP('',(#8472,#8473));
#2041=EDGE_LOOP('',(#8474));
#2042=EDGE_LOOP('',(#8475));
#2043=EDGE_LOOP('',(#8476,#8477,#8478,#8479,#8480));
#2044=EDGE_LOOP('',(#8481,#8482,#8483,#8484,#8485,#8486,#8487,#8488,#8489,
#8490,#8491,#8492,#8493,#8494,#8495,#8496,#8497,#8498,#8499,#8500,#8501,
#8502,#8503,#8504,#8505));
#2045=EDGE_LOOP('',(#8506));
#2046=EDGE_LOOP('',(#8507));
#2047=EDGE_LOOP('',(#8508,#8509,#8510,#8511));
#2048=EDGE_LOOP('',(#8512,#8513));
#2049=EDGE_LOOP('',(#8514,#8515));
#2050=EDGE_LOOP('',(#8516,#8517));
#2051=EDGE_LOOP('',(#8518,#8519));
#2052=EDGE_LOOP('',(#8520,#8521));
#2053=EDGE_LOOP('',(#8522,#8523,#8524,#8525,#8526,#8527));
#2054=EDGE_LOOP('',(#8528,#8529,#8530,#8531,#8532,#8533));
#2055=EDGE_LOOP('',(#8534,#8535,#8536,#8537,#8538,#8539));
#2056=EDGE_LOOP('',(#8540,#8541,#8542,#8543,#8544,#8545));
#2057=EDGE_LOOP('',(#8546,#8547,#8548,#8549,#8550,#8551));
#2058=EDGE_LOOP('',(#8552,#8553,#8554,#8555));
#2059=EDGE_LOOP('',(#8556,#8557,#8558,#8559));
#2060=EDGE_LOOP('',(#8560));
#2061=EDGE_LOOP('',(#8561));
#2062=EDGE_LOOP('',(#8562,#8563,#8564,#8565));
#2063=EDGE_LOOP('',(#8566));
#2064=EDGE_LOOP('',(#8567));
#2065=EDGE_LOOP('',(#8568,#8569,#8570,#8571));
#2066=EDGE_LOOP('',(#8572,#8573,#8574,#8575));
#2067=EDGE_LOOP('',(#8576,#8577,#8578,#8579));
#2068=EDGE_LOOP('',(#8580,#8581,#8582,#8583));
#2069=EDGE_LOOP('',(#8584,#8585,#8586,#8587));
#2070=EDGE_LOOP('',(#8588,#8589,#8590,#8591));
#2071=EDGE_LOOP('',(#8592,#8593,#8594,#8595));
#2072=EDGE_LOOP('',(#8596,#8597,#8598,#8599));
#2073=EDGE_LOOP('',(#8600,#8601,#8602,#8603));
#2074=EDGE_LOOP('',(#8604,#8605,#8606,#8607));
#2075=EDGE_LOOP('',(#8608,#8609,#8610,#8611,#8612,#8613));
#2076=EDGE_LOOP('',(#8614,#8615,#8616,#8617));
#2077=EDGE_LOOP('',(#8618,#8619,#8620,#8621));
#2078=EDGE_LOOP('',(#8622,#8623,#8624,#8625,#8626,#8627));
#2079=EDGE_LOOP('',(#8628,#8629,#8630,#8631,#8632,#8633));
#2080=EDGE_LOOP('',(#8634,#8635,#8636,#8637));
#2081=EDGE_LOOP('',(#8638,#8639,#8640,#8641));
#2082=EDGE_LOOP('',(#8642,#8643,#8644,#8645,#8646,#8647));
#2083=EDGE_LOOP('',(#8648,#8649,#8650,#8651,#8652,#8653));
#2084=EDGE_LOOP('',(#8654,#8655,#8656,#8657));
#2085=EDGE_LOOP('',(#8658,#8659,#8660,#8661));
#2086=EDGE_LOOP('',(#8662,#8663,#8664,#8665,#8666,#8667));
#2087=EDGE_LOOP('',(#8668,#8669,#8670,#8671,#8672,#8673));
#2088=EDGE_LOOP('',(#8674,#8675,#8676,#8677));
#2089=EDGE_LOOP('',(#8678,#8679,#8680,#8681));
#2090=EDGE_LOOP('',(#8682,#8683,#8684,#8685,#8686,#8687));
#2091=EDGE_LOOP('',(#8688,#8689,#8690,#8691,#8692,#8693));
#2092=EDGE_LOOP('',(#8694,#8695,#8696,#8697));
#2093=EDGE_LOOP('',(#8698,#8699,#8700,#8701));
#2094=EDGE_LOOP('',(#8702,#8703,#8704,#8705,#8706,#8707));
#2095=EDGE_LOOP('',(#8708,#8709,#8710,#8711,#8712,#8713));
#2096=EDGE_LOOP('',(#8714,#8715,#8716,#8717));
#2097=EDGE_LOOP('',(#8718,#8719,#8720,#8721));
#2098=EDGE_LOOP('',(#8722,#8723,#8724,#8725,#8726,#8727));
#2099=EDGE_LOOP('',(#8728,#8729,#8730,#8731,#8732,#8733));
#2100=EDGE_LOOP('',(#8734,#8735,#8736,#8737));
#2101=EDGE_LOOP('',(#8738,#8739,#8740,#8741));
#2102=EDGE_LOOP('',(#8742,#8743,#8744,#8745,#8746,#8747));
#2103=EDGE_LOOP('',(#8748,#8749,#8750,#8751,#8752,#8753));
#2104=EDGE_LOOP('',(#8754,#8755,#8756,#8757));
#2105=EDGE_LOOP('',(#8758,#8759,#8760,#8761));
#2106=EDGE_LOOP('',(#8762,#8763,#8764,#8765,#8766,#8767));
#2107=EDGE_LOOP('',(#8768,#8769,#8770,#8771,#8772,#8773));
#2108=EDGE_LOOP('',(#8774,#8775,#8776,#8777));
#2109=EDGE_LOOP('',(#8778,#8779,#8780,#8781));
#2110=EDGE_LOOP('',(#8782,#8783,#8784,#8785,#8786,#8787));
#2111=EDGE_LOOP('',(#8788,#8789,#8790,#8791,#8792,#8793));
#2112=EDGE_LOOP('',(#8794,#8795,#8796,#8797));
#2113=EDGE_LOOP('',(#8798,#8799,#8800,#8801));
#2114=EDGE_LOOP('',(#8802,#8803,#8804,#8805,#8806,#8807));
#2476=CIRCLE('',#10925,17.5);
#2477=CIRCLE('',#10926,17.5);
#2478=CIRCLE('',#10928,17.5);
#2479=CIRCLE('',#10929,17.5);
#2480=CIRCLE('',#10931,17.5);
#2481=CIRCLE('',#10932,17.5);
#2482=CIRCLE('',#10934,17.5);
#2483=CIRCLE('',#10935,17.5);
#2484=CIRCLE('',#10936,17.5);
#2485=CIRCLE('',#10938,17.5);
#2486=CIRCLE('',#10939,17.5);
#2487=CIRCLE('',#10941,17.5);
#2488=CIRCLE('',#10942,17.5);
#2489=CIRCLE('',#10944,17.5);
#2490=CIRCLE('',#10945,17.5);
#2491=CIRCLE('',#10947,17.5);
#2492=CIRCLE('',#10948,17.5);
#2493=CIRCLE('',#10950,17.5);
#2494=CIRCLE('',#10951,17.5);
#2495=CIRCLE('',#10953,4.98804347826086);
#2496=CIRCLE('',#10954,4.98804347826086);
#2497=CIRCLE('',#10955,4.98804347826086);
#2498=CIRCLE('',#10956,4.98804347826086);
#2499=CIRCLE('',#10957,4.98804347826086);
#2500=CIRCLE('',#10958,4.98804347826086);
#2501=CIRCLE('',#10959,4.98804347826086);
#2502=CIRCLE('',#10960,4.98804347826086);
#2503=CIRCLE('',#10961,17.5);
#2504=CIRCLE('',#10962,4.98804347826086);
#2505=CIRCLE('',#10963,4.98804347826087);
#2506=CIRCLE('',#10964,15.);
#2507=CIRCLE('',#10966,14.);
#2508=CIRCLE('',#10967,14.);
#2509=CIRCLE('',#10969,14.);
#2510=CIRCLE('',#10970,14.);
#2511=CIRCLE('',#10972,17.5);
#2512=CIRCLE('',#10974,12.35);
#2513=CIRCLE('',#10975,11.35);
#2514=CIRCLE('',#10977,13.);
#2515=CIRCLE('',#10978,13.);
#2516=CIRCLE('',#10980,13.);
#2517=CIRCLE('',#10982,16.);
#2518=CIRCLE('',#10984,16.);
#2519=CIRCLE('',#10985,16.);
#2520=CIRCLE('',#10988,11.35);
#2521=CIRCLE('',#10996,15.);
#2522=CIRCLE('',#10999,15.5);
#2523=CIRCLE('',#11001,15.5);
#2524=CIRCLE('',#11004,4.48804347826086);
#2525=CIRCLE('',#11006,4.48804347826086);
#2526=CIRCLE('',#11008,4.48804347826086);
#2527=CIRCLE('',#11010,4.48804347826086);
#2528=CIRCLE('',#11012,4.48804347826086);
#2529=CIRCLE('',#11014,4.48804347826086);
#2530=CIRCLE('',#11016,4.48804347826086);
#2531=CIRCLE('',#11018,4.48804347826086);
#2532=CIRCLE('',#11020,4.48804347826086);
#2533=CIRCLE('',#11022,4.48804347826087);
#3184=LINE('',#28044,#3934);
#3185=LINE('',#28062,#3935);
#3186=LINE('',#28072,#3936);
#3187=LINE('',#28092,#3937);
#3188=LINE('',#28111,#3938);
#3189=LINE('',#28131,#3939);
#3190=LINE('',#28150,#3940);
#3191=LINE('',#28170,#3941);
#3192=LINE('',#28202,#3942);
#3193=LINE('',#28220,#3943);
#3194=LINE('',#28230,#3944);
#3195=LINE('',#28250,#3945);
#3196=LINE('',#28269,#3946);
#3197=LINE('',#28289,#3947);
#3198=LINE('',#28308,#3948);
#3199=LINE('',#28328,#3949);
#3200=LINE('',#28347,#3950);
#3201=LINE('',#28367,#3951);
#3202=LINE('',#28403,#3952);
#3203=LINE('',#28409,#3953);
#3204=LINE('',#28414,#3954);
#3205=LINE('',#28431,#3955);
#3206=LINE('',#28457,#3956);
#3207=LINE('',#28460,#3957);
#3208=LINE('',#28658,#3958);
#3209=LINE('',#29066,#3959);
#3210=LINE('',#29260,#3960);
#3211=LINE('',#29453,#3961);
#3212=LINE('',#29455,#3962);
#3213=LINE('',#29457,#3963);
#3214=LINE('',#29459,#3964);
#3215=LINE('',#29461,#3965);
#3216=LINE('',#29465,#3966);
#3217=LINE('',#29467,#3967);
#3218=LINE('',#29473,#3968);
#3219=LINE('',#29479,#3969);
#3220=LINE('',#29483,#3970);
#3221=LINE('',#29505,#3971);
#3222=LINE('',#29509,#3972);
#3223=LINE('',#29595,#3973);
#3224=LINE('',#29599,#3974);
#3225=LINE('',#29621,#3975);
#3226=LINE('',#29625,#3976);
#3227=LINE('',#29714,#3977);
#3228=LINE('',#29718,#3978);
#3229=LINE('',#29823,#3979);
#3230=LINE('',#29826,#3980);
#3231=LINE('',#29830,#3981);
#3232=LINE('',#29834,#3982);
#3233=LINE('',#29920,#3983);
#3234=LINE('',#29924,#3984);
#3235=LINE('',#29946,#3985);
#3236=LINE('',#29950,#3986);
#3237=LINE('',#30039,#3987);
#3238=LINE('',#30043,#3988);
#3934=VECTOR('',#13135,1000.);
#3935=VECTOR('',#13138,1000.);
#3936=VECTOR('',#13141,1000.);
#3937=VECTOR('',#13144,1000.);
#3938=VECTOR('',#13149,1000.);
#3939=VECTOR('',#13152,1000.);
#3940=VECTOR('',#13157,1000.);
#3941=VECTOR('',#13160,1000.);
#3942=VECTOR('',#13169,1000.);
#3943=VECTOR('',#13172,1000.);
#3944=VECTOR('',#13175,1000.);
#3945=VECTOR('',#13178,1000.);
#3946=VECTOR('',#13183,1000.);
#3947=VECTOR('',#13186,1000.);
#3948=VECTOR('',#13191,1000.);
#3949=VECTOR('',#13194,1000.);
#3950=VECTOR('',#13199,1000.);
#3951=VECTOR('',#13202,1000.);
#3952=VECTOR('',#13235,14.);
#3953=VECTOR('',#13242,14.);
#3954=VECTOR('',#13247,1000.);
#3955=VECTOR('',#13248,1000.);
#3956=VECTOR('',#13263,13.);
#3957=VECTOR('',#13266,13.);
#3958=VECTOR('',#13275,16.);
#3959=VECTOR('',#13282,16.);
#3960=VECTOR('',#13289,11.35);
#3961=VECTOR('',#13292,1.87499999999999);
#3962=VECTOR('',#13295,1.87500000000001);
#3963=VECTOR('',#13298,1.875);
#3964=VECTOR('',#13301,1.875);
#3965=VECTOR('',#13304,1.875);
#3966=VECTOR('',#13309,15.);
#3967=VECTOR('',#13312,13.5);
#3968=VECTOR('',#13319,15.5);
#3969=VECTOR('',#13326,1000.);
#3970=VECTOR('',#13329,1000.);
#3971=VECTOR('',#13332,1000.);
#3972=VECTOR('',#13335,1000.);
#3973=VECTOR('',#13338,1000.);
#3974=VECTOR('',#13341,1000.);
#3975=VECTOR('',#13344,1000.);
#3976=VECTOR('',#13347,1000.);
#3977=VECTOR('',#13350,1000.);
#3978=VECTOR('',#13353,1000.);
#3979=VECTOR('',#13356,1000.);
#3980=VECTOR('',#13359,1000.);
#3981=VECTOR('',#13362,1000.);
#3982=VECTOR('',#13365,1000.);
#3983=VECTOR('',#13368,1000.);
#3984=VECTOR('',#13371,1000.);
#3985=VECTOR('',#13374,1000.);
#3986=VECTOR('',#13377,1000.);
#3987=VECTOR('',#13380,1000.);
#3988=VECTOR('',#13383,1000.);
#4731=VERTEX_POINT('',#28031);
#4732=VERTEX_POINT('',#28032);
#4733=VERTEX_POINT('',#28034);
#4734=VERTEX_POINT('',#28043);
#4735=VERTEX_POINT('',#28045);
#4736=VERTEX_POINT('',#28052);
#4737=VERTEX_POINT('',#28054);
#4738=VERTEX_POINT('',#28061);
#4739=VERTEX_POINT('',#28070);
#4740=VERTEX_POINT('',#28071);
#4741=VERTEX_POINT('',#28073);
#4742=VERTEX_POINT('',#28080);
#4743=VERTEX_POINT('',#28082);
#4744=VERTEX_POINT('',#28091);
#4745=VERTEX_POINT('',#28093);
#4746=VERTEX_POINT('',#28100);
#4747=VERTEX_POINT('',#28109);
#4748=VERTEX_POINT('',#28110);
#4749=VERTEX_POINT('',#28112);
#4750=VERTEX_POINT('',#28119);
#4751=VERTEX_POINT('',#28121);
#4752=VERTEX_POINT('',#28130);
#4753=VERTEX_POINT('',#28132);
#4754=VERTEX_POINT('',#28139);
#4755=VERTEX_POINT('',#28148);
#4756=VERTEX_POINT('',#28149);
#4757=VERTEX_POINT('',#28151);
#4758=VERTEX_POINT('',#28158);
#4759=VERTEX_POINT('',#28160);
#4760=VERTEX_POINT('',#28169);
#4761=VERTEX_POINT('',#28171);
#4762=VERTEX_POINT('',#28178);
#4763=VERTEX_POINT('',#28180);
#4764=VERTEX_POINT('',#28189);
#4765=VERTEX_POINT('',#28190);
#4766=VERTEX_POINT('',#28192);
#4767=VERTEX_POINT('',#28201);
#4768=VERTEX_POINT('',#28203);
#4769=VERTEX_POINT('',#28210);
#4770=VERTEX_POINT('',#28212);
#4771=VERTEX_POINT('',#28219);
#4772=VERTEX_POINT('',#28228);
#4773=VERTEX_POINT('',#28229);
#4774=VERTEX_POINT('',#28231);
#4775=VERTEX_POINT('',#28238);
#4776=VERTEX_POINT('',#28240);
#4777=VERTEX_POINT('',#28249);
#4778=VERTEX_POINT('',#28251);
#4779=VERTEX_POINT('',#28258);
#4780=VERTEX_POINT('',#28267);
#4781=VERTEX_POINT('',#28268);
#4782=VERTEX_POINT('',#28270);
#4783=VERTEX_POINT('',#28277);
#4784=VERTEX_POINT('',#28279);
#4785=VERTEX_POINT('',#28288);
#4786=VERTEX_POINT('',#28290);
#4787=VERTEX_POINT('',#28297);
#4788=VERTEX_POINT('',#28306);
#4789=VERTEX_POINT('',#28307);
#4790=VERTEX_POINT('',#28309);
#4791=VERTEX_POINT('',#28316);
#4792=VERTEX_POINT('',#28318);
#4793=VERTEX_POINT('',#28327);
#4794=VERTEX_POINT('',#28329);
#4795=VERTEX_POINT('',#28336);
#4796=VERTEX_POINT('',#28345);
#4797=VERTEX_POINT('',#28346);
#4798=VERTEX_POINT('',#28348);
#4799=VERTEX_POINT('',#28355);
#4800=VERTEX_POINT('',#28357);
#4801=VERTEX_POINT('',#28366);
#4802=VERTEX_POINT('',#28368);
#4803=VERTEX_POINT('',#28375);
#4804=VERTEX_POINT('',#28391);
#4805=VERTEX_POINT('',#28393);
#4806=VERTEX_POINT('',#28397);
#4807=VERTEX_POINT('',#28400);
#4808=VERTEX_POINT('',#28402);
#4809=VERTEX_POINT('',#28406);
#4810=VERTEX_POINT('',#28408);
#4811=VERTEX_POINT('',#28412);
#4812=VERTEX_POINT('',#28413);
#4813=VERTEX_POINT('',#28421);
#4814=VERTEX_POINT('',#28430);
#4815=VERTEX_POINT('',#28432);
#4816=VERTEX_POINT('',#28439);
#4817=VERTEX_POINT('',#28448);
#4818=VERTEX_POINT('',#28450);
#4819=VERTEX_POINT('',#28453);
#4820=VERTEX_POINT('',#28454);
#4821=VERTEX_POINT('',#28459);
#4822=VERTEX_POINT('',#28462);
#4823=VERTEX_POINT('',#28463);
#4824=VERTEX_POINT('',#28500);
#4825=VERTEX_POINT('',#28501);
#4826=VERTEX_POINT('',#28538);
#4827=VERTEX_POINT('',#28539);
#4828=VERTEX_POINT('',#28576);
#4829=VERTEX_POINT('',#28577);
#4830=VERTEX_POINT('',#28614);
#4831=VERTEX_POINT('',#28615);
#4832=VERTEX_POINT('',#28654);
#4833=VERTEX_POINT('',#28657);
#4834=VERTEX_POINT('',#28659);
#4835=VERTEX_POINT('',#29257);
#4836=VERTEX_POINT('',#29261);
#4837=VERTEX_POINT('',#29262);
#4838=VERTEX_POINT('',#29299);
#4839=VERTEX_POINT('',#29300);
#4840=VERTEX_POINT('',#29337);
#4841=VERTEX_POINT('',#29338);
#4842=VERTEX_POINT('',#29375);
#4843=VERTEX_POINT('',#29376);
#4844=VERTEX_POINT('',#29413);
#4845=VERTEX_POINT('',#29414);
#4846=VERTEX_POINT('',#29463);
#4847=VERTEX_POINT('',#29469);
#4848=VERTEX_POINT('',#29472);
#4849=VERTEX_POINT('',#29477);
#4850=VERTEX_POINT('',#29478);
#4851=VERTEX_POINT('',#29480);
#4852=VERTEX_POINT('',#29482);
#4853=VERTEX_POINT('',#29503);
#4854=VERTEX_POINT('',#29504);
#4855=VERTEX_POINT('',#29506);
#4856=VERTEX_POINT('',#29508);
#4857=VERTEX_POINT('',#29593);
#4858=VERTEX_POINT('',#29594);
#4859=VERTEX_POINT('',#29596);
#4860=VERTEX_POINT('',#29598);
#4861=VERTEX_POINT('',#29619);
#4862=VERTEX_POINT('',#29620);
#4863=VERTEX_POINT('',#29622);
#4864=VERTEX_POINT('',#29624);
#4865=VERTEX_POINT('',#29712);
#4866=VERTEX_POINT('',#29713);
#4867=VERTEX_POINT('',#29715);
#4868=VERTEX_POINT('',#29717);
#4869=VERTEX_POINT('',#29802);
#4870=VERTEX_POINT('',#29803);
#4871=VERTEX_POINT('',#29822);
#4872=VERTEX_POINT('',#29824);
#4873=VERTEX_POINT('',#29828);
#4874=VERTEX_POINT('',#29829);
#4875=VERTEX_POINT('',#29831);
#4876=VERTEX_POINT('',#29833);
#4877=VERTEX_POINT('',#29918);
#4878=VERTEX_POINT('',#29919);
#4879=VERTEX_POINT('',#29921);
#4880=VERTEX_POINT('',#29923);
#4881=VERTEX_POINT('',#29944);
#4882=VERTEX_POINT('',#29945);
#4883=VERTEX_POINT('',#29947);
#4884=VERTEX_POINT('',#29949);
#4885=VERTEX_POINT('',#30037);
#4886=VERTEX_POINT('',#30038);
#4887=VERTEX_POINT('',#30040);
#4888=VERTEX_POINT('',#30042);
#5984=EDGE_CURVE('',#4731,#4732,#2476,.T.);
#5985=EDGE_CURVE('',#4732,#4733,#639,.T.);
#5986=EDGE_CURVE('',#4733,#4734,#3184,.T.);
#5987=EDGE_CURVE('',#4734,#4735,#640,.T.);
#5988=EDGE_CURVE('',#4735,#4736,#2477,.T.);
#5989=EDGE_CURVE('',#4736,#4737,#641,.T.);
#5990=EDGE_CURVE('',#4737,#4738,#3185,.T.);
#5991=EDGE_CURVE('',#4738,#4731,#642,.T.);
#5992=EDGE_CURVE('',#4739,#4740,#3186,.T.);
#5993=EDGE_CURVE('',#4740,#4741,#643,.T.);
#5994=EDGE_CURVE('',#4741,#4742,#2478,.T.);
#5995=EDGE_CURVE('',#4742,#4743,#644,.T.);
#5996=EDGE_CURVE('',#4743,#4744,#3187,.T.);
#5997=EDGE_CURVE('',#4744,#4745,#645,.T.);
#5998=EDGE_CURVE('',#4745,#4746,#2479,.T.);
#5999=EDGE_CURVE('',#4746,#4739,#646,.T.);
#6000=EDGE_CURVE('',#4747,#4748,#3188,.T.);
#6001=EDGE_CURVE('',#4748,#4749,#647,.T.);
#6002=EDGE_CURVE('',#4749,#4750,#2480,.T.);
#6003=EDGE_CURVE('',#4750,#4751,#648,.T.);
#6004=EDGE_CURVE('',#4751,#4752,#3189,.T.);
#6005=EDGE_CURVE('',#4752,#4753,#649,.T.);
#6006=EDGE_CURVE('',#4753,#4754,#2481,.T.);
#6007=EDGE_CURVE('',#4754,#4747,#650,.T.);
#6008=EDGE_CURVE('',#4755,#4756,#3190,.T.);
#6009=EDGE_CURVE('',#4756,#4757,#651,.T.);
#6010=EDGE_CURVE('',#4757,#4758,#2482,.T.);
#6011=EDGE_CURVE('',#4758,#4759,#652,.T.);
#6012=EDGE_CURVE('',#4759,#4760,#3191,.T.);
#6013=EDGE_CURVE('',#4760,#4761,#653,.T.);
#6014=EDGE_CURVE('',#4761,#4762,#2483,.T.);
#6015=EDGE_CURVE('',#4762,#4763,#2484,.T.);
#6016=EDGE_CURVE('',#4763,#4755,#654,.T.);
#6017=EDGE_CURVE('',#4764,#4765,#2485,.T.);
#6018=EDGE_CURVE('',#4765,#4766,#655,.T.);
#6019=EDGE_CURVE('',#4766,#4767,#3192,.T.);
#6020=EDGE_CURVE('',#4767,#4768,#656,.T.);
#6021=EDGE_CURVE('',#4768,#4769,#2486,.T.);
#6022=EDGE_CURVE('',#4769,#4770,#657,.T.);
#6023=EDGE_CURVE('',#4770,#4771,#3193,.T.);
#6024=EDGE_CURVE('',#4771,#4764,#658,.T.);
#6025=EDGE_CURVE('',#4772,#4773,#3194,.T.);
#6026=EDGE_CURVE('',#4773,#4774,#659,.T.);
#6027=EDGE_CURVE('',#4774,#4775,#2487,.T.);
#6028=EDGE_CURVE('',#4775,#4776,#660,.T.);
#6029=EDGE_CURVE('',#4776,#4777,#3195,.T.);
#6030=EDGE_CURVE('',#4777,#4778,#661,.T.);
#6031=EDGE_CURVE('',#4778,#4779,#2488,.T.);
#6032=EDGE_CURVE('',#4779,#4772,#662,.T.);
#6033=EDGE_CURVE('',#4780,#4781,#3196,.T.);
#6034=EDGE_CURVE('',#4781,#4782,#663,.T.);
#6035=EDGE_CURVE('',#4782,#4783,#2489,.T.);
#6036=EDGE_CURVE('',#4783,#4784,#664,.T.);
#6037=EDGE_CURVE('',#4784,#4785,#3197,.T.);
#6038=EDGE_CURVE('',#4785,#4786,#665,.T.);
#6039=EDGE_CURVE('',#4786,#4787,#2490,.T.);
#6040=EDGE_CURVE('',#4787,#4780,#666,.T.);
#6041=EDGE_CURVE('',#4788,#4789,#3198,.T.);
#6042=EDGE_CURVE('',#4789,#4790,#667,.T.);
#6043=EDGE_CURVE('',#4790,#4791,#2491,.T.);
#6044=EDGE_CURVE('',#4791,#4792,#668,.T.);
#6045=EDGE_CURVE('',#4792,#4793,#3199,.T.);
#6046=EDGE_CURVE('',#4793,#4794,#669,.T.);
#6047=EDGE_CURVE('',#4794,#4795,#2492,.T.);
#6048=EDGE_CURVE('',#4795,#4788,#670,.T.);
#6049=EDGE_CURVE('',#4796,#4797,#3200,.T.);
#6050=EDGE_CURVE('',#4797,#4798,#671,.T.);
#6051=EDGE_CURVE('',#4798,#4799,#2493,.T.);
#6052=EDGE_CURVE('',#4799,#4800,#672,.T.);
#6053=EDGE_CURVE('',#4800,#4801,#3201,.T.);
#6054=EDGE_CURVE('',#4801,#4802,#673,.T.);
#6055=EDGE_CURVE('',#4802,#4803,#2494,.T.);
#6056=EDGE_CURVE('',#4803,#4796,#674,.T.);
#6057=EDGE_CURVE('',#4741,#4750,#2495,.T.);
#6058=EDGE_CURVE('',#4749,#4758,#2496,.T.);
#6059=EDGE_CURVE('',#4757,#4765,#2497,.T.);
#6060=EDGE_CURVE('',#4764,#4775,#2498,.T.);
#6061=EDGE_CURVE('',#4774,#4783,#2499,.T.);
#6062=EDGE_CURVE('',#4782,#4791,#2500,.T.);
#6063=EDGE_CURVE('',#4790,#4799,#2501,.T.);
#6064=EDGE_CURVE('',#4798,#4804,#2502,.T.);
#6065=EDGE_CURVE('',#4805,#4804,#2503,.T.);
#6066=EDGE_CURVE('',#4805,#4732,#2504,.T.);
#6067=EDGE_CURVE('',#4731,#4742,#2505,.T.);
#6068=EDGE_CURVE('',#4806,#4806,#2506,.T.);
#6069=EDGE_CURVE('',#4807,#4807,#2507,.T.);
#6070=EDGE_CURVE('',#4807,#4808,#3202,.T.);
#6071=EDGE_CURVE('',#4808,#4808,#2508,.T.);
#6072=EDGE_CURVE('',#4809,#4809,#2509,.T.);
#6073=EDGE_CURVE('',#4809,#4810,#3203,.T.);
#6074=EDGE_CURVE('',#4810,#4810,#2510,.T.);
#6075=EDGE_CURVE('',#4811,#4812,#3204,.T.);
#6076=EDGE_CURVE('',#4812,#4805,#675,.T.);
#6077=EDGE_CURVE('',#4804,#4813,#676,.T.);
#6078=EDGE_CURVE('',#4813,#4814,#3205,.T.);
#6079=EDGE_CURVE('',#4814,#4815,#677,.T.);
#6080=EDGE_CURVE('',#4815,#4816,#2511,.T.);
#6081=EDGE_CURVE('',#4816,#4811,#678,.T.);
#6082=EDGE_CURVE('',#4817,#4817,#2512,.T.);
#6083=EDGE_CURVE('',#4818,#4818,#2513,.T.);
#6084=EDGE_CURVE('',#4819,#4820,#2514,.T.);
#6085=EDGE_CURVE('',#4820,#4819,#2515,.T.);
#6086=EDGE_CURVE('',#4819,#4817,#3206,.T.);
#6087=EDGE_CURVE('',#4820,#4821,#3207,.T.);
#6088=EDGE_CURVE('',#4821,#4821,#2516,.T.);
#6089=EDGE_CURVE('',#4822,#4823,#679,.T.);
#6090=EDGE_CURVE('',#4823,#4822,#680,.T.);
#6091=EDGE_CURVE('',#4824,#4825,#681,.T.);
#6092=EDGE_CURVE('',#4825,#4824,#682,.T.);
#6093=EDGE_CURVE('',#4826,#4827,#683,.T.);
#6094=EDGE_CURVE('',#4827,#4826,#684,.T.);
#6095=EDGE_CURVE('',#4828,#4829,#685,.T.);
#6096=EDGE_CURVE('',#4829,#4828,#686,.T.);
#6097=EDGE_CURVE('',#4830,#4831,#687,.T.);
#6098=EDGE_CURVE('',#4831,#4830,#688,.T.);
#6099=EDGE_CURVE('',#4832,#4832,#2517,.T.);
#6100=EDGE_CURVE('',#4832,#4833,#3208,.T.);
#6101=EDGE_CURVE('',#4833,#4834,#2518,.T.);
#6102=EDGE_CURVE('',#4834,#4833,#2519,.T.);
#6103=EDGE_CURVE('',#4735,#4816,#689,.T.);
#6104=EDGE_CURVE('',#4815,#4803,#690,.T.);
#6105=EDGE_CURVE('',#4802,#4795,#691,.T.);
#6106=EDGE_CURVE('',#4794,#4787,#692,.T.);
#6107=EDGE_CURVE('',#4786,#4779,#693,.T.);
#6108=EDGE_CURVE('',#4778,#4769,#694,.T.);
#6109=EDGE_CURVE('',#4768,#4763,#695,.T.);
#6110=EDGE_CURVE('',#4762,#4834,#3209,.T.);
#6111=EDGE_CURVE('',#4761,#4754,#696,.T.);
#6112=EDGE_CURVE('',#4753,#4746,#697,.T.);
#6113=EDGE_CURVE('',#4745,#4736,#698,.T.);
#6114=EDGE_CURVE('',#4835,#4835,#2520,.T.);
#6115=EDGE_CURVE('',#4835,#4818,#3210,.T.);
#6116=EDGE_CURVE('',#4836,#4837,#699,.T.);
#6117=EDGE_CURVE('',#4837,#4836,#700,.T.);
#6118=EDGE_CURVE('',#4838,#4839,#701,.T.);
#6119=EDGE_CURVE('',#4839,#4838,#702,.T.);
#6120=EDGE_CURVE('',#4840,#4841,#703,.T.);
#6121=EDGE_CURVE('',#4841,#4840,#704,.T.);
#6122=EDGE_CURVE('',#4842,#4843,#705,.T.);
#6123=EDGE_CURVE('',#4843,#4842,#706,.T.);
#6124=EDGE_CURVE('',#4844,#4845,#707,.T.);
#6125=EDGE_CURVE('',#4845,#4844,#708,.T.);
#6126=EDGE_CURVE('',#4831,#4845,#3211,.T.);
#6127=EDGE_CURVE('',#4829,#4843,#3212,.T.);
#6128=EDGE_CURVE('',#4827,#4841,#3213,.T.);
#6129=EDGE_CURVE('',#4825,#4839,#3214,.T.);
#6130=EDGE_CURVE('',#4823,#4837,#3215,.T.);
#6131=EDGE_CURVE('',#4846,#4846,#2521,.T.);
#6132=EDGE_CURVE('',#4846,#4806,#3216,.T.);
#6133=EDGE_CURVE('',#4808,#4846,#3217,.T.);
#6134=EDGE_CURVE('',#4847,#4847,#2522,.T.);
#6135=EDGE_CURVE('',#4847,#4848,#3218,.T.);
#6136=EDGE_CURVE('',#4848,#4848,#2523,.T.);
#6137=EDGE_CURVE('',#4849,#4850,#3219,.T.);
#6138=EDGE_CURVE('',#4850,#4851,#2524,.T.);
#6139=EDGE_CURVE('',#4851,#4852,#3220,.T.);
#6140=EDGE_CURVE('',#4852,#4849,#709,.T.);
#6141=EDGE_CURVE('',#4853,#4854,#3221,.T.);
#6142=EDGE_CURVE('',#4854,#4855,#2525,.T.);
#6143=EDGE_CURVE('',#4855,#4856,#3222,.T.);
#6144=EDGE_CURVE('',#4856,#4853,#710,.T.);
#6145=EDGE_CURVE('',#4857,#4858,#3223,.T.);
#6146=EDGE_CURVE('',#4858,#4859,#2526,.T.);
#6147=EDGE_CURVE('',#4859,#4860,#3224,.T.);
#6148=EDGE_CURVE('',#4860,#4857,#711,.T.);
#6149=EDGE_CURVE('',#4861,#4862,#3225,.T.);
#6150=EDGE_CURVE('',#4862,#4863,#2527,.T.);
#6151=EDGE_CURVE('',#4863,#4864,#3226,.T.);
#6152=EDGE_CURVE('',#4864,#4861,#712,.T.);
#6153=EDGE_CURVE('',#4865,#4866,#3227,.T.);
#6154=EDGE_CURVE('',#4866,#4867,#2528,.T.);
#6155=EDGE_CURVE('',#4867,#4868,#3228,.T.);
#6156=EDGE_CURVE('',#4868,#4865,#713,.T.);
#6157=EDGE_CURVE('',#4869,#4870,#714,.T.);
#6158=EDGE_CURVE('',#4870,#4871,#3229,.T.);
#6159=EDGE_CURVE('',#4871,#4872,#2529,.T.);
#6160=EDGE_CURVE('',#4872,#4869,#3230,.T.);
#6161=EDGE_CURVE('',#4873,#4874,#3231,.T.);
#6162=EDGE_CURVE('',#4874,#4875,#2530,.T.);
#6163=EDGE_CURVE('',#4875,#4876,#3232,.T.);
#6164=EDGE_CURVE('',#4876,#4873,#715,.T.);
#6165=EDGE_CURVE('',#4877,#4878,#3233,.T.);
#6166=EDGE_CURVE('',#4878,#4879,#2531,.T.);
#6167=EDGE_CURVE('',#4879,#4880,#3234,.T.);
#6168=EDGE_CURVE('',#4880,#4877,#716,.T.);
#6169=EDGE_CURVE('',#4881,#4882,#3235,.T.);
#6170=EDGE_CURVE('',#4882,#4883,#2532,.T.);
#6171=EDGE_CURVE('',#4883,#4884,#3236,.T.);
#6172=EDGE_CURVE('',#4884,#4881,#717,.T.);
#6173=EDGE_CURVE('',#4885,#4886,#3237,.T.);
#6174=EDGE_CURVE('',#4886,#4887,#2533,.T.);
#6175=EDGE_CURVE('',#4887,#4888,#3238,.T.);
#6176=EDGE_CURVE('',#4888,#4885,#718,.T.);
#6177=EDGE_CURVE('',#4881,#4752,#719,.T.);
#6178=EDGE_CURVE('',#4739,#4884,#410,.T.);
#6179=EDGE_CURVE('',#4882,#4751,#720,.T.);
#6180=EDGE_CURVE('',#4740,#4883,#721,.T.);
#6181=EDGE_CURVE('',#4877,#4760,#722,.T.);
#6182=EDGE_CURVE('',#4747,#4880,#411,.T.);
#6183=EDGE_CURVE('',#4878,#4759,#723,.T.);
#6184=EDGE_CURVE('',#4748,#4879,#724,.T.);
#6185=EDGE_CURVE('',#4873,#4767,#725,.T.);
#6186=EDGE_CURVE('',#4755,#4876,#726,.T.);
#6187=EDGE_CURVE('',#4874,#4766,#727,.T.);
#6188=EDGE_CURVE('',#4756,#4875,#728,.T.);
#6189=EDGE_CURVE('',#4870,#4777,#729,.T.);
#6190=EDGE_CURVE('',#4770,#4869,#412,.T.);
#6191=EDGE_CURVE('',#4871,#4776,#730,.T.);
#6192=EDGE_CURVE('',#4771,#4872,#731,.T.);
#6193=EDGE_CURVE('',#4865,#4785,#732,.T.);
#6194=EDGE_CURVE('',#4772,#4868,#733,.T.);
#6195=EDGE_CURVE('',#4866,#4784,#734,.T.);
#6196=EDGE_CURVE('',#4773,#4867,#735,.T.);
#6197=EDGE_CURVE('',#4861,#4793,#736,.T.);
#6198=EDGE_CURVE('',#4780,#4864,#413,.T.);
#6199=EDGE_CURVE('',#4862,#4792,#737,.T.);
#6200=EDGE_CURVE('',#4781,#4863,#738,.T.);
#6201=EDGE_CURVE('',#4857,#4801,#739,.T.);
#6202=EDGE_CURVE('',#4788,#4860,#414,.T.);
#6203=EDGE_CURVE('',#4858,#4800,#740,.T.);
#6204=EDGE_CURVE('',#4789,#4859,#741,.T.);
#6205=EDGE_CURVE('',#4853,#4814,#742,.T.);
#6206=EDGE_CURVE('',#4796,#4856,#743,.T.);
#6207=EDGE_CURVE('',#4854,#4813,#744,.T.);
#6208=EDGE_CURVE('',#4797,#4855,#745,.T.);
#6209=EDGE_CURVE('',#4849,#4734,#746,.T.);
#6210=EDGE_CURVE('',#4811,#4852,#415,.T.);
#6211=EDGE_CURVE('',#4850,#4733,#747,.T.);
#6212=EDGE_CURVE('',#4812,#4851,#748,.T.);
#6213=EDGE_CURVE('',#4885,#4744,#749,.T.);
#6214=EDGE_CURVE('',#4737,#4888,#750,.T.);
#6215=EDGE_CURVE('',#4886,#4743,#751,.T.);
#6216=EDGE_CURVE('',#4738,#4887,#752,.T.);
#8342=ORIENTED_EDGE('',*,*,#5984,.T.);
#8343=ORIENTED_EDGE('',*,*,#5985,.T.);
#8344=ORIENTED_EDGE('',*,*,#5986,.T.);
#8345=ORIENTED_EDGE('',*,*,#5987,.T.);
#8346=ORIENTED_EDGE('',*,*,#5988,.T.);
#8347=ORIENTED_EDGE('',*,*,#5989,.T.);
#8348=ORIENTED_EDGE('',*,*,#5990,.T.);
#8349=ORIENTED_EDGE('',*,*,#5991,.T.);
#8350=ORIENTED_EDGE('',*,*,#5992,.T.);
#8351=ORIENTED_EDGE('',*,*,#5993,.T.);
#8352=ORIENTED_EDGE('',*,*,#5994,.T.);
#8353=ORIENTED_EDGE('',*,*,#5995,.T.);
#8354=ORIENTED_EDGE('',*,*,#5996,.T.);
#8355=ORIENTED_EDGE('',*,*,#5997,.T.);
#8356=ORIENTED_EDGE('',*,*,#5998,.T.);
#8357=ORIENTED_EDGE('',*,*,#5999,.T.);
#8358=ORIENTED_EDGE('',*,*,#6000,.T.);
#8359=ORIENTED_EDGE('',*,*,#6001,.T.);
#8360=ORIENTED_EDGE('',*,*,#6002,.T.);
#8361=ORIENTED_EDGE('',*,*,#6003,.T.);
#8362=ORIENTED_EDGE('',*,*,#6004,.T.);
#8363=ORIENTED_EDGE('',*,*,#6005,.T.);
#8364=ORIENTED_EDGE('',*,*,#6006,.T.);
#8365=ORIENTED_EDGE('',*,*,#6007,.T.);
#8366=ORIENTED_EDGE('',*,*,#6008,.T.);
#8367=ORIENTED_EDGE('',*,*,#6009,.T.);
#8368=ORIENTED_EDGE('',*,*,#6010,.T.);
#8369=ORIENTED_EDGE('',*,*,#6011,.T.);
#8370=ORIENTED_EDGE('',*,*,#6012,.T.);
#8371=ORIENTED_EDGE('',*,*,#6013,.T.);
#8372=ORIENTED_EDGE('',*,*,#6014,.T.);
#8373=ORIENTED_EDGE('',*,*,#6015,.T.);
#8374=ORIENTED_EDGE('',*,*,#6016,.T.);
#8375=ORIENTED_EDGE('',*,*,#6017,.T.);
#8376=ORIENTED_EDGE('',*,*,#6018,.T.);
#8377=ORIENTED_EDGE('',*,*,#6019,.T.);
#8378=ORIENTED_EDGE('',*,*,#6020,.T.);
#8379=ORIENTED_EDGE('',*,*,#6021,.T.);
#8380=ORIENTED_EDGE('',*,*,#6022,.T.);
#8381=ORIENTED_EDGE('',*,*,#6023,.T.);
#8382=ORIENTED_EDGE('',*,*,#6024,.T.);
#8383=ORIENTED_EDGE('',*,*,#6025,.T.);
#8384=ORIENTED_EDGE('',*,*,#6026,.T.);
#8385=ORIENTED_EDGE('',*,*,#6027,.T.);
#8386=ORIENTED_EDGE('',*,*,#6028,.T.);
#8387=ORIENTED_EDGE('',*,*,#6029,.T.);
#8388=ORIENTED_EDGE('',*,*,#6030,.T.);
#8389=ORIENTED_EDGE('',*,*,#6031,.T.);
#8390=ORIENTED_EDGE('',*,*,#6032,.T.);
#8391=ORIENTED_EDGE('',*,*,#6033,.T.);
#8392=ORIENTED_EDGE('',*,*,#6034,.T.);
#8393=ORIENTED_EDGE('',*,*,#6035,.T.);
#8394=ORIENTED_EDGE('',*,*,#6036,.T.);
#8395=ORIENTED_EDGE('',*,*,#6037,.T.);
#8396=ORIENTED_EDGE('',*,*,#6038,.T.);
#8397=ORIENTED_EDGE('',*,*,#6039,.T.);
#8398=ORIENTED_EDGE('',*,*,#6040,.T.);
#8399=ORIENTED_EDGE('',*,*,#6041,.T.);
#8400=ORIENTED_EDGE('',*,*,#6042,.T.);
#8401=ORIENTED_EDGE('',*,*,#6043,.T.);
#8402=ORIENTED_EDGE('',*,*,#6044,.T.);
#8403=ORIENTED_EDGE('',*,*,#6045,.T.);
#8404=ORIENTED_EDGE('',*,*,#6046,.T.);
#8405=ORIENTED_EDGE('',*,*,#6047,.T.);
#8406=ORIENTED_EDGE('',*,*,#6048,.T.);
#8407=ORIENTED_EDGE('',*,*,#6049,.T.);
#8408=ORIENTED_EDGE('',*,*,#6050,.T.);
#8409=ORIENTED_EDGE('',*,*,#6051,.T.);
#8410=ORIENTED_EDGE('',*,*,#6052,.T.);
#8411=ORIENTED_EDGE('',*,*,#6053,.T.);
#8412=ORIENTED_EDGE('',*,*,#6054,.T.);
#8413=ORIENTED_EDGE('',*,*,#6055,.T.);
#8414=ORIENTED_EDGE('',*,*,#6056,.T.);
#8415=ORIENTED_EDGE('',*,*,#5994,.F.);
#8416=ORIENTED_EDGE('',*,*,#6057,.T.);
#8417=ORIENTED_EDGE('',*,*,#6002,.F.);
#8418=ORIENTED_EDGE('',*,*,#6058,.T.);
#8419=ORIENTED_EDGE('',*,*,#6010,.F.);
#8420=ORIENTED_EDGE('',*,*,#6059,.T.);
#8421=ORIENTED_EDGE('',*,*,#6017,.F.);
#8422=ORIENTED_EDGE('',*,*,#6060,.T.);
#8423=ORIENTED_EDGE('',*,*,#6027,.F.);
#8424=ORIENTED_EDGE('',*,*,#6061,.T.);
#8425=ORIENTED_EDGE('',*,*,#6035,.F.);
#8426=ORIENTED_EDGE('',*,*,#6062,.T.);
#8427=ORIENTED_EDGE('',*,*,#6043,.F.);
#8428=ORIENTED_EDGE('',*,*,#6063,.T.);
#8429=ORIENTED_EDGE('',*,*,#6051,.F.);
#8430=ORIENTED_EDGE('',*,*,#6064,.T.);
#8431=ORIENTED_EDGE('',*,*,#6065,.F.);
#8432=ORIENTED_EDGE('',*,*,#6066,.T.);
#8433=ORIENTED_EDGE('',*,*,#5984,.F.);
#8434=ORIENTED_EDGE('',*,*,#6067,.T.);
#8435=ORIENTED_EDGE('',*,*,#6068,.F.);
#8436=ORIENTED_EDGE('',*,*,#6069,.T.);
#8437=ORIENTED_EDGE('',*,*,#6070,.T.);
#8438=ORIENTED_EDGE('',*,*,#6071,.T.);
#8439=ORIENTED_EDGE('',*,*,#6070,.F.);
#8440=ORIENTED_EDGE('',*,*,#6072,.F.);
#8441=ORIENTED_EDGE('',*,*,#6073,.T.);
#8442=ORIENTED_EDGE('',*,*,#6074,.F.);
#8443=ORIENTED_EDGE('',*,*,#6073,.F.);
#8444=ORIENTED_EDGE('',*,*,#6075,.T.);
#8445=ORIENTED_EDGE('',*,*,#6076,.T.);
#8446=ORIENTED_EDGE('',*,*,#6065,.T.);
#8447=ORIENTED_EDGE('',*,*,#6077,.T.);
#8448=ORIENTED_EDGE('',*,*,#6078,.T.);
#8449=ORIENTED_EDGE('',*,*,#6079,.T.);
#8450=ORIENTED_EDGE('',*,*,#6080,.T.);
#8451=ORIENTED_EDGE('',*,*,#6081,.T.);
#8452=ORIENTED_EDGE('',*,*,#6082,.T.);
#8453=ORIENTED_EDGE('',*,*,#6083,.F.);
#8454=ORIENTED_EDGE('',*,*,#6084,.T.);
#8455=ORIENTED_EDGE('',*,*,#6085,.T.);
#8456=ORIENTED_EDGE('',*,*,#6086,.T.);
#8457=ORIENTED_EDGE('',*,*,#6082,.F.);
#8458=ORIENTED_EDGE('',*,*,#6086,.F.);
#8459=ORIENTED_EDGE('',*,*,#6084,.F.);
#8460=ORIENTED_EDGE('',*,*,#6085,.F.);
#8461=ORIENTED_EDGE('',*,*,#6087,.T.);
#8462=ORIENTED_EDGE('',*,*,#6088,.T.);
#8463=ORIENTED_EDGE('',*,*,#6087,.F.);
#8464=ORIENTED_EDGE('',*,*,#6089,.T.);
#8465=ORIENTED_EDGE('',*,*,#6090,.T.);
#8466=ORIENTED_EDGE('',*,*,#6091,.T.);
#8467=ORIENTED_EDGE('',*,*,#6092,.T.);
#8468=ORIENTED_EDGE('',*,*,#6093,.T.);
#8469=ORIENTED_EDGE('',*,*,#6094,.T.);
#8470=ORIENTED_EDGE('',*,*,#6095,.T.);
#8471=ORIENTED_EDGE('',*,*,#6096,.T.);
#8472=ORIENTED_EDGE('',*,*,#6097,.T.);
#8473=ORIENTED_EDGE('',*,*,#6098,.T.);
#8474=ORIENTED_EDGE('',*,*,#6099,.T.);
#8475=ORIENTED_EDGE('',*,*,#6088,.F.);
#8476=ORIENTED_EDGE('',*,*,#6099,.F.);
#8477=ORIENTED_EDGE('',*,*,#6100,.T.);
#8478=ORIENTED_EDGE('',*,*,#6101,.T.);
#8479=ORIENTED_EDGE('',*,*,#6102,.T.);
#8480=ORIENTED_EDGE('',*,*,#6100,.F.);
#8481=ORIENTED_EDGE('',*,*,#5988,.F.);
#8482=ORIENTED_EDGE('',*,*,#6103,.T.);
#8483=ORIENTED_EDGE('',*,*,#6080,.F.);
#8484=ORIENTED_EDGE('',*,*,#6104,.T.);
#8485=ORIENTED_EDGE('',*,*,#6055,.F.);
#8486=ORIENTED_EDGE('',*,*,#6105,.T.);
#8487=ORIENTED_EDGE('',*,*,#6047,.F.);
#8488=ORIENTED_EDGE('',*,*,#6106,.T.);
#8489=ORIENTED_EDGE('',*,*,#6039,.F.);
#8490=ORIENTED_EDGE('',*,*,#6107,.T.);
#8491=ORIENTED_EDGE('',*,*,#6031,.F.);
#8492=ORIENTED_EDGE('',*,*,#6108,.T.);
#8493=ORIENTED_EDGE('',*,*,#6021,.F.);
#8494=ORIENTED_EDGE('',*,*,#6109,.T.);
#8495=ORIENTED_EDGE('',*,*,#6015,.F.);
#8496=ORIENTED_EDGE('',*,*,#6110,.T.);
#8497=ORIENTED_EDGE('',*,*,#6101,.F.);
#8498=ORIENTED_EDGE('',*,*,#6102,.F.);
#8499=ORIENTED_EDGE('',*,*,#6110,.F.);
#8500=ORIENTED_EDGE('',*,*,#6014,.F.);
#8501=ORIENTED_EDGE('',*,*,#6111,.T.);
#8502=ORIENTED_EDGE('',*,*,#6006,.F.);
#8503=ORIENTED_EDGE('',*,*,#6112,.T.);
#8504=ORIENTED_EDGE('',*,*,#5998,.F.);
#8505=ORIENTED_EDGE('',*,*,#6113,.T.);
#8506=ORIENTED_EDGE('',*,*,#6072,.T.);
#8507=ORIENTED_EDGE('',*,*,#6114,.T.);
#8508=ORIENTED_EDGE('',*,*,#6114,.F.);
#8509=ORIENTED_EDGE('',*,*,#6115,.T.);
#8510=ORIENTED_EDGE('',*,*,#6083,.T.);
#8511=ORIENTED_EDGE('',*,*,#6115,.F.);
#8512=ORIENTED_EDGE('',*,*,#6116,.T.);
#8513=ORIENTED_EDGE('',*,*,#6117,.T.);
#8514=ORIENTED_EDGE('',*,*,#6118,.T.);
#8515=ORIENTED_EDGE('',*,*,#6119,.T.);
#8516=ORIENTED_EDGE('',*,*,#6120,.T.);
#8517=ORIENTED_EDGE('',*,*,#6121,.T.);
#8518=ORIENTED_EDGE('',*,*,#6122,.T.);
#8519=ORIENTED_EDGE('',*,*,#6123,.T.);
#8520=ORIENTED_EDGE('',*,*,#6124,.T.);
#8521=ORIENTED_EDGE('',*,*,#6125,.T.);
#8522=ORIENTED_EDGE('',*,*,#6097,.F.);
#8523=ORIENTED_EDGE('',*,*,#6098,.F.);
#8524=ORIENTED_EDGE('',*,*,#6126,.T.);
#8525=ORIENTED_EDGE('',*,*,#6124,.F.);
#8526=ORIENTED_EDGE('',*,*,#6125,.F.);
#8527=ORIENTED_EDGE('',*,*,#6126,.F.);
#8528=ORIENTED_EDGE('',*,*,#6095,.F.);
#8529=ORIENTED_EDGE('',*,*,#6096,.F.);
#8530=ORIENTED_EDGE('',*,*,#6127,.T.);
#8531=ORIENTED_EDGE('',*,*,#6122,.F.);
#8532=ORIENTED_EDGE('',*,*,#6123,.F.);
#8533=ORIENTED_EDGE('',*,*,#6127,.F.);
#8534=ORIENTED_EDGE('',*,*,#6093,.F.);
#8535=ORIENTED_EDGE('',*,*,#6094,.F.);
#8536=ORIENTED_EDGE('',*,*,#6128,.T.);
#8537=ORIENTED_EDGE('',*,*,#6120,.F.);
#8538=ORIENTED_EDGE('',*,*,#6121,.F.);
#8539=ORIENTED_EDGE('',*,*,#6128,.F.);
#8540=ORIENTED_EDGE('',*,*,#6091,.F.);
#8541=ORIENTED_EDGE('',*,*,#6092,.F.);
#8542=ORIENTED_EDGE('',*,*,#6129,.T.);
#8543=ORIENTED_EDGE('',*,*,#6118,.F.);
#8544=ORIENTED_EDGE('',*,*,#6119,.F.);
#8545=ORIENTED_EDGE('',*,*,#6129,.F.);
#8546=ORIENTED_EDGE('',*,*,#6089,.F.);
#8547=ORIENTED_EDGE('',*,*,#6090,.F.);
#8548=ORIENTED_EDGE('',*,*,#6130,.T.);
#8549=ORIENTED_EDGE('',*,*,#6116,.F.);
#8550=ORIENTED_EDGE('',*,*,#6117,.F.);
#8551=ORIENTED_EDGE('',*,*,#6130,.F.);
#8552=ORIENTED_EDGE('',*,*,#6131,.T.);
#8553=ORIENTED_EDGE('',*,*,#6132,.T.);
#8554=ORIENTED_EDGE('',*,*,#6068,.T.);
#8555=ORIENTED_EDGE('',*,*,#6132,.F.);
#8556=ORIENTED_EDGE('',*,*,#6071,.F.);
#8557=ORIENTED_EDGE('',*,*,#6133,.T.);
#8558=ORIENTED_EDGE('',*,*,#6131,.F.);
#8559=ORIENTED_EDGE('',*,*,#6133,.F.);
#8560=ORIENTED_EDGE('',*,*,#6134,.T.);
#8561=ORIENTED_EDGE('',*,*,#6069,.F.);
#8562=ORIENTED_EDGE('',*,*,#6134,.F.);
#8563=ORIENTED_EDGE('',*,*,#6135,.T.);
#8564=ORIENTED_EDGE('',*,*,#6136,.T.);
#8565=ORIENTED_EDGE('',*,*,#6135,.F.);
#8566=ORIENTED_EDGE('',*,*,#6136,.F.);
#8567=ORIENTED_EDGE('',*,*,#6074,.T.);
#8568=ORIENTED_EDGE('',*,*,#6137,.T.);
#8569=ORIENTED_EDGE('',*,*,#6138,.T.);
#8570=ORIENTED_EDGE('',*,*,#6139,.T.);
#8571=ORIENTED_EDGE('',*,*,#6140,.T.);
#8572=ORIENTED_EDGE('',*,*,#6141,.T.);
#8573=ORIENTED_EDGE('',*,*,#6142,.T.);
#8574=ORIENTED_EDGE('',*,*,#6143,.T.);
#8575=ORIENTED_EDGE('',*,*,#6144,.T.);
#8576=ORIENTED_EDGE('',*,*,#6145,.T.);
#8577=ORIENTED_EDGE('',*,*,#6146,.T.);
#8578=ORIENTED_EDGE('',*,*,#6147,.T.);
#8579=ORIENTED_EDGE('',*,*,#6148,.T.);
#8580=ORIENTED_EDGE('',*,*,#6149,.T.);
#8581=ORIENTED_EDGE('',*,*,#6150,.T.);
#8582=ORIENTED_EDGE('',*,*,#6151,.T.);
#8583=ORIENTED_EDGE('',*,*,#6152,.T.);
#8584=ORIENTED_EDGE('',*,*,#6153,.T.);
#8585=ORIENTED_EDGE('',*,*,#6154,.T.);
#8586=ORIENTED_EDGE('',*,*,#6155,.T.);
#8587=ORIENTED_EDGE('',*,*,#6156,.T.);
#8588=ORIENTED_EDGE('',*,*,#6157,.T.);
#8589=ORIENTED_EDGE('',*,*,#6158,.T.);
#8590=ORIENTED_EDGE('',*,*,#6159,.T.);
#8591=ORIENTED_EDGE('',*,*,#6160,.T.);
#8592=ORIENTED_EDGE('',*,*,#6161,.T.);
#8593=ORIENTED_EDGE('',*,*,#6162,.T.);
#8594=ORIENTED_EDGE('',*,*,#6163,.T.);
#8595=ORIENTED_EDGE('',*,*,#6164,.T.);
#8596=ORIENTED_EDGE('',*,*,#6165,.T.);
#8597=ORIENTED_EDGE('',*,*,#6166,.T.);
#8598=ORIENTED_EDGE('',*,*,#6167,.T.);
#8599=ORIENTED_EDGE('',*,*,#6168,.T.);
#8600=ORIENTED_EDGE('',*,*,#6169,.T.);
#8601=ORIENTED_EDGE('',*,*,#6170,.T.);
#8602=ORIENTED_EDGE('',*,*,#6171,.T.);
#8603=ORIENTED_EDGE('',*,*,#6172,.T.);
#8604=ORIENTED_EDGE('',*,*,#6173,.T.);
#8605=ORIENTED_EDGE('',*,*,#6174,.T.);
#8606=ORIENTED_EDGE('',*,*,#6175,.T.);
#8607=ORIENTED_EDGE('',*,*,#6176,.T.);
#8608=ORIENTED_EDGE('',*,*,#6112,.F.);
#8609=ORIENTED_EDGE('',*,*,#6005,.F.);
#8610=ORIENTED_EDGE('',*,*,#6177,.F.);
#8611=ORIENTED_EDGE('',*,*,#6172,.F.);
#8612=ORIENTED_EDGE('',*,*,#6178,.F.);
#8613=ORIENTED_EDGE('',*,*,#5999,.F.);
#8614=ORIENTED_EDGE('',*,*,#6177,.T.);
#8615=ORIENTED_EDGE('',*,*,#6004,.F.);
#8616=ORIENTED_EDGE('',*,*,#6179,.F.);
#8617=ORIENTED_EDGE('',*,*,#6169,.F.);
#8618=ORIENTED_EDGE('',*,*,#6178,.T.);
#8619=ORIENTED_EDGE('',*,*,#6171,.F.);
#8620=ORIENTED_EDGE('',*,*,#6180,.F.);
#8621=ORIENTED_EDGE('',*,*,#5992,.F.);
#8622=ORIENTED_EDGE('',*,*,#6003,.F.);
#8623=ORIENTED_EDGE('',*,*,#6057,.F.);
#8624=ORIENTED_EDGE('',*,*,#5993,.F.);
#8625=ORIENTED_EDGE('',*,*,#6180,.T.);
#8626=ORIENTED_EDGE('',*,*,#6170,.F.);
#8627=ORIENTED_EDGE('',*,*,#6179,.T.);
#8628=ORIENTED_EDGE('',*,*,#6111,.F.);
#8629=ORIENTED_EDGE('',*,*,#6013,.F.);
#8630=ORIENTED_EDGE('',*,*,#6181,.F.);
#8631=ORIENTED_EDGE('',*,*,#6168,.F.);
#8632=ORIENTED_EDGE('',*,*,#6182,.F.);
#8633=ORIENTED_EDGE('',*,*,#6007,.F.);
#8634=ORIENTED_EDGE('',*,*,#6181,.T.);
#8635=ORIENTED_EDGE('',*,*,#6012,.F.);
#8636=ORIENTED_EDGE('',*,*,#6183,.F.);
#8637=ORIENTED_EDGE('',*,*,#6165,.F.);
#8638=ORIENTED_EDGE('',*,*,#6182,.T.);
#8639=ORIENTED_EDGE('',*,*,#6167,.F.);
#8640=ORIENTED_EDGE('',*,*,#6184,.F.);
#8641=ORIENTED_EDGE('',*,*,#6000,.F.);
#8642=ORIENTED_EDGE('',*,*,#6011,.F.);
#8643=ORIENTED_EDGE('',*,*,#6058,.F.);
#8644=ORIENTED_EDGE('',*,*,#6001,.F.);
#8645=ORIENTED_EDGE('',*,*,#6184,.T.);
#8646=ORIENTED_EDGE('',*,*,#6166,.F.);
#8647=ORIENTED_EDGE('',*,*,#6183,.T.);
#8648=ORIENTED_EDGE('',*,*,#6109,.F.);
#8649=ORIENTED_EDGE('',*,*,#6020,.F.);
#8650=ORIENTED_EDGE('',*,*,#6185,.F.);
#8651=ORIENTED_EDGE('',*,*,#6164,.F.);
#8652=ORIENTED_EDGE('',*,*,#6186,.F.);
#8653=ORIENTED_EDGE('',*,*,#6016,.F.);
#8654=ORIENTED_EDGE('',*,*,#6185,.T.);
#8655=ORIENTED_EDGE('',*,*,#6019,.F.);
#8656=ORIENTED_EDGE('',*,*,#6187,.F.);
#8657=ORIENTED_EDGE('',*,*,#6161,.F.);
#8658=ORIENTED_EDGE('',*,*,#6186,.T.);
#8659=ORIENTED_EDGE('',*,*,#6163,.F.);
#8660=ORIENTED_EDGE('',*,*,#6188,.F.);
#8661=ORIENTED_EDGE('',*,*,#6008,.F.);
#8662=ORIENTED_EDGE('',*,*,#6018,.F.);
#8663=ORIENTED_EDGE('',*,*,#6059,.F.);
#8664=ORIENTED_EDGE('',*,*,#6009,.F.);
#8665=ORIENTED_EDGE('',*,*,#6188,.T.);
#8666=ORIENTED_EDGE('',*,*,#6162,.F.);
#8667=ORIENTED_EDGE('',*,*,#6187,.T.);
#8668=ORIENTED_EDGE('',*,*,#6108,.F.);
#8669=ORIENTED_EDGE('',*,*,#6030,.F.);
#8670=ORIENTED_EDGE('',*,*,#6189,.F.);
#8671=ORIENTED_EDGE('',*,*,#6157,.F.);
#8672=ORIENTED_EDGE('',*,*,#6190,.F.);
#8673=ORIENTED_EDGE('',*,*,#6022,.F.);
#8674=ORIENTED_EDGE('',*,*,#6189,.T.);
#8675=ORIENTED_EDGE('',*,*,#6029,.F.);
#8676=ORIENTED_EDGE('',*,*,#6191,.F.);
#8677=ORIENTED_EDGE('',*,*,#6158,.F.);
#8678=ORIENTED_EDGE('',*,*,#6190,.T.);
#8679=ORIENTED_EDGE('',*,*,#6160,.F.);
#8680=ORIENTED_EDGE('',*,*,#6192,.F.);
#8681=ORIENTED_EDGE('',*,*,#6023,.F.);
#8682=ORIENTED_EDGE('',*,*,#6028,.F.);
#8683=ORIENTED_EDGE('',*,*,#6060,.F.);
#8684=ORIENTED_EDGE('',*,*,#6024,.F.);
#8685=ORIENTED_EDGE('',*,*,#6192,.T.);
#8686=ORIENTED_EDGE('',*,*,#6159,.F.);
#8687=ORIENTED_EDGE('',*,*,#6191,.T.);
#8688=ORIENTED_EDGE('',*,*,#6107,.F.);
#8689=ORIENTED_EDGE('',*,*,#6038,.F.);
#8690=ORIENTED_EDGE('',*,*,#6193,.F.);
#8691=ORIENTED_EDGE('',*,*,#6156,.F.);
#8692=ORIENTED_EDGE('',*,*,#6194,.F.);
#8693=ORIENTED_EDGE('',*,*,#6032,.F.);
#8694=ORIENTED_EDGE('',*,*,#6193,.T.);
#8695=ORIENTED_EDGE('',*,*,#6037,.F.);
#8696=ORIENTED_EDGE('',*,*,#6195,.F.);
#8697=ORIENTED_EDGE('',*,*,#6153,.F.);
#8698=ORIENTED_EDGE('',*,*,#6194,.T.);
#8699=ORIENTED_EDGE('',*,*,#6155,.F.);
#8700=ORIENTED_EDGE('',*,*,#6196,.F.);
#8701=ORIENTED_EDGE('',*,*,#6025,.F.);
#8702=ORIENTED_EDGE('',*,*,#6036,.F.);
#8703=ORIENTED_EDGE('',*,*,#6061,.F.);
#8704=ORIENTED_EDGE('',*,*,#6026,.F.);
#8705=ORIENTED_EDGE('',*,*,#6196,.T.);
#8706=ORIENTED_EDGE('',*,*,#6154,.F.);
#8707=ORIENTED_EDGE('',*,*,#6195,.T.);
#8708=ORIENTED_EDGE('',*,*,#6106,.F.);
#8709=ORIENTED_EDGE('',*,*,#6046,.F.);
#8710=ORIENTED_EDGE('',*,*,#6197,.F.);
#8711=ORIENTED_EDGE('',*,*,#6152,.F.);
#8712=ORIENTED_EDGE('',*,*,#6198,.F.);
#8713=ORIENTED_EDGE('',*,*,#6040,.F.);
#8714=ORIENTED_EDGE('',*,*,#6197,.T.);
#8715=ORIENTED_EDGE('',*,*,#6045,.F.);
#8716=ORIENTED_EDGE('',*,*,#6199,.F.);
#8717=ORIENTED_EDGE('',*,*,#6149,.F.);
#8718=ORIENTED_EDGE('',*,*,#6198,.T.);
#8719=ORIENTED_EDGE('',*,*,#6151,.F.);
#8720=ORIENTED_EDGE('',*,*,#6200,.F.);
#8721=ORIENTED_EDGE('',*,*,#6033,.F.);
#8722=ORIENTED_EDGE('',*,*,#6044,.F.);
#8723=ORIENTED_EDGE('',*,*,#6062,.F.);
#8724=ORIENTED_EDGE('',*,*,#6034,.F.);
#8725=ORIENTED_EDGE('',*,*,#6200,.T.);
#8726=ORIENTED_EDGE('',*,*,#6150,.F.);
#8727=ORIENTED_EDGE('',*,*,#6199,.T.);
#8728=ORIENTED_EDGE('',*,*,#6105,.F.);
#8729=ORIENTED_EDGE('',*,*,#6054,.F.);
#8730=ORIENTED_EDGE('',*,*,#6201,.F.);
#8731=ORIENTED_EDGE('',*,*,#6148,.F.);
#8732=ORIENTED_EDGE('',*,*,#6202,.F.);
#8733=ORIENTED_EDGE('',*,*,#6048,.F.);
#8734=ORIENTED_EDGE('',*,*,#6201,.T.);
#8735=ORIENTED_EDGE('',*,*,#6053,.F.);
#8736=ORIENTED_EDGE('',*,*,#6203,.F.);
#8737=ORIENTED_EDGE('',*,*,#6145,.F.);
#8738=ORIENTED_EDGE('',*,*,#6202,.T.);
#8739=ORIENTED_EDGE('',*,*,#6147,.F.);
#8740=ORIENTED_EDGE('',*,*,#6204,.F.);
#8741=ORIENTED_EDGE('',*,*,#6041,.F.);
#8742=ORIENTED_EDGE('',*,*,#6052,.F.);
#8743=ORIENTED_EDGE('',*,*,#6063,.F.);
#8744=ORIENTED_EDGE('',*,*,#6042,.F.);
#8745=ORIENTED_EDGE('',*,*,#6204,.T.);
#8746=ORIENTED_EDGE('',*,*,#6146,.F.);
#8747=ORIENTED_EDGE('',*,*,#6203,.T.);
#8748=ORIENTED_EDGE('',*,*,#6104,.F.);
#8749=ORIENTED_EDGE('',*,*,#6079,.F.);
#8750=ORIENTED_EDGE('',*,*,#6205,.F.);
#8751=ORIENTED_EDGE('',*,*,#6144,.F.);
#8752=ORIENTED_EDGE('',*,*,#6206,.F.);
#8753=ORIENTED_EDGE('',*,*,#6056,.F.);
#8754=ORIENTED_EDGE('',*,*,#6205,.T.);
#8755=ORIENTED_EDGE('',*,*,#6078,.F.);
#8756=ORIENTED_EDGE('',*,*,#6207,.F.);
#8757=ORIENTED_EDGE('',*,*,#6141,.F.);
#8758=ORIENTED_EDGE('',*,*,#6206,.T.);
#8759=ORIENTED_EDGE('',*,*,#6143,.F.);
#8760=ORIENTED_EDGE('',*,*,#6208,.F.);
#8761=ORIENTED_EDGE('',*,*,#6049,.F.);
#8762=ORIENTED_EDGE('',*,*,#6077,.F.);
#8763=ORIENTED_EDGE('',*,*,#6064,.F.);
#8764=ORIENTED_EDGE('',*,*,#6050,.F.);
#8765=ORIENTED_EDGE('',*,*,#6208,.T.);
#8766=ORIENTED_EDGE('',*,*,#6142,.F.);
#8767=ORIENTED_EDGE('',*,*,#6207,.T.);
#8768=ORIENTED_EDGE('',*,*,#6103,.F.);
#8769=ORIENTED_EDGE('',*,*,#5987,.F.);
#8770=ORIENTED_EDGE('',*,*,#6209,.F.);
#8771=ORIENTED_EDGE('',*,*,#6140,.F.);
#8772=ORIENTED_EDGE('',*,*,#6210,.F.);
#8773=ORIENTED_EDGE('',*,*,#6081,.F.);
#8774=ORIENTED_EDGE('',*,*,#6209,.T.);
#8775=ORIENTED_EDGE('',*,*,#5986,.F.);
#8776=ORIENTED_EDGE('',*,*,#6211,.F.);
#8777=ORIENTED_EDGE('',*,*,#6137,.F.);
#8778=ORIENTED_EDGE('',*,*,#6210,.T.);
#8779=ORIENTED_EDGE('',*,*,#6139,.F.);
#8780=ORIENTED_EDGE('',*,*,#6212,.F.);
#8781=ORIENTED_EDGE('',*,*,#6075,.F.);
#8782=ORIENTED_EDGE('',*,*,#5985,.F.);
#8783=ORIENTED_EDGE('',*,*,#6066,.F.);
#8784=ORIENTED_EDGE('',*,*,#6076,.F.);
#8785=ORIENTED_EDGE('',*,*,#6212,.T.);
#8786=ORIENTED_EDGE('',*,*,#6138,.F.);
#8787=ORIENTED_EDGE('',*,*,#6211,.T.);
#8788=ORIENTED_EDGE('',*,*,#6113,.F.);
#8789=ORIENTED_EDGE('',*,*,#5997,.F.);
#8790=ORIENTED_EDGE('',*,*,#6213,.F.);
#8791=ORIENTED_EDGE('',*,*,#6176,.F.);
#8792=ORIENTED_EDGE('',*,*,#6214,.F.);
#8793=ORIENTED_EDGE('',*,*,#5989,.F.);
#8794=ORIENTED_EDGE('',*,*,#6213,.T.);
#8795=ORIENTED_EDGE('',*,*,#5996,.F.);
#8796=ORIENTED_EDGE('',*,*,#6215,.F.);
#8797=ORIENTED_EDGE('',*,*,#6173,.F.);
#8798=ORIENTED_EDGE('',*,*,#6214,.T.);
#8799=ORIENTED_EDGE('',*,*,#6175,.F.);
#8800=ORIENTED_EDGE('',*,*,#6216,.F.);
#8801=ORIENTED_EDGE('',*,*,#5990,.F.);
#8802=ORIENTED_EDGE('',*,*,#5995,.F.);
#8803=ORIENTED_EDGE('',*,*,#6067,.F.);
#8804=ORIENTED_EDGE('',*,*,#5991,.F.);
#8805=ORIENTED_EDGE('',*,*,#6216,.T.);
#8806=ORIENTED_EDGE('',*,*,#6174,.F.);
#8807=ORIENTED_EDGE('',*,*,#6215,.T.);
#9322=CYLINDRICAL_SURFACE('',#10924,17.5);
#9323=CYLINDRICAL_SURFACE('',#10927,17.5);
#9324=CYLINDRICAL_SURFACE('',#10930,17.5);
#9325=CYLINDRICAL_SURFACE('',#10933,17.5);
#9326=CYLINDRICAL_SURFACE('',#10937,17.5);
#9327=CYLINDRICAL_SURFACE('',#10940,17.5);
#9328=CYLINDRICAL_SURFACE('',#10943,17.5);
#9329=CYLINDRICAL_SURFACE('',#10946,17.5);
#9330=CYLINDRICAL_SURFACE('',#10949,17.5);
#9331=CYLINDRICAL_SURFACE('',#10965,14.);
#9332=CYLINDRICAL_SURFACE('',#10968,14.);
#9333=CYLINDRICAL_SURFACE('',#10971,17.5);
#9334=CYLINDRICAL_SURFACE('',#10979,13.);
#9335=CYLINDRICAL_SURFACE('',#10983,16.);
#9336=CYLINDRICAL_SURFACE('',#10989,11.35);
#9337=CYLINDRICAL_SURFACE('',#10990,1.87499999999999);
#9338=CYLINDRICAL_SURFACE('',#10991,1.87500000000001);
#9339=CYLINDRICAL_SURFACE('',#10992,1.875);
#9340=CYLINDRICAL_SURFACE('',#10993,1.875);
#9341=CYLINDRICAL_SURFACE('',#10994,1.875);
#9342=CYLINDRICAL_SURFACE('',#10995,15.);
#9343=CYLINDRICAL_SURFACE('',#11000,15.5);
#9344=CYLINDRICAL_SURFACE('',#11003,4.48804347826086);
#9345=CYLINDRICAL_SURFACE('',#11005,4.48804347826086);
#9346=CYLINDRICAL_SURFACE('',#11007,4.48804347826086);
#9347=CYLINDRICAL_SURFACE('',#11009,4.48804347826086);
#9348=CYLINDRICAL_SURFACE('',#11011,4.48804347826086);
#9349=CYLINDRICAL_SURFACE('',#11013,4.48804347826086);
#9350=CYLINDRICAL_SURFACE('',#11015,4.48804347826086);
#9351=CYLINDRICAL_SURFACE('',#11017,4.48804347826086);
#9352=CYLINDRICAL_SURFACE('',#11019,4.48804347826086);
#9353=CYLINDRICAL_SURFACE('',#11021,4.48804347826087);
#9354=CYLINDRICAL_SURFACE('',#11024,0.5);
#9355=CYLINDRICAL_SURFACE('',#11025,0.5);
#9356=CYLINDRICAL_SURFACE('',#11028,0.5);
#9357=CYLINDRICAL_SURFACE('',#11029,0.5);
#9358=CYLINDRICAL_SURFACE('',#11031,0.5);
#9359=CYLINDRICAL_SURFACE('',#11032,0.5);
#9360=CYLINDRICAL_SURFACE('',#11035,0.5);
#9361=CYLINDRICAL_SURFACE('',#11036,0.5);
#9362=CYLINDRICAL_SURFACE('',#11038,0.5);
#9363=CYLINDRICAL_SURFACE('',#11039,0.5);
#9364=CYLINDRICAL_SURFACE('',#11042,0.5);
#9365=CYLINDRICAL_SURFACE('',#11043,0.5);
#9366=CYLINDRICAL_SURFACE('',#11046,0.5);
#9367=CYLINDRICAL_SURFACE('',#11047,0.5);
#9368=CYLINDRICAL_SURFACE('',#11049,0.5);
#9369=CYLINDRICAL_SURFACE('',#11050,0.5);
#9370=CYLINDRICAL_SURFACE('',#11053,0.5);
#9371=CYLINDRICAL_SURFACE('',#11054,0.5);
#9372=CYLINDRICAL_SURFACE('',#11056,0.5);
#9373=CYLINDRICAL_SURFACE('',#11057,0.5);
#9775=ADVANCED_FACE('',(#1409),#9322,.T.);
#9776=ADVANCED_FACE('',(#1410),#9323,.T.);
#9777=ADVANCED_FACE('',(#1411),#9324,.T.);
#9778=ADVANCED_FACE('',(#1412),#9325,.T.);
#9779=ADVANCED_FACE('',(#1413),#9326,.T.);
#9780=ADVANCED_FACE('',(#1414),#9327,.T.);
#9781=ADVANCED_FACE('',(#1415),#9328,.T.);
#9782=ADVANCED_FACE('',(#1416),#9329,.T.);
#9783=ADVANCED_FACE('',(#1417),#9330,.T.);
#9784=ADVANCED_FACE('',(#1418,#527),#969,.F.);
#9785=ADVANCED_FACE('',(#1419),#9331,.F.);
#9786=ADVANCED_FACE('',(#1420),#9332,.F.);
#9787=ADVANCED_FACE('',(#1421),#9333,.T.);
#9788=ADVANCED_FACE('',(#1422,#528),#970,.F.);
#9789=ADVANCED_FACE('',(#1423),#360,.T.);
#9790=ADVANCED_FACE('',(#1424,#529,#530,#531,#532,#533),#9334,.T.);
#9791=ADVANCED_FACE('',(#1425,#534),#971,.F.);
#9792=ADVANCED_FACE('',(#1426),#9335,.T.);
#9793=ADVANCED_FACE('',(#1427),#361,.T.);
#9794=ADVANCED_FACE('',(#1428,#535),#972,.F.);
#9795=ADVANCED_FACE('',(#1429,#536,#537,#538,#539,#540),#9336,.F.);
#9796=ADVANCED_FACE('',(#1430),#9337,.F.);
#9797=ADVANCED_FACE('',(#1431),#9338,.F.);
#9798=ADVANCED_FACE('',(#1432),#9339,.F.);
#9799=ADVANCED_FACE('',(#1433),#9340,.F.);
#9800=ADVANCED_FACE('',(#1434),#9341,.F.);
#9801=ADVANCED_FACE('',(#1435),#9342,.F.);
#9802=ADVANCED_FACE('',(#1436),#362,.F.);
#9803=ADVANCED_FACE('',(#1437,#541),#973,.T.);
#9804=ADVANCED_FACE('',(#1438),#9343,.F.);
#9805=ADVANCED_FACE('',(#1439,#542),#974,.T.);
#9806=ADVANCED_FACE('',(#1440),#9344,.F.);
#9807=ADVANCED_FACE('',(#1441),#9345,.F.);
#9808=ADVANCED_FACE('',(#1442),#9346,.F.);
#9809=ADVANCED_FACE('',(#1443),#9347,.F.);
#9810=ADVANCED_FACE('',(#1444),#9348,.F.);
#9811=ADVANCED_FACE('',(#1445),#9349,.F.);
#9812=ADVANCED_FACE('',(#1446),#9350,.F.);
#9813=ADVANCED_FACE('',(#1447),#9351,.F.);
#9814=ADVANCED_FACE('',(#1448),#9352,.F.);
#9815=ADVANCED_FACE('',(#1449),#9353,.F.);
#9816=ADVANCED_FACE('',(#1450),#460,.T.);
#9817=ADVANCED_FACE('',(#1451),#9354,.T.);
#9818=ADVANCED_FACE('',(#1452),#9355,.T.);
#9819=ADVANCED_FACE('',(#1453),#393,.T.);
#9820=ADVANCED_FACE('',(#1454),#461,.T.);
#9821=ADVANCED_FACE('',(#1455),#9356,.T.);
#9822=ADVANCED_FACE('',(#1456),#9357,.T.);
#9823=ADVANCED_FACE('',(#1457),#394,.T.);
#9824=ADVANCED_FACE('',(#1458),#462,.T.);
#9825=ADVANCED_FACE('',(#1459),#9358,.T.);
#9826=ADVANCED_FACE('',(#1460),#9359,.T.);
#9827=ADVANCED_FACE('',(#1461),#395,.T.);
#9828=ADVANCED_FACE('',(#1462),#463,.T.);
#9829=ADVANCED_FACE('',(#1463),#9360,.T.);
#9830=ADVANCED_FACE('',(#1464),#9361,.T.);
#9831=ADVANCED_FACE('',(#1465),#396,.T.);
#9832=ADVANCED_FACE('',(#1466),#464,.T.);
#9833=ADVANCED_FACE('',(#1467),#9362,.T.);
#9834=ADVANCED_FACE('',(#1468),#9363,.T.);
#9835=ADVANCED_FACE('',(#1469),#397,.T.);
#9836=ADVANCED_FACE('',(#1470),#465,.T.);
#9837=ADVANCED_FACE('',(#1471),#9364,.T.);
#9838=ADVANCED_FACE('',(#1472),#9365,.T.);
#9839=ADVANCED_FACE('',(#1473),#398,.T.);
#9840=ADVANCED_FACE('',(#1474),#466,.T.);
#9841=ADVANCED_FACE('',(#1475),#9366,.T.);
#9842=ADVANCED_FACE('',(#1476),#9367,.T.);
#9843=ADVANCED_FACE('',(#1477),#399,.T.);
#9844=ADVANCED_FACE('',(#1478),#467,.T.);
#9845=ADVANCED_FACE('',(#1479),#9368,.T.);
#9846=ADVANCED_FACE('',(#1480),#9369,.T.);
#9847=ADVANCED_FACE('',(#1481),#400,.T.);
#9848=ADVANCED_FACE('',(#1482),#468,.T.);
#9849=ADVANCED_FACE('',(#1483),#9370,.T.);
#9850=ADVANCED_FACE('',(#1484),#9371,.T.);
#9851=ADVANCED_FACE('',(#1485),#401,.T.);
#9852=ADVANCED_FACE('',(#1486),#469,.T.);
#9853=ADVANCED_FACE('',(#1487),#9372,.T.);
#9854=ADVANCED_FACE('',(#1488),#9373,.T.);
#9855=ADVANCED_FACE('',(#1489),#402,.T.);
#9961=CLOSED_SHELL('',(#9775,#9776,#9777,#9778,#9779,#9780,#9781,#9782,
#9783,#9784,#9785,#9786,#9787,#9788,#9789,#9790,#9791,#9792,#9793,#9794,
#9795,#9796,#9797,#9798,#9799,#9800,#9801,#9802,#9803,#9804,#9805,#9806,
#9807,#9808,#9809,#9810,#9811,#9812,#9813,#9814,#9815,#9816,#9817,#9818,
#9819,#9820,#9821,#9822,#9823,#9824,#9825,#9826,#9827,#9828,#9829,#9830,
#9831,#9832,#9833,#9834,#9835,#9836,#9837,#9838,#9839,#9840,#9841,#9842,
#9843,#9844,#9845,#9846,#9847,#9848,#9849,#9850,#9851,#9852,#9853,#9854,
#9855));
#10923=AXIS2_PLACEMENT_3D('',#28029,#13129,#13130);
#10924=AXIS2_PLACEMENT_3D('',#28030,#13131,#13132);
#10925=AXIS2_PLACEMENT_3D('',#28033,#13133,#13134);
#10926=AXIS2_PLACEMENT_3D('',#28053,#13136,#13137);
#10927=AXIS2_PLACEMENT_3D('',#28069,#13139,#13140);
#10928=AXIS2_PLACEMENT_3D('',#28081,#13142,#13143);
#10929=AXIS2_PLACEMENT_3D('',#28101,#13145,#13146);
#10930=AXIS2_PLACEMENT_3D('',#28108,#13147,#13148);
#10931=AXIS2_PLACEMENT_3D('',#28120,#13150,#13151);
#10932=AXIS2_PLACEMENT_3D('',#28140,#13153,#13154);
#10933=AXIS2_PLACEMENT_3D('',#28147,#13155,#13156);
#10934=AXIS2_PLACEMENT_3D('',#28159,#13158,#13159);
#10935=AXIS2_PLACEMENT_3D('',#28179,#13161,#13162);
#10936=AXIS2_PLACEMENT_3D('',#28181,#13163,#13164);
#10937=AXIS2_PLACEMENT_3D('',#28188,#13165,#13166);
#10938=AXIS2_PLACEMENT_3D('',#28191,#13167,#13168);
#10939=AXIS2_PLACEMENT_3D('',#28211,#13170,#13171);
#10940=AXIS2_PLACEMENT_3D('',#28227,#13173,#13174);
#10941=AXIS2_PLACEMENT_3D('',#28239,#13176,#13177);
#10942=AXIS2_PLACEMENT_3D('',#28259,#13179,#13180);
#10943=AXIS2_PLACEMENT_3D('',#28266,#13181,#13182);
#10944=AXIS2_PLACEMENT_3D('',#28278,#13184,#13185);
#10945=AXIS2_PLACEMENT_3D('',#28298,#13187,#13188);
#10946=AXIS2_PLACEMENT_3D('',#28305,#13189,#13190);
#10947=AXIS2_PLACEMENT_3D('',#28317,#13192,#13193);
#10948=AXIS2_PLACEMENT_3D('',#28337,#13195,#13196);
#10949=AXIS2_PLACEMENT_3D('',#28344,#13197,#13198);
#10950=AXIS2_PLACEMENT_3D('',#28356,#13200,#13201);
#10951=AXIS2_PLACEMENT_3D('',#28376,#13203,#13204);
#10952=AXIS2_PLACEMENT_3D('',#28383,#13205,#13206);
#10953=AXIS2_PLACEMENT_3D('',#28384,#13207,#13208);
#10954=AXIS2_PLACEMENT_3D('',#28385,#13209,#13210);
#10955=AXIS2_PLACEMENT_3D('',#28386,#13211,#13212);
#10956=AXIS2_PLACEMENT_3D('',#28387,#13213,#13214);
#10957=AXIS2_PLACEMENT_3D('',#28388,#13215,#13216);
#10958=AXIS2_PLACEMENT_3D('',#28389,#13217,#13218);
#10959=AXIS2_PLACEMENT_3D('',#28390,#13219,#13220);
#10960=AXIS2_PLACEMENT_3D('',#28392,#13221,#13222);
#10961=AXIS2_PLACEMENT_3D('',#28394,#13223,#13224);
#10962=AXIS2_PLACEMENT_3D('',#28395,#13225,#13226);
#10963=AXIS2_PLACEMENT_3D('',#28396,#13227,#13228);
#10964=AXIS2_PLACEMENT_3D('',#28398,#13229,#13230);
#10965=AXIS2_PLACEMENT_3D('',#28399,#13231,#13232);
#10966=AXIS2_PLACEMENT_3D('',#28401,#13233,#13234);
#10967=AXIS2_PLACEMENT_3D('',#28404,#13236,#13237);
#10968=AXIS2_PLACEMENT_3D('',#28405,#13238,#13239);
#10969=AXIS2_PLACEMENT_3D('',#28407,#13240,#13241);
#10970=AXIS2_PLACEMENT_3D('',#28410,#13243,#13244);
#10971=AXIS2_PLACEMENT_3D('',#28411,#13245,#13246);
#10972=AXIS2_PLACEMENT_3D('',#28440,#13249,#13250);
#10973=AXIS2_PLACEMENT_3D('',#28447,#13251,#13252);
#10974=AXIS2_PLACEMENT_3D('',#28449,#13253,#13254);
#10975=AXIS2_PLACEMENT_3D('',#28451,#13255,#13256);
#10976=AXIS2_PLACEMENT_3D('',#28452,#13257,#13258);
#10977=AXIS2_PLACEMENT_3D('',#28455,#13259,#13260);
#10978=AXIS2_PLACEMENT_3D('',#28456,#13261,#13262);
#10979=AXIS2_PLACEMENT_3D('',#28458,#13264,#13265);
#10980=AXIS2_PLACEMENT_3D('',#28461,#13267,#13268);
#10981=AXIS2_PLACEMENT_3D('',#28653,#13269,#13270);
#10982=AXIS2_PLACEMENT_3D('',#28655,#13271,#13272);
#10983=AXIS2_PLACEMENT_3D('',#28656,#13273,#13274);
#10984=AXIS2_PLACEMENT_3D('',#28660,#13276,#13277);
#10985=AXIS2_PLACEMENT_3D('',#28661,#13278,#13279);
#10986=AXIS2_PLACEMENT_3D('',#28662,#13280,#13281);
#10987=AXIS2_PLACEMENT_3D('',#29256,#13283,#13284);
#10988=AXIS2_PLACEMENT_3D('',#29258,#13285,#13286);
#10989=AXIS2_PLACEMENT_3D('',#29259,#13287,#13288);
#10990=AXIS2_PLACEMENT_3D('',#29452,#13290,#13291);
#10991=AXIS2_PLACEMENT_3D('',#29454,#13293,#13294);
#10992=AXIS2_PLACEMENT_3D('',#29456,#13296,#13297);
#10993=AXIS2_PLACEMENT_3D('',#29458,#13299,#13300);
#10994=AXIS2_PLACEMENT_3D('',#29460,#13302,#13303);
#10995=AXIS2_PLACEMENT_3D('',#29462,#13305,#13306);
#10996=AXIS2_PLACEMENT_3D('',#29464,#13307,#13308);
#10997=AXIS2_PLACEMENT_3D('',#29466,#13310,#13311);
#10998=AXIS2_PLACEMENT_3D('',#29468,#13313,#13314);
#10999=AXIS2_PLACEMENT_3D('',#29470,#13315,#13316);
#11000=AXIS2_PLACEMENT_3D('',#29471,#13317,#13318);
#11001=AXIS2_PLACEMENT_3D('',#29474,#13320,#13321);
#11002=AXIS2_PLACEMENT_3D('',#29475,#13322,#13323);
#11003=AXIS2_PLACEMENT_3D('',#29476,#13324,#13325);
#11004=AXIS2_PLACEMENT_3D('',#29481,#13327,#13328);
#11005=AXIS2_PLACEMENT_3D('',#29502,#13330,#13331);
#11006=AXIS2_PLACEMENT_3D('',#29507,#13333,#13334);
#11007=AXIS2_PLACEMENT_3D('',#29592,#13336,#13337);
#11008=AXIS2_PLACEMENT_3D('',#29597,#13339,#13340);
#11009=AXIS2_PLACEMENT_3D('',#29618,#13342,#13343);
#11010=AXIS2_PLACEMENT_3D('',#29623,#13345,#13346);
#11011=AXIS2_PLACEMENT_3D('',#29711,#13348,#13349);
#11012=AXIS2_PLACEMENT_3D('',#29716,#13351,#13352);
#11013=AXIS2_PLACEMENT_3D('',#29801,#13354,#13355);
#11014=AXIS2_PLACEMENT_3D('',#29825,#13357,#13358);
#11015=AXIS2_PLACEMENT_3D('',#29827,#13360,#13361);
#11016=AXIS2_PLACEMENT_3D('',#29832,#13363,#13364);
#11017=AXIS2_PLACEMENT_3D('',#29917,#13366,#13367);
#11018=AXIS2_PLACEMENT_3D('',#29922,#13369,#13370);
#11019=AXIS2_PLACEMENT_3D('',#29943,#13372,#13373);
#11020=AXIS2_PLACEMENT_3D('',#29948,#13375,#13376);
#11021=AXIS2_PLACEMENT_3D('',#30036,#13378,#13379);
#11022=AXIS2_PLACEMENT_3D('',#30041,#13381,#13382);
#11023=AXIS2_PLACEMENT_3D('',#30208,#13384,#13385);
#11024=AXIS2_PLACEMENT_3D('',#30209,#13386,#13387);
#11025=AXIS2_PLACEMENT_3D('',#30218,#13388,#13389);
#11026=AXIS2_PLACEMENT_3D('',#30227,#13390,#13391);
#11027=AXIS2_PLACEMENT_3D('',#30310,#13392,#13393);
#11028=AXIS2_PLACEMENT_3D('',#30311,#13394,#13395);
#11029=AXIS2_PLACEMENT_3D('',#30320,#13396,#13397);
#11030=AXIS2_PLACEMENT_3D('',#30329,#13398,#13399);
#11031=AXIS2_PLACEMENT_3D('',#30416,#13400,#13401);
#11032=AXIS2_PLACEMENT_3D('',#30425,#13402,#13403);
#11033=AXIS2_PLACEMENT_3D('',#30434,#13404,#13405);
#11034=AXIS2_PLACEMENT_3D('',#30517,#13406,#13407);
#11035=AXIS2_PLACEMENT_3D('',#30518,#13408,#13409);
#11036=AXIS2_PLACEMENT_3D('',#30527,#13410,#13411);
#11037=AXIS2_PLACEMENT_3D('',#30536,#13412,#13413);
#11038=AXIS2_PLACEMENT_3D('',#30623,#13414,#13415);
#11039=AXIS2_PLACEMENT_3D('',#30632,#13416,#13417);
#11040=AXIS2_PLACEMENT_3D('',#30641,#13418,#13419);
#11041=AXIS2_PLACEMENT_3D('',#30724,#13420,#13421);
#11042=AXIS2_PLACEMENT_3D('',#30725,#13422,#13423);
#11043=AXIS2_PLACEMENT_3D('',#30734,#13424,#13425);
#11044=AXIS2_PLACEMENT_3D('',#30743,#13426,#13427);
#11045=AXIS2_PLACEMENT_3D('',#30826,#13428,#13429);
#11046=AXIS2_PLACEMENT_3D('',#30827,#13430,#13431);
#11047=AXIS2_PLACEMENT_3D('',#30836,#13432,#13433);
#11048=AXIS2_PLACEMENT_3D('',#30845,#13434,#13435);
#11049=AXIS2_PLACEMENT_3D('',#30932,#13436,#13437);
#11050=AXIS2_PLACEMENT_3D('',#30941,#13438,#13439);
#11051=AXIS2_PLACEMENT_3D('',#30950,#13440,#13441);
#11052=AXIS2_PLACEMENT_3D('',#31033,#13442,#13443);
#11053=AXIS2_PLACEMENT_3D('',#31034,#13444,#13445);
#11054=AXIS2_PLACEMENT_3D('',#31043,#13446,#13447);
#11055=AXIS2_PLACEMENT_3D('',#31052,#13448,#13449);
#11056=AXIS2_PLACEMENT_3D('',#31139,#13450,#13451);
#11057=AXIS2_PLACEMENT_3D('',#31148,#13452,#13453);
#11058=AXIS2_PLACEMENT_3D('',#31157,#13454,#13455);
#13129=DIRECTION('axis',(0.,0.,1.));
#13130=DIRECTION('refdir',(1.,0.,0.));
#13131=DIRECTION('center_axis',(0.,0.,1.));
#13132=DIRECTION('ref_axis',(1.,0.,0.));
#13133=DIRECTION('center_axis',(0.,0.,1.));
#13134=DIRECTION('ref_axis',(1.,0.,0.));
#13135=DIRECTION('',(0.,0.,1.));
#13136=DIRECTION('center_axis',(0.,0.,-1.));
#13137=DIRECTION('ref_axis',(-1.,0.,0.));
#13138=DIRECTION('',(0.,0.,-1.));
#13139=DIRECTION('center_axis',(0.,0.,1.));
#13140=DIRECTION('ref_axis',(1.,0.,0.));
#13141=DIRECTION('',(0.,0.,-1.));
#13142=DIRECTION('center_axis',(0.,0.,1.));
#13143=DIRECTION('ref_axis',(1.,0.,0.));
#13144=DIRECTION('',(0.,0.,1.));
#13145=DIRECTION('center_axis',(0.,0.,-1.));
#13146=DIRECTION('ref_axis',(-1.,0.,0.));
#13147=DIRECTION('center_axis',(0.,0.,1.));
#13148=DIRECTION('ref_axis',(1.,0.,0.));
#13149=DIRECTION('',(0.,0.,-1.));
#13150=DIRECTION('center_axis',(0.,0.,1.));
#13151=DIRECTION('ref_axis',(1.,0.,0.));
#13152=DIRECTION('',(0.,0.,1.));
#13153=DIRECTION('center_axis',(0.,0.,-1.));
#13154=DIRECTION('ref_axis',(-1.,0.,0.));
#13155=DIRECTION('center_axis',(0.,0.,1.));
#13156=DIRECTION('ref_axis',(1.,0.,0.));
#13157=DIRECTION('',(0.,0.,-1.));
#13158=DIRECTION('center_axis',(0.,0.,1.));
#13159=DIRECTION('ref_axis',(1.,0.,0.));
#13160=DIRECTION('',(0.,0.,1.));
#13161=DIRECTION('center_axis',(0.,0.,-1.));
#13162=DIRECTION('ref_axis',(-1.,0.,0.));
#13163=DIRECTION('center_axis',(0.,0.,-1.));
#13164=DIRECTION('ref_axis',(-1.,0.,0.));
#13165=DIRECTION('center_axis',(0.,0.,1.));
#13166=DIRECTION('ref_axis',(1.,0.,0.));
#13167=DIRECTION('center_axis',(0.,0.,1.));
#13168=DIRECTION('ref_axis',(1.,0.,0.));
#13169=DIRECTION('',(0.,0.,1.));
#13170=DIRECTION('center_axis',(0.,0.,-1.));
#13171=DIRECTION('ref_axis',(-1.,0.,0.));
#13172=DIRECTION('',(0.,0.,-1.));
#13173=DIRECTION('center_axis',(0.,0.,1.));
#13174=DIRECTION('ref_axis',(1.,0.,0.));
#13175=DIRECTION('',(0.,0.,-1.));
#13176=DIRECTION('center_axis',(0.,0.,1.));
#13177=DIRECTION('ref_axis',(1.,0.,0.));
#13178=DIRECTION('',(0.,0.,1.));
#13179=DIRECTION('center_axis',(0.,0.,-1.));
#13180=DIRECTION('ref_axis',(-1.,0.,0.));
#13181=DIRECTION('center_axis',(0.,0.,1.));
#13182=DIRECTION('ref_axis',(1.,0.,0.));
#13183=DIRECTION('',(0.,0.,-1.));
#13184=DIRECTION('center_axis',(0.,0.,1.));
#13185=DIRECTION('ref_axis',(1.,0.,0.));
#13186=DIRECTION('',(0.,0.,1.));
#13187=DIRECTION('center_axis',(0.,0.,-1.));
#13188=DIRECTION('ref_axis',(-1.,0.,0.));
#13189=DIRECTION('center_axis',(0.,0.,1.));
#13190=DIRECTION('ref_axis',(1.,0.,0.));
#13191=DIRECTION('',(0.,0.,-1.));
#13192=DIRECTION('center_axis',(0.,0.,1.));
#13193=DIRECTION('ref_axis',(1.,0.,0.));
#13194=DIRECTION('',(0.,0.,1.));
#13195=DIRECTION('center_axis',(0.,0.,-1.));
#13196=DIRECTION('ref_axis',(-1.,0.,0.));
#13197=DIRECTION('center_axis',(0.,0.,1.));
#13198=DIRECTION('ref_axis',(-0.999999999999999,4.09856065867257E-8,0.));
#13199=DIRECTION('',(0.,0.,-1.));
#13200=DIRECTION('center_axis',(0.,0.,1.));
#13201=DIRECTION('ref_axis',(1.,0.,0.));
#13202=DIRECTION('',(0.,0.,1.));
#13203=DIRECTION('center_axis',(0.,0.,-1.));
#13204=DIRECTION('ref_axis',(-1.,0.,0.));
#13205=DIRECTION('center_axis',(0.,0.,1.));
#13206=DIRECTION('ref_axis',(1.,0.,0.));
#13207=DIRECTION('center_axis',(0.,0.,1.));
#13208=DIRECTION('ref_axis',(1.,0.,0.));
#13209=DIRECTION('center_axis',(0.,0.,1.));
#13210=DIRECTION('ref_axis',(1.,0.,0.));
#13211=DIRECTION('center_axis',(0.,0.,1.));
#13212=DIRECTION('ref_axis',(1.,0.,0.));
#13213=DIRECTION('center_axis',(0.,0.,1.));
#13214=DIRECTION('ref_axis',(1.,0.,0.));
#13215=DIRECTION('center_axis',(0.,0.,1.));
#13216=DIRECTION('ref_axis',(1.,0.,0.));
#13217=DIRECTION('center_axis',(0.,0.,1.));
#13218=DIRECTION('ref_axis',(1.,0.,0.));
#13219=DIRECTION('center_axis',(0.,0.,1.));
#13220=DIRECTION('ref_axis',(1.,0.,0.));
#13221=DIRECTION('center_axis',(0.,0.,1.));
#13222=DIRECTION('ref_axis',(1.,0.,0.));
#13223=DIRECTION('center_axis',(0.,0.,1.));
#13224=DIRECTION('ref_axis',(1.,0.,0.));
#13225=DIRECTION('center_axis',(0.,0.,1.));
#13226=DIRECTION('ref_axis',(1.,0.,0.));
#13227=DIRECTION('center_axis',(0.,0.,1.));
#13228=DIRECTION('ref_axis',(1.,0.,0.));
#13229=DIRECTION('center_axis',(0.,0.,-1.));
#13230=DIRECTION('ref_axis',(-1.,0.,0.));
#13231=DIRECTION('center_axis',(0.,0.,-1.));
#13232=DIRECTION('ref_axis',(-1.,0.,0.));
#13233=DIRECTION('center_axis',(0.,0.,1.));
#13234=DIRECTION('ref_axis',(1.,0.,0.));
#13235=DIRECTION('',(0.,0.,-1.));
#13236=DIRECTION('center_axis',(0.,0.,-1.));
#13237=DIRECTION('ref_axis',(-1.,0.,0.));
#13238=DIRECTION('center_axis',(0.,0.,-1.));
#13239=DIRECTION('ref_axis',(-1.,0.,0.));
#13240=DIRECTION('center_axis',(0.,0.,-1.));
#13241=DIRECTION('ref_axis',(-1.,0.,0.));
#13242=DIRECTION('',(0.,0.,-1.));
#13243=DIRECTION('center_axis',(0.,0.,1.));
#13244=DIRECTION('ref_axis',(1.,0.,0.));
#13245=DIRECTION('center_axis',(0.,0.,1.));
#13246=DIRECTION('ref_axis',(1.,0.,0.));
#13247=DIRECTION('',(0.,0.,-1.));
#13248=DIRECTION('',(0.,0.,1.));
#13249=DIRECTION('center_axis',(0.,0.,-1.));
#13250=DIRECTION('ref_axis',(-1.,0.,0.));
#13251=DIRECTION('center_axis',(0.,0.,-1.));
#13252=DIRECTION('ref_axis',(-1.,0.,0.));
#13253=DIRECTION('center_axis',(0.,0.,1.));
#13254=DIRECTION('ref_axis',(1.,0.,0.));
#13255=DIRECTION('center_axis',(0.,0.,1.));
#13256=DIRECTION('ref_axis',(1.,0.,0.));
#13257=DIRECTION('center_axis',(0.,0.,-1.));
#13258=DIRECTION('ref_axis',(-1.,0.,0.));
#13259=DIRECTION('center_axis',(0.,0.,1.));
#13260=DIRECTION('ref_axis',(1.,0.,0.));
#13261=DIRECTION('center_axis',(0.,0.,1.));
#13262=DIRECTION('ref_axis',(1.,0.,0.));
#13263=DIRECTION('',(-0.028249590671202,3.45957707927105E-18,0.999600900673318));
#13264=DIRECTION('center_axis',(0.,0.,1.));
#13265=DIRECTION('ref_axis',(1.,0.,0.));
#13266=DIRECTION('',(0.,0.,-1.));
#13267=DIRECTION('center_axis',(0.,0.,1.));
#13268=DIRECTION('ref_axis',(1.,0.,0.));
#13269=DIRECTION('center_axis',(0.,0.,-1.));
#13270=DIRECTION('ref_axis',(-1.,0.,0.));
#13271=DIRECTION('center_axis',(0.,0.,1.));
#13272=DIRECTION('ref_axis',(1.,0.,0.));
#13273=DIRECTION('center_axis',(0.,0.,1.));
#13274=DIRECTION('ref_axis',(1.,0.,0.));
#13275=DIRECTION('',(0.,0.,-1.));
#13276=DIRECTION('center_axis',(0.,0.,1.));
#13277=DIRECTION('ref_axis',(1.,0.,0.));
#13278=DIRECTION('center_axis',(0.,0.,1.));
#13279=DIRECTION('ref_axis',(1.,0.,0.));
#13280=DIRECTION('center_axis',(0.,0.,-1.));
#13281=DIRECTION('ref_axis',(-1.,0.,0.));
#13282=DIRECTION('',(-0.707106781186543,8.65956056235487E-17,0.707106781186552));
#13283=DIRECTION('center_axis',(0.,0.,1.));
#13284=DIRECTION('ref_axis',(1.,0.,0.));
#13285=DIRECTION('center_axis',(0.,0.,1.));
#13286=DIRECTION('ref_axis',(1.,0.,0.));
#13287=DIRECTION('center_axis',(0.,0.,1.));
#13288=DIRECTION('ref_axis',(1.,0.,0.));
#13289=DIRECTION('',(0.,0.,1.));
#13290=DIRECTION('center_axis',(0.,1.,0.));
#13291=DIRECTION('ref_axis',(0.,0.,1.));
#13292=DIRECTION('',(0.,1.,0.));
#13293=DIRECTION('center_axis',(-0.951056516295155,0.309016994374945,0.));
#13294=DIRECTION('ref_axis',(-0.309016994374945,-0.951056516295155,0.));
#13295=DIRECTION('',(-0.951056516295154,0.309016994374945,0.));
#13296=DIRECTION('center_axis',(0.95105651629515,0.309016994374958,0.));
#13297=DIRECTION('ref_axis',(-0.309016994374958,0.95105651629515,0.));
#13298=DIRECTION('',(0.95105651629515,0.309016994374958,0.));
#13299=DIRECTION('center_axis',(0.58778525229248,-0.809016994374942,0.));
#13300=DIRECTION('ref_axis',(0.809016994374942,0.58778525229248,0.));
#13301=DIRECTION('',(0.58778525229248,-0.809016994374942,0.));
#13302=DIRECTION('center_axis',(-0.587785252292469,-0.809016994374951,0.));
#13303=DIRECTION('ref_axis',(0.809016994374951,-0.587785252292469,0.));
#13304=DIRECTION('',(-0.587785252292469,-0.809016994374951,0.));
#13305=DIRECTION('center_axis',(0.,0.,-1.));
#13306=DIRECTION('ref_axis',(-1.,0.,0.));
#13307=DIRECTION('center_axis',(0.,0.,1.));
#13308=DIRECTION('ref_axis',(-1.,0.,0.));
#13309=DIRECTION('',(0.,0.,-1.));
#13310=DIRECTION('center_axis',(0.,0.,-1.));
#13311=DIRECTION('ref_axis',(-1.,0.,0.));
#13312=DIRECTION('',(0.707106781186551,-8.65956056235497E-17,-0.707106781186544));
#13313=DIRECTION('center_axis',(0.,0.,1.));
#13314=DIRECTION('ref_axis',(1.,0.,0.));
#13315=DIRECTION('center_axis',(0.,0.,1.));
#13316=DIRECTION('ref_axis',(1.,0.,0.));
#13317=DIRECTION('center_axis',(0.,0.,1.));
#13318=DIRECTION('ref_axis',(1.,0.,0.));
#13319=DIRECTION('',(0.,0.,1.));
#13320=DIRECTION('center_axis',(0.,0.,1.));
#13321=DIRECTION('ref_axis',(1.,0.,0.));
#13322=DIRECTION('center_axis',(0.,0.,-1.));
#13323=DIRECTION('ref_axis',(-1.,0.,0.));
#13324=DIRECTION('center_axis',(0.,0.,-1.));
#13325=DIRECTION('ref_axis',(-1.,0.,0.));
#13326=DIRECTION('',(0.,0.,-1.));
#13327=DIRECTION('center_axis',(0.,0.,-1.));
#13328=DIRECTION('ref_axis',(1.,0.,0.));
#13329=DIRECTION('',(0.,0.,1.));
#13330=DIRECTION('center_axis',(0.,0.,-1.));
#13331=DIRECTION('ref_axis',(0.951056370825966,-0.309017442082712,0.));
#13332=DIRECTION('',(0.,0.,-1.));
#13333=DIRECTION('center_axis',(0.,0.,-1.));
#13334=DIRECTION('ref_axis',(1.,0.,0.));
#13335=DIRECTION('',(0.,0.,1.));
#13336=DIRECTION('center_axis',(0.,0.,-1.));
#13337=DIRECTION('ref_axis',(0.951056516295154,0.309016994374948,0.));
#13338=DIRECTION('',(0.,0.,-1.));
#13339=DIRECTION('center_axis',(0.,0.,-1.));
#13340=DIRECTION('ref_axis',(1.,-3.47868984768418E-15,0.));
#13341=DIRECTION('',(0.,0.,1.));
#13342=DIRECTION('center_axis',(0.,0.,-1.));
#13343=DIRECTION('ref_axis',(-1.,0.,0.));
#13344=DIRECTION('',(0.,0.,-1.));
#13345=DIRECTION('center_axis',(0.,0.,-1.));
#13346=DIRECTION('ref_axis',(1.,-7.73042188374262E-16,0.));
#13347=DIRECTION('',(0.,0.,1.));
#13348=DIRECTION('center_axis',(0.,0.,-1.));
#13349=DIRECTION('ref_axis',(-1.,0.,0.));
#13350=DIRECTION('',(0.,0.,-1.));
#13351=DIRECTION('center_axis',(0.,0.,-1.));
#13352=DIRECTION('ref_axis',(1.,0.,0.));
#13353=DIRECTION('',(0.,0.,1.));
#13354=DIRECTION('center_axis',(0.,0.,-1.));
#13355=DIRECTION('ref_axis',(-1.,0.,0.));
#13356=DIRECTION('',(0.,0.,-1.));
#13357=DIRECTION('center_axis',(0.,0.,-1.));
#13358=DIRECTION('ref_axis',(1.,0.,0.));
#13359=DIRECTION('',(0.,0.,1.));
#13360=DIRECTION('center_axis',(0.,0.,-1.));
#13361=DIRECTION('ref_axis',(-1.,0.,0.));
#13362=DIRECTION('',(0.,0.,-1.));
#13363=DIRECTION('center_axis',(0.,0.,-1.));
#13364=DIRECTION('ref_axis',(1.,9.66302735467828E-16,0.));
#13365=DIRECTION('',(0.,0.,1.));
#13366=DIRECTION('center_axis',(0.,0.,-1.));
#13367=DIRECTION('ref_axis',(-1.,0.,0.));
#13368=DIRECTION('',(0.,0.,-1.));
#13369=DIRECTION('center_axis',(0.,0.,-1.));
#13370=DIRECTION('ref_axis',(1.,1.73934492384209E-15,0.));
#13371=DIRECTION('',(0.,0.,1.));
#13372=DIRECTION('center_axis',(0.,0.,-1.));
#13373=DIRECTION('ref_axis',(-1.,0.,0.));
#13374=DIRECTION('',(0.,0.,-1.));
#13375=DIRECTION('center_axis',(0.,0.,-1.));
#13376=DIRECTION('ref_axis',(1.,7.73042188374263E-16,0.));
#13377=DIRECTION('',(0.,0.,1.));
#13378=DIRECTION('center_axis',(0.,0.,-1.));
#13379=DIRECTION('ref_axis',(-1.,0.,0.));
#13380=DIRECTION('',(0.,0.,-1.));
#13381=DIRECTION('center_axis',(0.,0.,-1.));
#13382=DIRECTION('ref_axis',(1.,0.,0.));
#13383=DIRECTION('',(0.,0.,1.));
#13384=DIRECTION('center_axis',(-0.133354245949418,0.449306005611305,-0.883368982027825));
#13385=DIRECTION('ref_axis',(-0.236981598329056,0.85101681114339,0.468625766688881));
#13386=DIRECTION('center_axis',(0.,0.,-1.));
#13387=DIRECTION('ref_axis',(-1.,0.,0.));
#13388=DIRECTION('center_axis',(0.,0.,1.));
#13389=DIRECTION('ref_axis',(1.,0.,0.));
#13390=DIRECTION('center_axis',(0.,0.,1.));
#13391=DIRECTION('ref_axis',(1.,0.,0.));
#13392=DIRECTION('center_axis',(0.156188207235421,0.441878562474938,-0.883373409123043));
#13393=DIRECTION('ref_axis',(0.308715861485718,0.827704076309612,0.468615491557399));
#13394=DIRECTION('center_axis',(0.,0.,-1.));
#13395=DIRECTION('ref_axis',(-1.,0.,0.));
#13396=DIRECTION('center_axis',(0.,0.,1.));
#13397=DIRECTION('ref_axis',(1.,0.,0.));
#13398=DIRECTION('center_axis',(0.,0.,1.));
#13399=DIRECTION('ref_axis',(-0.951056516295154,-0.309016994374948,0.));
#13400=DIRECTION('center_axis',(0.,0.,-1.));
#13401=DIRECTION('ref_axis',(0.995706539546764,-0.0925661228733769,0.));
#13402=DIRECTION('center_axis',(0.,0.,1.));
#13403=DIRECTION('ref_axis',(1.,0.,0.));
#13404=DIRECTION('center_axis',(0.,0.,1.));
#13405=DIRECTION('ref_axis',(-0.951056516295153,0.309016994374948,0.));
#13406=DIRECTION('center_axis',(0.468516296465704,-0.0119958265706286,-0.883373409205274));
#13407=DIRECTION('ref_axis',(0.88259180291303,-0.0378316095121115,0.468615491370537));
#13408=DIRECTION('center_axis',(0.,0.,-1.));
#13409=DIRECTION('ref_axis',(-1.,0.,0.));
#13410=DIRECTION('center_axis',(0.,0.,1.));
#13411=DIRECTION('ref_axis',(1.,0.,0.));
#13412=DIRECTION('center_axis',(0.,0.,1.));
#13413=DIRECTION('ref_axis',(1.,0.,0.));
#13414=DIRECTION('center_axis',(0.,0.,-1.));
#13415=DIRECTION('ref_axis',(-1.,0.,0.));
#13416=DIRECTION('center_axis',(0.,0.,1.));
#13417=DIRECTION('ref_axis',(1.,0.,0.));
#13418=DIRECTION('center_axis',(0.,0.,1.));
#13419=DIRECTION('ref_axis',(1.,0.,0.));
#13420=DIRECTION('center_axis',(0.133354245974411,-0.449306005592514,-0.88336898203361));
#13421=DIRECTION('ref_axis',(-0.23698159806395,0.851016811224501,-0.468625766675648));
#13422=DIRECTION('center_axis',(0.,0.,-1.));
#13423=DIRECTION('ref_axis',(-1.,0.,0.));
#13424=DIRECTION('center_axis',(0.,0.,1.));
#13425=DIRECTION('ref_axis',(1.,0.,0.));
#13426=DIRECTION('center_axis',(0.,0.,1.));
#13427=DIRECTION('ref_axis',(1.,0.,0.));
#13428=DIRECTION('center_axis',(-0.156188207223913,-0.441878562475276,-0.883373409124909));
#13429=DIRECTION('ref_axis',(0.308715861503055,0.827704076305292,-0.468615491553608));
#13430=DIRECTION('center_axis',(0.,0.,-1.));
#13431=DIRECTION('ref_axis',(-1.,0.,0.));
#13432=DIRECTION('center_axis',(0.,0.,1.));
#13433=DIRECTION('ref_axis',(-0.995706539546737,-0.0925661228736592,0.));
#13434=DIRECTION('center_axis',(0.,0.,1.));
#13435=DIRECTION('ref_axis',(1.,0.,0.));
#13436=DIRECTION('center_axis',(0.,0.,-1.));
#13437=DIRECTION('ref_axis',(-1.,0.,0.));
#13438=DIRECTION('center_axis',(0.,0.,1.));
#13439=DIRECTION('ref_axis',(1.,0.,0.));
#13440=DIRECTION('center_axis',(0.,0.,1.));
#13441=DIRECTION('ref_axis',(1.,0.,0.));
#13442=DIRECTION('center_axis',(-0.468516296601123,0.0119958269794971,-0.883373409127899));
#13443=DIRECTION('ref_axis',(0.882591802968309,-0.0378316060417926,-0.468615491546586));
#13444=DIRECTION('center_axis',(0.,0.,-1.));
#13445=DIRECTION('ref_axis',(-1.,0.,0.));
#13446=DIRECTION('center_axis',(0.,0.,1.));
#13447=DIRECTION('ref_axis',(1.,0.,0.));
#13448=DIRECTION('center_axis',(0.,0.,1.));
#13449=DIRECTION('ref_axis',(1.,0.,0.));
#13450=DIRECTION('center_axis',(0.,0.,-1.));
#13451=DIRECTION('ref_axis',(-1.,0.,0.));
#13452=DIRECTION('center_axis',(0.,0.,1.));
#13453=DIRECTION('ref_axis',(1.,0.,0.));
#13454=DIRECTION('center_axis',(0.,0.,1.));
#13455=DIRECTION('ref_axis',(1.,0.,0.));
#28029=CARTESIAN_POINT('',(0.,0.,0.));
#28030=CARTESIAN_POINT('Origin',(0.,0.,0.));
#28031=CARTESIAN_POINT('',(-3.38063404204883,17.1703614834907,5.26598123633362E-16));
#28032=CARTESIAN_POINT('',(-7.35749486474657,15.8782010730192,5.26598123633362E-16));
#28033=CARTESIAN_POINT('Origin',(0.,0.,5.26598123633362E-16));
#28034=CARTESIAN_POINT('',(-7.75098709974896,15.6898756840048,0.134720657333156));
#28035=CARTESIAN_POINT('Ctrl Pts',(-7.35749486474656,15.8782010730192,4.02239005992122E-16));
#28036=CARTESIAN_POINT('Ctrl Pts',(-7.40654917656635,15.8554707369032,-1.1304709011049E-17));
#28037=CARTESIAN_POINT('Ctrl Pts',(-7.45547662735319,15.8325185186142,0.0057118776195191));
#28038=CARTESIAN_POINT('Ctrl Pts',(-7.58311255681024,15.771945196048,0.0353494158279855));
#28039=CARTESIAN_POINT('Ctrl Pts',(-7.66048059708591,15.7344445945251,0.0693026530250561));
#28040=CARTESIAN_POINT('Ctrl Pts',(-7.73596042367391,15.6972924318009,0.123164970119313));
#28041=CARTESIAN_POINT('Ctrl Pts',(-7.74353659553706,15.6935563226023,0.12884558346146));
#28042=CARTESIAN_POINT('Ctrl Pts',(-7.75098709974896,15.6898756840048,0.134720657333156));
#28043=CARTESIAN_POINT('',(-7.75098748126848,15.6898754955296,98.476464169983));
#28044=CARTESIAN_POINT('',(-7.75098709974896,15.6898756840048,0.));
#28045=CARTESIAN_POINT('',(-7.62166407822416,15.7531022199328,98.5000002325512));
#28046=CARTESIAN_POINT('Ctrl Pts',(-7.75098827006065,15.6898751058567,98.4764666117908));
#28047=CARTESIAN_POINT('Ctrl Pts',(-7.73036519553247,15.7000631543709,98.4847544570797));
#28048=CARTESIAN_POINT('Ctrl Pts',(-7.70899812928367,15.7105675084655,98.4906432907328));
#28049=CARTESIAN_POINT('Ctrl Pts',(-7.6656344940948,15.7317713310211,98.4982621653015));
#28050=CARTESIAN_POINT('Ctrl Pts',(-7.64364124698384,15.7424694536167,98.5000001531237));
#28051=CARTESIAN_POINT('Ctrl Pts',(-7.62166492311257,15.7531020373701,98.5000000867633));
#28052=CARTESIAN_POINT('',(-3.09338542091479,17.2244295086968,98.5000006225421));
#28053=CARTESIAN_POINT('Origin',(0.,0.,98.5));
#28054=CARTESIAN_POINT('',(-2.95159725048241,17.2492919759318,98.4764616066469));
#28055=CARTESIAN_POINT('Ctrl Pts',(-3.09338528775832,17.2244293798512,98.5000011593602));
#28056=CARTESIAN_POINT('Ctrl Pts',(-3.06935680199578,17.228744725382,98.5000018789964));
#28057=CARTESIAN_POINT('Ctrl Pts',(-3.04527498726421,17.2330171964727,98.4982647459743));
#28058=CARTESIAN_POINT('Ctrl Pts',(-2.99772878170085,17.241351622266,98.4906474053966));
#28059=CARTESIAN_POINT('Ctrl Pts',(-2.97426775127845,17.2454127370105,98.4847593539947));
#28060=CARTESIAN_POINT('Ctrl Pts',(-2.95159454990789,17.249292438038,98.4764721130873));
#28061=CARTESIAN_POINT('',(-2.95159725048241,17.2492919759318,0.134720657333159));
#28062=CARTESIAN_POINT('',(-2.95159725048241,17.2492919759318,0.));
#28063=CARTESIAN_POINT('Ctrl Pts',(-2.95159725048241,17.2492919759318,0.134720657333162));
#28064=CARTESIAN_POINT('Ctrl Pts',(-3.01054883678071,17.2392045276891,0.0924371122250883));
#28065=CARTESIAN_POINT('Ctrl Pts',(-3.07862853003574,17.2272341593699,0.0586496504523806));
#28066=CARTESIAN_POINT('Ctrl Pts',(-3.22585327793649,17.2002767814783,0.0120815387590075));
#28067=CARTESIAN_POINT('Ctrl Pts',(-3.3034974264849,17.1855487390831,4.12448671408897E-16));
#28068=CARTESIAN_POINT('Ctrl Pts',(-3.38063404204883,17.1703614834907,4.16333634234434E-16));
#28069=CARTESIAN_POINT('Origin',(0.,0.,0.));
#28070=CARTESIAN_POINT('',(7.7509870154707,15.6898756108788,98.4764611650906));
#28071=CARTESIAN_POINT('',(7.75098709974897,15.6898756840048,0.13472065733317));
#28072=CARTESIAN_POINT('',(7.75098709974897,15.6898756840048,0.));
#28073=CARTESIAN_POINT('',(7.35749486474656,15.8782010730192,5.26598123633362E-16));
#28074=CARTESIAN_POINT('Ctrl Pts',(7.75098709974897,15.6898756840048,0.134720657333169));
#28075=CARTESIAN_POINT('Ctrl Pts',(7.697365011278,15.716365639972,0.092437112225102));
#28076=CARTESIAN_POINT('Ctrl Pts',(7.6352513765003,15.7466976482487,0.0586496504523873));
#28077=CARTESIAN_POINT('Ctrl Pts',(7.50029890429084,15.8114252069992,0.0120815387590058));
#28078=CARTESIAN_POINT('Ctrl Pts',(7.42882654248636,15.8451480558511,-2.91946290751094E-16));
#28079=CARTESIAN_POINT('Ctrl Pts',(7.35749486474656,15.8782010730192,4.16333634234434E-16));
#28080=CARTESIAN_POINT('',(3.38063404204883,17.1703614834907,5.26598123633362E-16));
#28081=CARTESIAN_POINT('Origin',(0.,0.,5.26598123633362E-16));
#28082=CARTESIAN_POINT('',(2.95159725048241,17.2492919759318,0.134720657333159));
#28083=CARTESIAN_POINT('Ctrl Pts',(3.38063404204883,17.1703614834907,3.78386558197441E-16));
#28084=CARTESIAN_POINT('Ctrl Pts',(3.32758771379059,17.180805656334,3.54366411019119E-16));
#28085=CARTESIAN_POINT('Ctrl Pts',(3.27451359919498,17.1909957556844,0.00571187761951955));
#28086=CARTESIAN_POINT('Ctrl Pts',(3.13564985748462,17.2170134253201,0.0353494158279847));
#28087=CARTESIAN_POINT('Ctrl Pts',(3.05101549755283,17.2321505944616,0.0693026530250554));
#28088=CARTESIAN_POINT('Ctrl Pts',(2.96811354177061,17.2464597923539,0.123164970119314));
#28089=CARTESIAN_POINT('Ctrl Pts',(2.95978826009315,17.2478903786094,0.128845583461463));
#28090=CARTESIAN_POINT('Ctrl Pts',(2.95159725048241,17.2492919759318,0.134720657333162));
#28091=CARTESIAN_POINT('',(2.95159683426415,17.2492920471526,98.4764641502857));
#28092=CARTESIAN_POINT('',(2.95159725048241,17.2492919759318,0.));
#28093=CARTESIAN_POINT('',(3.09338455449675,17.2244295302922,98.5000000582798));
#28094=CARTESIAN_POINT('Ctrl Pts',(2.95159597373243,17.2492921944017,98.4764665733303));
#28095=CARTESIAN_POINT('Ctrl Pts',(2.97426877032574,17.245412560711,98.4847544660921));
#28096=CARTESIAN_POINT('Ctrl Pts',(2.99772938956493,17.2413515161254,98.4906433246677));
#28097=CARTESIAN_POINT('Ctrl Pts',(3.04527460155141,17.2330172636463,98.4982622140882));
#28098=CARTESIAN_POINT('Ctrl Pts',(3.06935553227654,17.2287449523539,98.5000001907974));
#28099=CARTESIAN_POINT('Ctrl Pts',(3.09338455123434,17.2244295121256,98.5000001151055));
#28100=CARTESIAN_POINT('',(7.62166294207788,15.7531030650529,98.5000002711098));
#28101=CARTESIAN_POINT('Origin',(0.,0.,98.5));
#28102=CARTESIAN_POINT('Ctrl Pts',(7.62166291493897,15.7531030089644,98.5000005001312));
#28103=CARTESIAN_POINT('Ctrl Pts',(7.6436435511221,15.7424683422865,98.5000007104308));
#28104=CARTESIAN_POINT('Ctrl Pts',(7.66563431697673,15.7317714169945,98.4982623363922));
#28105=CARTESIAN_POINT('Ctrl Pts',(7.70900073858223,15.7105662332998,98.4906410122901));
#28106=CARTESIAN_POINT('Ctrl Pts',(7.73036164225094,15.7000649076559,98.4847522013256));
#28107=CARTESIAN_POINT('Ctrl Pts',(7.7509869987881,15.6898757338807,98.4764609724326));
#28108=CARTESIAN_POINT('Origin',(0.,0.,0.));
#28109=CARTESIAN_POINT('',(15.4929577055454,8.13746014975801,98.4764611351391));
#28110=CARTESIAN_POINT('',(15.4929578242382,8.13746016004849,0.134720657333155));
#28111=CARTESIAN_POINT('',(15.4929578242382,8.13746016004849,0.));
#28112=CARTESIAN_POINT('',(15.2853108052616,8.52110753285942,5.26598123633362E-16));
#28113=CARTESIAN_POINT('Ctrl Pts',(15.4929578242382,8.13746016004849,0.134720657333156));
#28114=CARTESIAN_POINT('Ctrl Pts',(15.4651470488427,8.19040925740651,0.0924371122251327));
#28115=CARTESIAN_POINT('Ctrl Pts',(15.4327247698627,8.25145784606448,0.0586496504524068));
#28116=CARTESIAN_POINT('Ctrl Pts',(15.3615918308627,8.38314661402319,0.0120815387590046));
#28117=CARTESIAN_POINT('Ctrl Pts',(15.3235912687552,8.45243937205836,-8.0627802103072E-17));
#28118=CARTESIAN_POINT('Ctrl Pts',(15.2853108052616,8.52110753285941,4.16333634234434E-16));
#28119=CARTESIAN_POINT('',(12.8274756483065,11.9040274063908,5.26598123633362E-16));
#28120=CARTESIAN_POINT('Origin',(0.,0.,5.26598123633362E-16));
#28121=CARTESIAN_POINT('',(12.5267717721302,12.2200650149237,0.134720657333169));
#28122=CARTESIAN_POINT('Ctrl Pts',(12.8274756483065,11.9040274063908,4.38017677684144E-16));
#28123=CARTESIAN_POINT('Ctrl Pts',(12.7906991980261,11.9436567691517,-2.13930726438973E-16));
#28124=CARTESIAN_POINT('Ctrl Pts',(12.7537509274744,11.9830969145383,0.00571187761951889));
#28125=CARTESIAN_POINT('Ctrl Pts',(12.6567006030391,12.0857677108831,0.0353494158279851));
#28126=CARTESIAN_POINT('Ctrl Pts',(12.597127372329,12.1477607665704,0.0693026530250562));
#28127=CARTESIAN_POINT('Ctrl Pts',(12.5384690167276,12.2080656978362,0.123164970119317));
#28128=CARTESIAN_POINT('Ctrl Pts',(12.5325745998707,12.2141165442201,0.128845583461466));
#28129=CARTESIAN_POINT('Ctrl Pts',(12.5267717721302,12.2200650149237,0.134720657333167));
#28130=CARTESIAN_POINT('',(12.5267714753738,12.2200653191283,98.4764641666045));
#28131=CARTESIAN_POINT('',(12.5267717721302,12.2200650149237,0.));
#28132=CARTESIAN_POINT('',(12.6268663170878,12.1166104030896,98.5000000583843));
#28133=CARTESIAN_POINT('Ctrl Pts',(12.5267708618295,12.2200659480716,98.4764666051942));
#28134=CARTESIAN_POINT('Ctrl Pts',(12.5428331499379,12.2036005211659,98.4847544881405));
#28135=CARTESIAN_POINT('Ctrl Pts',(12.5594261690095,12.1865252595175,98.4906433390831));
#28136=CARTESIAN_POINT('Ctrl Pts',(12.5929923076291,12.1518363282392,98.4982622190212));
#28137=CARTESIAN_POINT('Ctrl Pts',(12.6099629957874,12.1342255319368,98.5000001912344));
#28138=CARTESIAN_POINT('Ctrl Pts',(12.6268663036908,12.1166103902337,98.500000115428));
#28139=CARTESIAN_POINT('',(15.4254964602665,8.26462701674586,98.5000002246578));
#28140=CARTESIAN_POINT('Origin',(0.,0.,98.5));
#28141=CARTESIAN_POINT('Ctrl Pts',(15.4254964408324,8.26462700633656,98.5000005203777));
#28142=CARTESIAN_POINT('Ctrl Pts',(15.4370282602941,8.24310346511366,98.5000007416219));
#28143=CARTESIAN_POINT('Ctrl Pts',(15.4485316552151,8.22152364814352,98.4982623777968));
#28144=CARTESIAN_POINT('Ctrl Pts',(15.471151745739,8.17887812715057,98.4906410339749));
#28145=CARTESIAN_POINT('Ctrl Pts',(15.4822605547264,8.15782675347633,98.4847521990831));
#28146=CARTESIAN_POINT('Ctrl Pts',(15.4929577683353,8.13746026648231,98.4764609294304));
#28147=CARTESIAN_POINT('Origin',(0.,0.,0.));
#28148=CARTESIAN_POINT('',(17.3171451173558,-2.52318944679936,98.4764669873976));
#28149=CARTESIAN_POINT('',(17.3171452461371,-2.52318856294819,0.134720657333157));
#28150=CARTESIAN_POINT('',(17.3171452461371,-2.52318856294819,0.));
#28151=CARTESIAN_POINT('',(17.3746575467727,-2.0907594630599,5.26598123633362E-16));
#28152=CARTESIAN_POINT('Ctrl Pts',(17.3171452461371,-2.52318856294818,0.134720657333159));
#28153=CARTESIAN_POINT('Ctrl Pts',(17.3257685547646,-2.46400507971643,0.0924371122251101));
#28154=CARTESIAN_POINT('Ctrl Pts',(17.3354218401598,-2.3955583965793,0.0586496504523934));
#28155=CARTESIAN_POINT('Ctrl Pts',(17.3552787993477,-2.24720905283605,0.012081538759007));
#28156=CARTESIAN_POINT('Ctrl Pts',(17.3652649600707,-2.1688138640129,4.12448671408897E-16));
#28157=CARTESIAN_POINT('Ctrl Pts',(17.3746575467727,-2.0907594630599,4.16333634234434E-16));
#28158=CARTESIAN_POINT('',(17.3746575467727,2.09075946305989,5.26598123633362E-16));
#28159=CARTESIAN_POINT('Origin',(0.,0.,5.26598123633362E-16));
#28160=CARTESIAN_POINT('',(17.3171452461371,2.52318856294818,0.134720657333156));
#28161=CARTESIAN_POINT('Ctrl Pts',(17.3746575467727,2.09075946305989,3.50197301712818E-16));
#28162=CARTESIAN_POINT('Ctrl Pts',(17.3681983284916,2.14443694611619,-1.60626590021751E-17));
#28163=CARTESIAN_POINT('Ctrl Pts',(17.3614888855091,2.19806234252259,0.00571187761951884));
#28164=CARTESIAN_POINT('Ctrl Pts',(17.3433219036639,2.33816951102481,0.0353494158279827));
#28165=CARTESIAN_POINT('Ctrl Pts',(17.3315647514872,2.42333921305185,0.069302653025052));
#28166=CARTESIAN_POINT('Ctrl Pts',(17.3195554941821,2.50660544363676,0.123164970119312));
#28167=CARTESIAN_POINT('Ctrl Pts',(17.3183434090412,2.51496533249098,0.12884558346146));
#28168=CARTESIAN_POINT('Ctrl Pts',(17.3171452461371,2.52318856294818,0.134720657333157));
#28169=CARTESIAN_POINT('',(17.3171451847825,2.52318898403686,98.476464169983));
#28170=CARTESIAN_POINT('',(17.3171452461371,2.52318856294818,0.));
#28171=CARTESIAN_POINT('',(17.3373142437191,2.38065698652278,98.5000002325512));
#28172=CARTESIAN_POINT('Ctrl Pts',(17.3171450579317,2.52318985463833,98.4764666117908));
#28173=CARTESIAN_POINT('Ctrl Pts',(17.3204615873541,2.50042786509176,98.4847544570796));
#28174=CARTESIAN_POINT('Ctrl Pts',(17.3238490351745,2.47686055357144,98.4906432907328));
#28175=CARTESIAN_POINT('Ctrl Pts',(17.3306149685751,2.42906694423961,98.4982621653014));
#28176=CARTESIAN_POINT('Ctrl Pts',(17.3339932006629,2.40484422157029,98.5000001531237));
#28177=CARTESIAN_POINT('Ctrl Pts',(17.3373143311766,2.38065784647434,98.5000000867633));
#28178=CARTESIAN_POINT('',(17.5,-2.14313189850787E-15,98.5));
#28179=CARTESIAN_POINT('Origin',(0.,0.,98.5));
#28180=CARTESIAN_POINT('',(17.337314588927,-2.38065707462705,98.5000006225421));
#28181=CARTESIAN_POINT('Origin',(0.,0.,98.5));
#28182=CARTESIAN_POINT('Ctrl Pts',(17.3373144252399,-2.3806571614509,98.5000011593602));
#28183=CARTESIAN_POINT('Ctrl Pts',(17.3339933522773,-2.40484312451782,98.5000018789964));
#28184=CARTESIAN_POINT('Ctrl Pts',(17.3306150237414,-2.42906655751746,98.4982647459742));
#28185=CARTESIAN_POINT('Ctrl Pts',(17.3238489481645,-2.47686116535237,98.4906474053964));
#28186=CARTESIAN_POINT('Ctrl Pts',(17.3204614406997,-2.50042888468657,98.4847593539944));
#28187=CARTESIAN_POINT('Ctrl Pts',(17.3171448511027,-2.52319127414576,98.476472113087));
#28188=CARTESIAN_POINT('Origin',(0.,0.,0.));
#28189=CARTESIAN_POINT('',(12.8274756483065,-11.9040274063908,5.26598123633362E-16));
#28190=CARTESIAN_POINT('',(15.2853108052616,-8.52110753285942,5.26598123633362E-16));
#28191=CARTESIAN_POINT('Origin',(0.,0.,5.26598123633362E-16));
#28192=CARTESIAN_POINT('',(15.4929578242382,-8.13746016004849,0.134720657333159));
#28193=CARTESIAN_POINT('Ctrl Pts',(15.2853108052616,-8.52110753285942,5.64869331864948E-16));
#28194=CARTESIAN_POINT('Ctrl Pts',(15.3116360208225,-8.47388490360466,5.23827033142938E-16));
#28195=CARTESIAN_POINT('Ctrl Pts',(15.3377281845829,-8.42655733494556,0.00571187761951928));
#28196=CARTESIAN_POINT('Ctrl Pts',(15.4053837149197,-8.30252997058624,0.0353494158279845));
#28197=CARTESIAN_POINT('Ctrl Pts',(15.4459334737969,-8.22671555358209,0.0693026530250558));
#28198=CARTESIAN_POINT('Ctrl Pts',(15.485160442899,-8.15229289364641,0.123164970119313));
#28199=CARTESIAN_POINT('Ctrl Pts',(15.4890936648008,-8.14481715572195,0.128845583461463));
#28200=CARTESIAN_POINT('Ctrl Pts',(15.4929578242382,-8.13746016004849,0.13472065733316));
#28201=CARTESIAN_POINT('',(15.4929580205917,-8.13745978620985,98.4764641502857));
#28202=CARTESIAN_POINT('',(15.4929578242382,-8.13746016004849,0.));
#28203=CARTESIAN_POINT('',(15.4254975467744,-8.26462498123526,98.5000000582797));
#28204=CARTESIAN_POINT('Ctrl Pts',(15.4929584265528,-8.137459013298,98.4764665733302));
#28205=CARTESIAN_POINT('Ctrl Pts',(15.4822623961932,-8.15782325149815,98.4847544660919));
#28206=CARTESIAN_POINT('Ctrl Pts',(15.4711503832338,-8.17888069450974,98.4906433246675));
#28207=CARTESIAN_POINT('Ctrl Pts',(15.4485317595999,-8.22152345253711,98.4982622140881));
#28208=CARTESIAN_POINT('Ctrl Pts',(15.4370271332713,-8.24310556182698,98.5000001907974));
#28209=CARTESIAN_POINT('Ctrl Pts',(15.4254975305051,-8.26462497251875,98.5000001151055));
#28210=CARTESIAN_POINT('',(12.626867931918,-12.1166087252795,98.5000002246578));
#28211=CARTESIAN_POINT('Origin',(0.,0.,98.5));
#28212=CARTESIAN_POINT('',(12.5267717256653,-12.22006490522,98.476461135139));
#28213=CARTESIAN_POINT('Ctrl Pts',(12.6268679160127,-12.1166087100132,98.5000005203778));
#28214=CARTESIAN_POINT('Ctrl Pts',(12.6099613400687,-12.134227262074,98.5000007416219));
#28215=CARTESIAN_POINT('Ctrl Pts',(12.5929924590424,-12.1518361709524,98.4982623777968));
#28216=CARTESIAN_POINT('Ctrl Pts',(12.5594241507975,-12.1865273461652,98.4906410339749));
#28217=CARTESIAN_POINT('Ctrl Pts',(12.5428359154519,-12.2035976835612,98.484752199083));
#28218=CARTESIAN_POINT('Ctrl Pts',(12.5267718560799,-12.220064928867,98.4764609294303));
#28219=CARTESIAN_POINT('',(12.5267717721302,-12.2200650149237,0.134720657333167));
#28220=CARTESIAN_POINT('',(12.5267717721302,-12.2200650149237,0.));
#28221=CARTESIAN_POINT('Ctrl Pts',(12.5267717721302,-12.2200650149237,0.134720657333168));
#28222=CARTESIAN_POINT('Ctrl Pts',(12.5685353539806,-12.1772532248401,0.0924371122250518));
#28223=CARTESIAN_POINT('Ctrl Pts',(12.6165769768333,-12.127552753765,0.0586496504523597));
#28224=CARTESIAN_POINT('Ctrl Pts',(12.7198391507123,-12.0192072413384,0.0120815387590086));
#28225=CARTESIAN_POINT('Ctrl Pts',(12.7739976602867,-11.9616539193032,-7.14583268047246E-16));
#28226=CARTESIAN_POINT('Ctrl Pts',(12.8274756483065,-11.9040274063908,4.16333634234434E-16));
#28227=CARTESIAN_POINT('Origin',(0.,0.,0.));
#28228=CARTESIAN_POINT('',(2.95159637009437,-17.2492921265785,98.4764669873977));
#28229=CARTESIAN_POINT('',(2.95159725048241,-17.2492919759318,0.134720657333156));
#28230=CARTESIAN_POINT('',(2.95159725048241,-17.2492919759318,0.));
#28231=CARTESIAN_POINT('',(3.38063404204883,-17.1703614834907,5.26598123633362E-16));
#28232=CARTESIAN_POINT('Ctrl Pts',(2.95159725048241,-17.2492919759318,0.134720657333158));
#28233=CARTESIAN_POINT('Ctrl Pts',(3.01054883678064,-17.2392045276891,0.092437112225137));
#28234=CARTESIAN_POINT('Ctrl Pts',(3.07862853003564,-17.2272341593699,0.0586496504524089));
#28235=CARTESIAN_POINT('Ctrl Pts',(3.22585327793649,-17.2002767814783,0.0120815387590052));
#28236=CARTESIAN_POINT('Ctrl Pts',(3.3034974264849,-17.1855487390831,2.01130182760907E-16));
#28237=CARTESIAN_POINT('Ctrl Pts',(3.38063404204882,-17.1703614834907,4.16333634234434E-16));
#28238=CARTESIAN_POINT('',(7.35749486474657,-15.8782010730192,5.26598123633362E-16));
#28239=CARTESIAN_POINT('Origin',(0.,0.,5.26598123633362E-16));
#28240=CARTESIAN_POINT('',(7.75098709974897,-15.6898756840048,0.134720657333169));
#28241=CARTESIAN_POINT('Ctrl Pts',(7.35749486474656,-15.8782010730192,5.13911829758129E-16));
#28242=CARTESIAN_POINT('Ctrl Pts',(7.40654917656635,-15.8554707369032,-9.57648980318245E-17));
#28243=CARTESIAN_POINT('Ctrl Pts',(7.45547662735319,-15.8325185186142,0.00571187761951924));
#28244=CARTESIAN_POINT('Ctrl Pts',(7.58311255681024,-15.771945196048,0.0353494158279854));
#28245=CARTESIAN_POINT('Ctrl Pts',(7.66048059708591,-15.7344445945251,0.0693026530250574));
#28246=CARTESIAN_POINT('Ctrl Pts',(7.73596042367391,-15.6972924318009,0.123164970119317));
#28247=CARTESIAN_POINT('Ctrl Pts',(7.74353659553707,-15.6935563226023,0.128845583461468));
#28248=CARTESIAN_POINT('Ctrl Pts',(7.75098709974897,-15.6898756840048,0.134720657333169));
#28249=CARTESIAN_POINT('',(7.75098748126849,-15.6898754955296,98.476464169983));
#28250=CARTESIAN_POINT('',(7.75098709974897,-15.6898756840048,0.));
#28251=CARTESIAN_POINT('',(7.62166407822415,-15.7531022199328,98.5000002325512));
#28252=CARTESIAN_POINT('Ctrl Pts',(7.75098827006064,-15.6898751058567,98.4764666117908));
#28253=CARTESIAN_POINT('Ctrl Pts',(7.7303651955325,-15.7000631543709,98.4847544570796));
#28254=CARTESIAN_POINT('Ctrl Pts',(7.70899812928377,-15.7105675084655,98.4906432907328));
#28255=CARTESIAN_POINT('Ctrl Pts',(7.66563449409477,-15.7317713310212,98.4982621653014));
#28256=CARTESIAN_POINT('Ctrl Pts',(7.64364124698376,-15.7424694536168,98.5000001531238));
#28257=CARTESIAN_POINT('Ctrl Pts',(7.62166492311255,-15.7531020373702,98.5000000867633));
#28258=CARTESIAN_POINT('',(3.09338542091476,-17.2244295086968,98.5000006225421));
#28259=CARTESIAN_POINT('Origin',(0.,0.,98.5));
#28260=CARTESIAN_POINT('Ctrl Pts',(3.09338528775829,-17.2244293798512,98.5000011593602));
#28261=CARTESIAN_POINT('Ctrl Pts',(3.06935680199565,-17.228744725382,98.5000018789964));
#28262=CARTESIAN_POINT('Ctrl Pts',(3.04527498726416,-17.2330171964727,98.4982647459742));
#28263=CARTESIAN_POINT('Ctrl Pts',(2.99772878170086,-17.241351622266,98.4906474053965));
#28264=CARTESIAN_POINT('Ctrl Pts',(2.97426775127848,-17.2454127370105,98.4847593539945));
#28265=CARTESIAN_POINT('Ctrl Pts',(2.95159454990794,-17.249292438038,98.4764721130871));
#28266=CARTESIAN_POINT('Origin',(0.,0.,0.));
#28267=CARTESIAN_POINT('',(-7.7509870154707,-15.6898756108788,98.4764611650906));
#28268=CARTESIAN_POINT('',(-7.75098709974897,-15.6898756840048,0.134720657333168));
#28269=CARTESIAN_POINT('',(-7.75098709974897,-15.6898756840048,0.));
#28270=CARTESIAN_POINT('',(-7.35749486474657,-15.8782010730192,5.26598123633362E-16));
#28271=CARTESIAN_POINT('Ctrl Pts',(-7.75098709974897,-15.6898756840048,
0.134720657333169));
#28272=CARTESIAN_POINT('Ctrl Pts',(-7.697365011278,-15.716365639972,0.0924371122250959));
#28273=CARTESIAN_POINT('Ctrl Pts',(-7.6352513765003,-15.7466976482487,0.0586496504523847));
#28274=CARTESIAN_POINT('Ctrl Pts',(-7.50029890429085,-15.8114252069992,
0.0120815387590078));
#28275=CARTESIAN_POINT('Ctrl Pts',(-7.42882654248637,-15.8451480558511,
1.30690686544886E-16));
#28276=CARTESIAN_POINT('Ctrl Pts',(-7.35749486474657,-15.8782010730192,
4.16333634234434E-16));
#28277=CARTESIAN_POINT('',(-3.38063404204883,-17.1703614834907,5.26598123633362E-16));
#28278=CARTESIAN_POINT('Origin',(0.,0.,5.26598123633362E-16));
#28279=CARTESIAN_POINT('',(-2.95159725048241,-17.2492919759318,0.134720657333156));
#28280=CARTESIAN_POINT('Ctrl Pts',(-3.38063404204883,-17.1703614834907,
4.22838847269347E-16));
#28281=CARTESIAN_POINT('Ctrl Pts',(-3.32758771379059,-17.180805656334,1.88689696034983E-16));
#28282=CARTESIAN_POINT('Ctrl Pts',(-3.27451359919498,-17.1909957556844,
0.00571187761951954));
#28283=CARTESIAN_POINT('Ctrl Pts',(-3.13564985748461,-17.2170134253201,
0.0353494158279846));
#28284=CARTESIAN_POINT('Ctrl Pts',(-3.05101549755282,-17.2321505944616,
0.0693026530250558));
#28285=CARTESIAN_POINT('Ctrl Pts',(-2.96811354177061,-17.2464597923539,
0.123164970119312));
#28286=CARTESIAN_POINT('Ctrl Pts',(-2.95978826009315,-17.2478903786094,
0.128845583461462));
#28287=CARTESIAN_POINT('Ctrl Pts',(-2.95159725048241,-17.2492919759318,
0.134720657333158));
#28288=CARTESIAN_POINT('',(-2.95159683426415,-17.2492920471526,98.4764641502857));
#28289=CARTESIAN_POINT('',(-2.95159725048241,-17.2492919759318,0.));
#28290=CARTESIAN_POINT('',(-3.09338455449681,-17.2244295302922,98.5000000582797));
#28291=CARTESIAN_POINT('Ctrl Pts',(-2.95159597373243,-17.2492921944017,
98.4764665733303));
#28292=CARTESIAN_POINT('Ctrl Pts',(-2.9742687703255,-17.245412560711,98.4847544660919));
#28293=CARTESIAN_POINT('Ctrl Pts',(-2.99772938956436,-17.2413515161255,
98.4906433246676));
#28294=CARTESIAN_POINT('Ctrl Pts',(-3.04527460155157,-17.2330172636463,
98.4982622140882));
#28295=CARTESIAN_POINT('Ctrl Pts',(-3.06935553227692,-17.2287449523538,
98.5000001907974));
#28296=CARTESIAN_POINT('Ctrl Pts',(-3.09338455123441,-17.2244295121256,
98.5000001151055));
#28297=CARTESIAN_POINT('',(-7.62166294207788,-15.7531030650529,98.5000002711098));
#28298=CARTESIAN_POINT('Origin',(0.,0.,98.5));
#28299=CARTESIAN_POINT('Ctrl Pts',(-7.62166291493897,-15.7531030089644,
98.5000005001312));
#28300=CARTESIAN_POINT('Ctrl Pts',(-7.64364355112194,-15.7424683422865,
98.5000007104308));
#28301=CARTESIAN_POINT('Ctrl Pts',(-7.66563431697665,-15.7317714169945,
98.4982623363923));
#28302=CARTESIAN_POINT('Ctrl Pts',(-7.70900073858256,-15.7105662332996,
98.4906410122901));
#28303=CARTESIAN_POINT('Ctrl Pts',(-7.73036164225108,-15.7000649076559,
98.4847522013256));
#28304=CARTESIAN_POINT('Ctrl Pts',(-7.75098699878812,-15.6898757338807,
98.4764609724326));
#28305=CARTESIAN_POINT('Origin',(0.,0.,0.));
#28306=CARTESIAN_POINT('',(-15.4929577055453,-8.137460149758,98.4764611351388));
#28307=CARTESIAN_POINT('',(-15.4929578242382,-8.13746016004849,0.134720657333155));
#28308=CARTESIAN_POINT('',(-15.4929578242382,-8.13746016004849,0.));
#28309=CARTESIAN_POINT('',(-15.2853108052616,-8.52110753285942,5.26598123633362E-16));
#28310=CARTESIAN_POINT('Ctrl Pts',(-15.4929578242382,-8.13746016004849,
0.134720657333155));
#28311=CARTESIAN_POINT('Ctrl Pts',(-15.4651470488427,-8.19040925740653,
0.0924371122251127));
#28312=CARTESIAN_POINT('Ctrl Pts',(-15.4327247698626,-8.25145784606452,
0.0586496504523958));
#28313=CARTESIAN_POINT('Ctrl Pts',(-15.3615918308627,-8.38314661402319,
0.0120815387590066));
#28314=CARTESIAN_POINT('Ctrl Pts',(-15.3235912687552,-8.45243937205836,
6.02511903288972E-17));
#28315=CARTESIAN_POINT('Ctrl Pts',(-15.2853108052616,-8.52110753285941,
4.16333634234434E-16));
#28316=CARTESIAN_POINT('',(-12.8274756483065,-11.9040274063908,5.26598123633362E-16));
#28317=CARTESIAN_POINT('Origin',(0.,0.,5.26598123633362E-16));
#28318=CARTESIAN_POINT('',(-12.5267717721302,-12.2200650149237,0.13472065733317));
#28319=CARTESIAN_POINT('Ctrl Pts',(-12.8274756483065,-11.9040274063908,
4.28259858131774E-16));
#28320=CARTESIAN_POINT('Ctrl Pts',(-12.7906991980261,-11.9436567691517,
-2.49978313375409E-16));
#28321=CARTESIAN_POINT('Ctrl Pts',(-12.7537509274744,-11.9830969145383,
0.00571187761951878));
#28322=CARTESIAN_POINT('Ctrl Pts',(-12.6567006030391,-12.0857677108831,
0.0353494158279818));
#28323=CARTESIAN_POINT('Ctrl Pts',(-12.597127372329,-12.1477607665704,0.0693026530250494));
#28324=CARTESIAN_POINT('Ctrl Pts',(-12.5384690167276,-12.2080656978362,
0.123164970119316));
#28325=CARTESIAN_POINT('Ctrl Pts',(-12.5325745998707,-12.21411654422,0.128845583461468));
#28326=CARTESIAN_POINT('Ctrl Pts',(-12.5267717721302,-12.2200650149237,
0.134720657333169));
#28327=CARTESIAN_POINT('',(-12.5267714753738,-12.2200653191283,98.4764641666045));
#28328=CARTESIAN_POINT('',(-12.5267717721302,-12.2200650149237,0.));
#28329=CARTESIAN_POINT('',(-12.6268663170877,-12.1166104030897,98.5000000583843));
#28330=CARTESIAN_POINT('Ctrl Pts',(-12.5267708618295,-12.2200659480716,
98.4764666051942));
#28331=CARTESIAN_POINT('Ctrl Pts',(-12.5428331499379,-12.2036005211659,
98.4847544881405));
#28332=CARTESIAN_POINT('Ctrl Pts',(-12.5594261690095,-12.1865252595175,
98.4906433390831));
#28333=CARTESIAN_POINT('Ctrl Pts',(-12.5929923076292,-12.1518363282392,
98.4982622190212));
#28334=CARTESIAN_POINT('Ctrl Pts',(-12.6099629957876,-12.1342255319367,
98.5000001912344));
#28335=CARTESIAN_POINT('Ctrl Pts',(-12.6268663036907,-12.1166103902338,
98.500000115428));
#28336=CARTESIAN_POINT('',(-15.4254964602665,-8.26462701674582,98.5000002246579));
#28337=CARTESIAN_POINT('Origin',(0.,0.,98.5));
#28338=CARTESIAN_POINT('Ctrl Pts',(-15.4254964408324,-8.26462700633653,
98.5000005203777));
#28339=CARTESIAN_POINT('Ctrl Pts',(-15.4370282602939,-8.2431034651139,98.5000007416218));
#28340=CARTESIAN_POINT('Ctrl Pts',(-15.448531655215,-8.2215236481436,98.4982623777968));
#28341=CARTESIAN_POINT('Ctrl Pts',(-15.4711517457392,-8.17887812715025,
98.4906410339747));
#28342=CARTESIAN_POINT('Ctrl Pts',(-15.4822605547265,-8.15782675347622,
98.4847521990827));
#28343=CARTESIAN_POINT('Ctrl Pts',(-15.4929577683353,-8.13746026648238,
98.47646092943));
#28344=CARTESIAN_POINT('Origin',(0.,0.,0.));
#28345=CARTESIAN_POINT('',(-17.3171451173558,2.52318944679938,98.4764669873977));
#28346=CARTESIAN_POINT('',(-17.3171452461371,2.52318856294819,0.134720657333157));
#28347=CARTESIAN_POINT('',(-17.3171452461371,2.52318856294819,0.));
#28348=CARTESIAN_POINT('',(-17.3746575467727,2.0907594630599,5.26598123633362E-16));
#28349=CARTESIAN_POINT('Ctrl Pts',(-17.3171452461371,2.52318856294819,0.134720657333156));
#28350=CARTESIAN_POINT('Ctrl Pts',(-17.3257685547646,2.46400507971636,0.0924371122250624));
#28351=CARTESIAN_POINT('Ctrl Pts',(-17.3354218401598,2.39555839657922,0.0586496504523668));
#28352=CARTESIAN_POINT('Ctrl Pts',(-17.3552787993477,2.24720905283605,0.0120815387590083));
#28353=CARTESIAN_POINT('Ctrl Pts',(-17.3652649600707,2.1688138640129,1.30690686544881E-16));
#28354=CARTESIAN_POINT('Ctrl Pts',(-17.3746575467727,2.0907594630599,4.16333634234434E-16));
#28355=CARTESIAN_POINT('',(-17.3746575467727,-2.0907594630599,5.26598123633362E-16));
#28356=CARTESIAN_POINT('Origin',(0.,0.,5.26598123633362E-16));
#28357=CARTESIAN_POINT('',(-17.3171452461371,-2.52318856294818,0.134720657333156));
#28358=CARTESIAN_POINT('Ctrl Pts',(-17.3746575467727,-2.0907594630599,4.36933475511658E-16));
#28359=CARTESIAN_POINT('Ctrl Pts',(-17.3681983284916,-2.14443694611619,
2.29452361695802E-16));
#28360=CARTESIAN_POINT('Ctrl Pts',(-17.3614888855091,-2.1980623425226,0.00571187761951909));
#28361=CARTESIAN_POINT('Ctrl Pts',(-17.3433219036639,-2.33816951102481,
0.0353494158279826));
#28362=CARTESIAN_POINT('Ctrl Pts',(-17.3315647514872,-2.42333921305186,
0.0693026530250511));
#28363=CARTESIAN_POINT('Ctrl Pts',(-17.3195554941821,-2.50660544363677,
0.123164970119312));
#28364=CARTESIAN_POINT('Ctrl Pts',(-17.3183434090412,-2.51496533249098,
0.128845583461461));
#28365=CARTESIAN_POINT('Ctrl Pts',(-17.3171452461371,-2.52318856294818,
0.134720657333157));
#28366=CARTESIAN_POINT('',(-17.3171451847825,-2.5231889840369,98.4764641699832));
#28367=CARTESIAN_POINT('',(-17.3171452461371,-2.52318856294818,0.));
#28368=CARTESIAN_POINT('',(-17.3373142437191,-2.38065698652274,98.5000002325512));
#28369=CARTESIAN_POINT('Ctrl Pts',(-17.3171450579317,-2.52318985463842,
98.4764666117912));
#28370=CARTESIAN_POINT('Ctrl Pts',(-17.3204615873541,-2.50042786509184,
98.48475445708));
#28371=CARTESIAN_POINT('Ctrl Pts',(-17.3238490351745,-2.47686055357152,
98.4906432907331));
#28372=CARTESIAN_POINT('Ctrl Pts',(-17.330614968575,-2.42906694423984,98.4982621653015));
#28373=CARTESIAN_POINT('Ctrl Pts',(-17.3339932006628,-2.40484422157081,
98.5000001531238));
#28374=CARTESIAN_POINT('Ctrl Pts',(-17.3373143311766,-2.38065784647426,
98.5000000867633));
#28375=CARTESIAN_POINT('',(-17.337314588927,2.38065707462717,98.5000006225421));
#28376=CARTESIAN_POINT('Origin',(0.,0.,98.5));
#28377=CARTESIAN_POINT('Ctrl Pts',(-17.3373144252399,2.38065716145103,98.5000011593602));
#28378=CARTESIAN_POINT('Ctrl Pts',(-17.3339933522773,2.4048431245179,98.5000018789964));
#28379=CARTESIAN_POINT('Ctrl Pts',(-17.3306150237413,2.42906655751751,98.4982647459742));
#28380=CARTESIAN_POINT('Ctrl Pts',(-17.3238489481646,2.47686116535221,98.4906474053964));
#28381=CARTESIAN_POINT('Ctrl Pts',(-17.3204614406997,2.50042888468654,98.4847593539945));
#28382=CARTESIAN_POINT('Ctrl Pts',(-17.3171448511027,2.5231912741458,98.476472113087));
#28383=CARTESIAN_POINT('Origin',(0.,17.5,2.63299061816681E-16));
#28384=CARTESIAN_POINT('Origin',(12.2482946431511,16.8583313034371,2.16840434497101E-16));
#28385=CARTESIAN_POINT('Origin',(19.8181570368417,6.43930956430664,2.16840434497101E-16));
#28386=CARTESIAN_POINT('Origin',(19.8181570368417,-6.43930956430665,2.16840434497101E-16));
#28387=CARTESIAN_POINT('Origin',(12.2482946431511,-16.8583313034371,2.16840434497101E-16));
#28388=CARTESIAN_POINT('Origin',(-2.55192432461455E-15,-20.8380434782609,
2.16840434497101E-16));
#28389=CARTESIAN_POINT('Origin',(-12.2482946431511,-16.8583313034371,2.16840434497101E-16));
#28390=CARTESIAN_POINT('Origin',(-19.8181570368417,-6.43930956430665,2.16840434497101E-16));
#28391=CARTESIAN_POINT('',(-15.2853108052616,8.52110753285942,5.26598123633362E-16));
#28392=CARTESIAN_POINT('Origin',(-19.8181570368417,6.43930956430665,2.16840434497101E-16));
#28393=CARTESIAN_POINT('',(-12.8274756483065,11.9040274063908,5.26598123633362E-16));
#28394=CARTESIAN_POINT('Origin',(0.,0.,5.26598123633362E-16));
#28395=CARTESIAN_POINT('Origin',(-12.2482946431511,16.8583313034371,2.16840434497101E-16));
#28396=CARTESIAN_POINT('Origin',(0.,20.8380434782609,2.16840434497101E-16));
#28397=CARTESIAN_POINT('',(15.,-1.83697019872103E-15,0.));
#28398=CARTESIAN_POINT('Origin',(0.,0.,0.));
#28399=CARTESIAN_POINT('Origin',(0.,0.,0.));
#28400=CARTESIAN_POINT('',(14.,0.,30.9));
#28401=CARTESIAN_POINT('Origin',(0.,0.,30.9));
#28402=CARTESIAN_POINT('',(14.,-1.71450551880629E-15,3.24999999999998));
#28403=CARTESIAN_POINT('',(14.,-1.71450551880629E-15,0.));
#28404=CARTESIAN_POINT('Origin',(0.,0.,3.24999999999998));
#28405=CARTESIAN_POINT('Origin',(0.,0.,0.));
#28406=CARTESIAN_POINT('',(14.,-1.71450551880629E-15,42.));
#28407=CARTESIAN_POINT('Origin',(0.,0.,42.));
#28408=CARTESIAN_POINT('',(14.,0.,32.8));
#28409=CARTESIAN_POINT('',(14.,-1.71450551880629E-15,0.));
#28410=CARTESIAN_POINT('Origin',(0.,0.,32.8));
#28411=CARTESIAN_POINT('Origin',(0.,0.,0.));
#28412=CARTESIAN_POINT('',(-12.5267717256653,12.22006490522,98.476461135139));
#28413=CARTESIAN_POINT('',(-12.5267717721302,12.2200650149237,0.134720657333155));
#28414=CARTESIAN_POINT('',(-12.5267717721302,12.2200650149237,0.));
#28415=CARTESIAN_POINT('Ctrl Pts',(-12.5267717721302,12.2200650149237,0.134720657333157));
#28416=CARTESIAN_POINT('Ctrl Pts',(-12.5685353539806,12.1772532248401,0.0924371122250874));
#28417=CARTESIAN_POINT('Ctrl Pts',(-12.6165769768332,12.127552753765,0.0586496504523806));
#28418=CARTESIAN_POINT('Ctrl Pts',(-12.7198391507123,12.0192072413384,0.0120815387590078));
#28419=CARTESIAN_POINT('Ctrl Pts',(-12.7739976602867,11.9616539193032,2.01130182760891E-16));
#28420=CARTESIAN_POINT('Ctrl Pts',(-12.8274756483065,11.9040274063908,4.16333634234434E-16));
#28421=CARTESIAN_POINT('',(-15.4929578242382,8.13746016004849,0.134720657333156));
#28422=CARTESIAN_POINT('Ctrl Pts',(-15.2853108052616,8.52110753285942,5.65953534037433E-16));
#28423=CARTESIAN_POINT('Ctrl Pts',(-15.3116360208225,8.47388490360466,3.69631386233599E-16));
#28424=CARTESIAN_POINT('Ctrl Pts',(-15.3377281845829,8.42655733494556,0.00571187761951948));
#28425=CARTESIAN_POINT('Ctrl Pts',(-15.4053837149197,8.30252997058624,0.0353494158279853));
#28426=CARTESIAN_POINT('Ctrl Pts',(-15.4459334737969,8.22671555358209,0.0693026530250567));
#28427=CARTESIAN_POINT('Ctrl Pts',(-15.485160442899,8.15229289364641,0.123164970119313));
#28428=CARTESIAN_POINT('Ctrl Pts',(-15.4890936648008,8.14481715572194,0.12884558346146));
#28429=CARTESIAN_POINT('Ctrl Pts',(-15.4929578242382,8.13746016004849,0.134720657333156));
#28430=CARTESIAN_POINT('',(-15.4929580205917,8.13745978620983,98.4764641502858));
#28431=CARTESIAN_POINT('',(-15.4929578242382,8.13746016004849,0.));
#28432=CARTESIAN_POINT('',(-15.4254975467744,8.26462498123528,98.5000000582797));
#28433=CARTESIAN_POINT('Ctrl Pts',(-15.4929584265529,8.13745901329798,98.4764665733304));
#28434=CARTESIAN_POINT('Ctrl Pts',(-15.4822623961932,8.15782325149825,98.4847544660921));
#28435=CARTESIAN_POINT('Ctrl Pts',(-15.4711503832337,8.17888069451006,98.4906433246677));
#28436=CARTESIAN_POINT('Ctrl Pts',(-15.4485317595999,8.22152345253713,98.4982622140882));
#28437=CARTESIAN_POINT('Ctrl Pts',(-15.4370271332712,8.24310556182703,98.5000001907974));
#28438=CARTESIAN_POINT('Ctrl Pts',(-15.4254975305051,8.26462497251878,98.5000001151055));
#28439=CARTESIAN_POINT('',(-12.626867931918,12.1166087252795,98.5000002246578));
#28440=CARTESIAN_POINT('Origin',(0.,0.,98.5));
#28441=CARTESIAN_POINT('Ctrl Pts',(-12.6268679160127,12.1166087100132,98.5000005203777));
#28442=CARTESIAN_POINT('Ctrl Pts',(-12.6099613400685,12.1342272620742,98.5000007416218));
#28443=CARTESIAN_POINT('Ctrl Pts',(-12.5929924590423,12.1518361709525,98.4982623777967));
#28444=CARTESIAN_POINT('Ctrl Pts',(-12.5594241507976,12.1865273461651,98.4906410339749));
#28445=CARTESIAN_POINT('Ctrl Pts',(-12.542835915452,12.2035976835611,98.484752199083));
#28446=CARTESIAN_POINT('Ctrl Pts',(-12.5267718560799,12.220064928867,98.4764609294303));
#28447=CARTESIAN_POINT('Origin',(0.,12.35,184.));
#28448=CARTESIAN_POINT('',(12.35,0.,184.));
#28449=CARTESIAN_POINT('Origin',(0.,0.,184.));
#28450=CARTESIAN_POINT('',(-11.35,-1.38997411703225E-15,184.));
#28451=CARTESIAN_POINT('Origin',(0.,0.,184.));
#28452=CARTESIAN_POINT('Origin',(0.,0.,161.));
#28453=CARTESIAN_POINT('',(13.,0.,161.));
#28454=CARTESIAN_POINT('',(-13.,-1.59204083889156E-15,161.));
#28455=CARTESIAN_POINT('Origin',(0.,0.,161.));
#28456=CARTESIAN_POINT('Origin',(0.,0.,161.));
#28457=CARTESIAN_POINT('',(13.,-1.59204083889156E-15,161.));
#28458=CARTESIAN_POINT('Origin',(0.,0.,0.));
#28459=CARTESIAN_POINT('',(-13.,-1.59204083889156E-15,111.));
#28460=CARTESIAN_POINT('',(-13.,-1.59204083889156E-15,0.));
#28461=CARTESIAN_POINT('Origin',(0.,0.,111.));
#28462=CARTESIAN_POINT('',(9.07821927770119,9.30515635258077,125.));
#28463=CARTESIAN_POINT('',(6.04440554879513,11.5093510486775,125.));
#28464=CARTESIAN_POINT('Ctrl Pts',(9.07821927770119,9.30515635258078,125.));
#28465=CARTESIAN_POINT('Ctrl Pts',(9.07821927770119,9.30515635258078,125.235784463582));
#28466=CARTESIAN_POINT('Ctrl Pts',(9.04424645795556,9.33867951762762,125.487056987681));
#28467=CARTESIAN_POINT('Ctrl Pts',(8.90448693202246,9.47203470845874,125.948918874434));
#28468=CARTESIAN_POINT('Ctrl Pts',(8.79848999736503,9.57154722295921,126.15953679602));
#28469=CARTESIAN_POINT('Ctrl Pts',(8.54947275134611,9.79461368903714,126.492111158983));
#28470=CARTESIAN_POINT('Ctrl Pts',(8.38972960894075,9.9330725460095,126.636358409655));
#28471=CARTESIAN_POINT('Ctrl Pts',(8.03108912785565,10.2252188501698,126.827811869943));
#28472=CARTESIAN_POINT('Ctrl Pts',(7.83195907934858,10.3786323587528,126.875));
#28473=CARTESIAN_POINT('Ctrl Pts',(7.45045748025558,10.6558094949959,126.875));
#28474=CARTESIAN_POINT('Ctrl Pts',(7.24301799415061,10.7977860438999,126.827811869943));
#28475=CARTESIAN_POINT('Ctrl Pts',(6.85434434434132,11.0485952376137,126.636358409655));
#28476=CARTESIAN_POINT('Ctrl Pts',(6.67329880044087,11.1577338543056,126.492111158983));
#28477=CARTESIAN_POINT('Ctrl Pts',(6.38419942339823,11.3256319999085,126.15953679602));
#28478=CARTESIAN_POINT('Ctrl Pts',(6.25680254386883,11.3956900171882,125.948918874434));
#28479=CARTESIAN_POINT('Ctrl Pts',(6.08678615200799,11.4874002047862,125.487056987681));
#28480=CARTESIAN_POINT('Ctrl Pts',(6.04440554879513,11.5093510486775,125.235784463582));
#28481=CARTESIAN_POINT('Ctrl Pts',(6.04440554879513,11.5093510486775,125.));
#28482=CARTESIAN_POINT('Ctrl Pts',(6.04440554879513,11.5093510486775,125.));
#28483=CARTESIAN_POINT('Ctrl Pts',(6.04440554879513,11.5093510486775,124.764215536418));
#28484=CARTESIAN_POINT('Ctrl Pts',(6.08678615200799,11.4874002047862,124.512943012319));
#28485=CARTESIAN_POINT('Ctrl Pts',(6.25680254386884,11.3956900171882,124.051081125566));
#28486=CARTESIAN_POINT('Ctrl Pts',(6.38419942339822,11.3256319999086,123.84046320398));
#28487=CARTESIAN_POINT('Ctrl Pts',(6.67329880044087,11.1577338543056,123.507888841017));
#28488=CARTESIAN_POINT('Ctrl Pts',(6.85434434434132,11.0485952376137,123.363641590345));
#28489=CARTESIAN_POINT('Ctrl Pts',(7.24301799415061,10.7977860438999,123.172188130057));
#28490=CARTESIAN_POINT('Ctrl Pts',(7.45045748025558,10.6558094949959,123.125));
#28491=CARTESIAN_POINT('Ctrl Pts',(7.83195907934858,10.3786323587528,123.125));
#28492=CARTESIAN_POINT('Ctrl Pts',(8.03108912785565,10.2252188501698,123.172188130057));
#28493=CARTESIAN_POINT('Ctrl Pts',(8.38972960894075,9.9330725460095,123.363641590345));
#28494=CARTESIAN_POINT('Ctrl Pts',(8.54947275134611,9.79461368903714,123.507888841017));
#28495=CARTESIAN_POINT('Ctrl Pts',(8.79848999736503,9.57154722295921,123.84046320398));
#28496=CARTESIAN_POINT('Ctrl Pts',(8.90448693202246,9.47203470845874,124.051081125566));
#28497=CARTESIAN_POINT('Ctrl Pts',(9.04424645795556,9.33867951762761,124.512943012319));
#28498=CARTESIAN_POINT('Ctrl Pts',(9.07821927770119,9.30515635258078,124.764215536418));
#28499=CARTESIAN_POINT('Ctrl Pts',(9.07821927770119,9.30515635258078,125.));
#28500=CARTESIAN_POINT('',(-6.04440554879529,11.5093510486774,125.));
#28501=CARTESIAN_POINT('',(-9.07821927770133,9.30515635258063,125.));
#28502=CARTESIAN_POINT('Ctrl Pts',(-6.0444055487953,11.5093510486774,125.));
#28503=CARTESIAN_POINT('Ctrl Pts',(-6.0444055487953,11.5093510486774,125.235784463582));
#28504=CARTESIAN_POINT('Ctrl Pts',(-6.08678615200817,11.4874002047861,125.487056987681));
#28505=CARTESIAN_POINT('Ctrl Pts',(-6.256802543869,11.3956900171881,125.948918874434));
#28506=CARTESIAN_POINT('Ctrl Pts',(-6.3841994233984,11.3256319999085,126.15953679602));
#28507=CARTESIAN_POINT('Ctrl Pts',(-6.67329880044104,11.1577338543055,126.492111158983));
#28508=CARTESIAN_POINT('Ctrl Pts',(-6.85434434434149,11.0485952376136,126.636358409655));
#28509=CARTESIAN_POINT('Ctrl Pts',(-7.24301799415078,10.7977860438998,126.827811869943));
#28510=CARTESIAN_POINT('Ctrl Pts',(-7.45045748025575,10.6558094949958,126.875));
#28511=CARTESIAN_POINT('Ctrl Pts',(-7.83195907934875,10.3786323587527,126.875));
#28512=CARTESIAN_POINT('Ctrl Pts',(-8.0310891278558,10.2252188501697,126.827811869943));
#28513=CARTESIAN_POINT('Ctrl Pts',(-8.3897296089409,9.93307254600937,126.636358409655));
#28514=CARTESIAN_POINT('Ctrl Pts',(-8.54947275134627,9.79461368903702,126.492111158983));
#28515=CARTESIAN_POINT('Ctrl Pts',(-8.79848999736518,9.57154722295908,126.15953679602));
#28516=CARTESIAN_POINT('Ctrl Pts',(-8.90448693202262,9.47203470845859,125.948918874434));
#28517=CARTESIAN_POINT('Ctrl Pts',(-9.04424645795571,9.33867951762747,125.487056987681));
#28518=CARTESIAN_POINT('Ctrl Pts',(-9.07821927770133,9.30515635258063,125.235784463582));
#28519=CARTESIAN_POINT('Ctrl Pts',(-9.07821927770133,9.30515635258063,125.));
#28520=CARTESIAN_POINT('Ctrl Pts',(-9.07821927770134,9.30515635258063,125.));
#28521=CARTESIAN_POINT('Ctrl Pts',(-9.07821927770134,9.30515635258063,124.764215536418));
#28522=CARTESIAN_POINT('Ctrl Pts',(-9.04424645795572,9.33867951762747,124.512943012319));
#28523=CARTESIAN_POINT('Ctrl Pts',(-8.90448693202261,9.4720347084586,124.051081125566));
#28524=CARTESIAN_POINT('Ctrl Pts',(-8.79848999736518,9.57154722295908,123.84046320398));
#28525=CARTESIAN_POINT('Ctrl Pts',(-8.54947275134627,9.79461368903702,123.507888841017));
#28526=CARTESIAN_POINT('Ctrl Pts',(-8.3897296089409,9.93307254600937,123.363641590345));
#28527=CARTESIAN_POINT('Ctrl Pts',(-8.0310891278558,10.2252188501697,123.172188130057));
#28528=CARTESIAN_POINT('Ctrl Pts',(-7.83195907934875,10.3786323587527,123.125));
#28529=CARTESIAN_POINT('Ctrl Pts',(-7.45045748025575,10.6558094949958,123.125));
#28530=CARTESIAN_POINT('Ctrl Pts',(-7.24301799415078,10.7977860438998,123.172188130057));
#28531=CARTESIAN_POINT('Ctrl Pts',(-6.85434434434149,11.0485952376136,123.363641590345));
#28532=CARTESIAN_POINT('Ctrl Pts',(-6.67329880044104,11.1577338543055,123.507888841017));
#28533=CARTESIAN_POINT('Ctrl Pts',(-6.3841994233984,11.3256319999085,123.84046320398));
#28534=CARTESIAN_POINT('Ctrl Pts',(-6.25680254386901,11.3956900171881,124.051081125566));
#28535=CARTESIAN_POINT('Ctrl Pts',(-6.08678615200816,11.4874002047862,124.512943012319));
#28536=CARTESIAN_POINT('Ctrl Pts',(-6.0444055487953,11.5093510486774,124.764215536418));
#28537=CARTESIAN_POINT('Ctrl Pts',(-6.0444055487953,11.5093510486774,125.));
#28538=CARTESIAN_POINT('',(-12.8138673486451,-2.19198621604393,125.));
#28539=CARTESIAN_POINT('',(-11.655053619739,-5.75844815215074,125.));
#28540=CARTESIAN_POINT('Ctrl Pts',(-12.8138673486451,-2.19198621604393,
125.));
#28541=CARTESIAN_POINT('Ctrl Pts',(-12.8138673486451,-2.19198621604393,
125.235784463582));
#28542=CARTESIAN_POINT('Ctrl Pts',(-12.8060871821488,-2.23907574869732,
125.487056987681));
#28543=CARTESIAN_POINT('Ctrl Pts',(-12.7714035650303,-2.42911095257868,
125.948918874434));
#28544=CARTESIAN_POINT('Ctrl Pts',(-12.7441422319827,-2.5719217029424,126.15953679602));
#28545=CARTESIAN_POINT('Ctrl Pts',(-12.6737982271025,-2.89875492965101,
126.492111158983));
#28546=CARTESIAN_POINT('Ctrl Pts',(-12.6259473843394,-3.1046651612241,126.636358409655));
#28547=CARTESIAN_POINT('Ctrl Pts',(-12.5075204293679,-3.55182007179051,
126.827811869943));
#28548=CARTESIAN_POINT('Ctrl Pts',(-12.4365950338825,-3.79297991320159,
126.875));
#28549=CARTESIAN_POINT('Ctrl Pts',(-12.2908743897914,-4.24146194054731,
126.875));
#28550=CARTESIAN_POINT('Ctrl Pts',(-12.2065040418452,-4.47825325208896,
126.827811869943));
#28551=CARTESIAN_POINT('Ctrl Pts',(-12.0394823990881,-4.90961879146154,
126.636358409655));
#28552=CARTESIAN_POINT('Ctrl Pts',(-11.9571635466639,-5.10432968780581,
126.492111158983));
#28553=CARTESIAN_POINT('Ctrl Pts',(-11.8219652914458,-5.41009049119521,
126.15953679602));
#28554=CARTESIAN_POINT('Ctrl Pts',(-11.760078120238,-5.54165062474212,125.948918874434));
#28555=CARTESIAN_POINT('Ctrl Pts',(-11.6764378656554,-5.71577885285004,
125.487056987681));
#28556=CARTESIAN_POINT('Ctrl Pts',(-11.655053619739,-5.75844815215074,125.235784463582));
#28557=CARTESIAN_POINT('Ctrl Pts',(-11.655053619739,-5.75844815215074,125.));
#28558=CARTESIAN_POINT('Ctrl Pts',(-11.655053619739,-5.75844815215074,125.));
#28559=CARTESIAN_POINT('Ctrl Pts',(-11.655053619739,-5.75844815215074,124.764215536418));
#28560=CARTESIAN_POINT('Ctrl Pts',(-11.6764378656554,-5.71577885285004,
124.512943012319));
#28561=CARTESIAN_POINT('Ctrl Pts',(-11.760078120238,-5.54165062474211,124.051081125566));
#28562=CARTESIAN_POINT('Ctrl Pts',(-11.8219652914458,-5.41009049119521,
123.84046320398));
#28563=CARTESIAN_POINT('Ctrl Pts',(-11.9571635466639,-5.10432968780581,
123.507888841017));
#28564=CARTESIAN_POINT('Ctrl Pts',(-12.0394823990881,-4.90961879146154,
123.363641590345));
#28565=CARTESIAN_POINT('Ctrl Pts',(-12.2065040418452,-4.47825325208896,
123.172188130057));
#28566=CARTESIAN_POINT('Ctrl Pts',(-12.2908743897914,-4.24146194054731,
123.125));
#28567=CARTESIAN_POINT('Ctrl Pts',(-12.4365950338825,-3.79297991320159,
123.125));
#28568=CARTESIAN_POINT('Ctrl Pts',(-12.5075204293679,-3.55182007179051,
123.172188130057));
#28569=CARTESIAN_POINT('Ctrl Pts',(-12.6259473843394,-3.10466516122411,
123.363641590345));
#28570=CARTESIAN_POINT('Ctrl Pts',(-12.6737982271025,-2.89875492965101,
123.507888841017));
#28571=CARTESIAN_POINT('Ctrl Pts',(-12.7441422319827,-2.57192170294239,
123.84046320398));
#28572=CARTESIAN_POINT('Ctrl Pts',(-12.7714035650303,-2.42911095257869,
124.051081125566));
#28573=CARTESIAN_POINT('Ctrl Pts',(-12.8060871821488,-2.23907574869732,
124.512943012319));
#28574=CARTESIAN_POINT('Ctrl Pts',(-12.8138673486451,-2.19198621604393,
124.764215536418));
#28575=CARTESIAN_POINT('Ctrl Pts',(-12.8138673486451,-2.19198621604393,
125.));
#28576=CARTESIAN_POINT('',(11.6550536197391,-5.75844815215058,125.));
#28577=CARTESIAN_POINT('',(12.8138673486451,-2.19198621604374,125.));
#28578=CARTESIAN_POINT('Ctrl Pts',(11.6550536197391,-5.75844815215058,125.));
#28579=CARTESIAN_POINT('Ctrl Pts',(11.6550536197391,-5.75844815215058,125.235784463582));
#28580=CARTESIAN_POINT('Ctrl Pts',(11.6764378656555,-5.71577885284987,125.487056987681));
#28581=CARTESIAN_POINT('Ctrl Pts',(11.7600781202381,-5.54165062474193,125.948918874434));
#28582=CARTESIAN_POINT('Ctrl Pts',(11.8219652914459,-5.41009049119505,126.15953679602));
#28583=CARTESIAN_POINT('Ctrl Pts',(11.957163546664,-5.10432968780564,126.492111158983));
#28584=CARTESIAN_POINT('Ctrl Pts',(12.0394823990882,-4.90961879146136,126.636358409655));
#28585=CARTESIAN_POINT('Ctrl Pts',(12.2065040418453,-4.47825325208878,126.827811869943));
#28586=CARTESIAN_POINT('Ctrl Pts',(12.2908743897914,-4.24146194054714,126.875));
#28587=CARTESIAN_POINT('Ctrl Pts',(12.4365950338825,-3.79297991320141,126.875));
#28588=CARTESIAN_POINT('Ctrl Pts',(12.5075204293679,-3.55182007179034,126.827811869943));
#28589=CARTESIAN_POINT('Ctrl Pts',(12.6259473843394,-3.10466516122393,126.636358409655));
#28590=CARTESIAN_POINT('Ctrl Pts',(12.6737982271026,-2.89875492965083,126.492111158983));
#28591=CARTESIAN_POINT('Ctrl Pts',(12.7441422319827,-2.57192170294221,126.15953679602));
#28592=CARTESIAN_POINT('Ctrl Pts',(12.7714035650303,-2.4291109525785,125.948918874434));
#28593=CARTESIAN_POINT('Ctrl Pts',(12.8060871821488,-2.23907574869713,125.487056987681));
#28594=CARTESIAN_POINT('Ctrl Pts',(12.8138673486451,-2.19198621604374,125.235784463582));
#28595=CARTESIAN_POINT('Ctrl Pts',(12.8138673486451,-2.19198621604374,125.));
#28596=CARTESIAN_POINT('Ctrl Pts',(12.8138673486451,-2.19198621604374,125.));
#28597=CARTESIAN_POINT('Ctrl Pts',(12.8138673486451,-2.19198621604374,124.764215536418));
#28598=CARTESIAN_POINT('Ctrl Pts',(12.8060871821488,-2.23907574869713,124.512943012319));
#28599=CARTESIAN_POINT('Ctrl Pts',(12.7714035650303,-2.42911095257849,124.051081125566));
#28600=CARTESIAN_POINT('Ctrl Pts',(12.7441422319827,-2.57192170294221,123.84046320398));
#28601=CARTESIAN_POINT('Ctrl Pts',(12.6737982271026,-2.89875492965083,123.507888841017));
#28602=CARTESIAN_POINT('Ctrl Pts',(12.6259473843394,-3.10466516122393,123.363641590345));
#28603=CARTESIAN_POINT('Ctrl Pts',(12.5075204293679,-3.55182007179033,123.172188130057));
#28604=CARTESIAN_POINT('Ctrl Pts',(12.4365950338825,-3.79297991320141,123.125));
#28605=CARTESIAN_POINT('Ctrl Pts',(12.2908743897914,-4.24146194054714,123.125));
#28606=CARTESIAN_POINT('Ctrl Pts',(12.2065040418453,-4.47825325208879,123.172188130057));
#28607=CARTESIAN_POINT('Ctrl Pts',(12.0394823990882,-4.90961879146136,123.363641590345));
#28608=CARTESIAN_POINT('Ctrl Pts',(11.957163546664,-5.10432968780564,123.507888841017));
#28609=CARTESIAN_POINT('Ctrl Pts',(11.8219652914459,-5.41009049119505,123.84046320398));
#28610=CARTESIAN_POINT('Ctrl Pts',(11.7600781202381,-5.54165062474194,124.051081125566));
#28611=CARTESIAN_POINT('Ctrl Pts',(11.6764378656555,-5.71577885284988,124.512943012319));
#28612=CARTESIAN_POINT('Ctrl Pts',(11.6550536197391,-5.75844815215058,124.764215536418));
#28613=CARTESIAN_POINT('Ctrl Pts',(11.6550536197391,-5.75844815215058,125.));
#28614=CARTESIAN_POINT('',(0.,-13.,126.875));
#28615=CARTESIAN_POINT('',(-2.29621274840127E-16,-13.,123.125));
#28616=CARTESIAN_POINT('Ctrl Pts',(1.38777878078145E-16,-13.,126.875));
#28617=CARTESIAN_POINT('Ctrl Pts',(0.23578095500191,-13.,126.875));
#28618=CARTESIAN_POINT('Ctrl Pts',(0.487054746182364,-12.9929315701904,
126.827811869943));
#28619=CARTESIAN_POINT('Ctrl Pts',(0.948920279348187,-12.9673838309378,
126.636358409655));
#28620=CARTESIAN_POINT('Ctrl Pts',(1.15953927046661,-12.9492629258861,126.492111158983));
#28621=CARTESIAN_POINT('Ctrl Pts',(1.49211363342996,-12.9151670287303,126.15953679602));
#28622=CARTESIAN_POINT('Ctrl Pts',(1.6363589433614,-12.8969631483263,125.948918874434));
#28623=CARTESIAN_POINT('Ctrl Pts',(1.82781098945425,-12.8712251208667,125.487056987681));
#28624=CARTESIAN_POINT('Ctrl Pts',(1.87499999999999,-12.8640730330638,125.235784463582));
#28625=CARTESIAN_POINT('Ctrl Pts',(1.87499999999999,-12.8640730330638,124.764215536418));
#28626=CARTESIAN_POINT('Ctrl Pts',(1.82781098945425,-12.8712251208667,124.512943012319));
#28627=CARTESIAN_POINT('Ctrl Pts',(1.63635894336139,-12.8969631483263,124.051081125566));
#28628=CARTESIAN_POINT('Ctrl Pts',(1.49211363342997,-12.9151670287303,123.84046320398));
#28629=CARTESIAN_POINT('Ctrl Pts',(1.15953927046661,-12.9492629258861,123.507888841017));
#28630=CARTESIAN_POINT('Ctrl Pts',(0.948920279348186,-12.9673838309378,
123.363641590345));
#28631=CARTESIAN_POINT('Ctrl Pts',(0.487054746182362,-12.9929315701904,
123.172188130057));
#28632=CARTESIAN_POINT('Ctrl Pts',(0.235780955001907,-13.,123.125));
#28633=CARTESIAN_POINT('Ctrl Pts',(-1.45716771982052E-15,-13.,123.125));
#28634=CARTESIAN_POINT('Ctrl Pts',(7.63278329429795E-16,-13.,123.125));
#28635=CARTESIAN_POINT('Ctrl Pts',(-0.235780955001908,-13.,123.125));
#28636=CARTESIAN_POINT('Ctrl Pts',(-0.487054746182362,-12.9929315701904,
123.172188130057));
#28637=CARTESIAN_POINT('Ctrl Pts',(-0.948920279348186,-12.9673838309378,
123.363641590345));
#28638=CARTESIAN_POINT('Ctrl Pts',(-1.15953927046661,-12.9492629258861,
123.507888841017));
#28639=CARTESIAN_POINT('Ctrl Pts',(-1.49211363342996,-12.9151670287303,
123.84046320398));
#28640=CARTESIAN_POINT('Ctrl Pts',(-1.63635894336139,-12.8969631483263,
124.051081125566));
#28641=CARTESIAN_POINT('Ctrl Pts',(-1.82781098945425,-12.8712251208667,
124.512943012319));
#28642=CARTESIAN_POINT('Ctrl Pts',(-1.87499999999999,-12.8640730330638,
124.764215536418));
#28643=CARTESIAN_POINT('Ctrl Pts',(-1.87499999999999,-12.8640730330638,
125.));
#28644=CARTESIAN_POINT('Ctrl Pts',(-1.87499999999999,-12.8640730330638,
125.235784463582));
#28645=CARTESIAN_POINT('Ctrl Pts',(-1.82781098945425,-12.8712251208667,
125.487056987681));
#28646=CARTESIAN_POINT('Ctrl Pts',(-1.6363589433614,-12.8969631483263,125.948918874434));
#28647=CARTESIAN_POINT('Ctrl Pts',(-1.49211363342996,-12.9151670287303,
126.15953679602));
#28648=CARTESIAN_POINT('Ctrl Pts',(-1.15953927046661,-12.9492629258861,
126.492111158983));
#28649=CARTESIAN_POINT('Ctrl Pts',(-0.948920279348187,-12.9673838309378,
126.636358409655));
#28650=CARTESIAN_POINT('Ctrl Pts',(-0.487054746182363,-12.9929315701904,
126.827811869943));
#28651=CARTESIAN_POINT('Ctrl Pts',(-0.235780955001909,-13.,126.875));
#28652=CARTESIAN_POINT('Ctrl Pts',(1.17961196366423E-15,-13.,126.875));
#28653=CARTESIAN_POINT('Origin',(0.,13.,111.));
#28654=CARTESIAN_POINT('',(-16.,-1.95943487863577E-15,111.));
#28655=CARTESIAN_POINT('Origin',(0.,0.,111.));
#28656=CARTESIAN_POINT('Origin',(0.,0.,0.));
#28657=CARTESIAN_POINT('',(-16.,-1.95943487863577E-15,100.));
#28658=CARTESIAN_POINT('',(-16.,-1.95943487863577E-15,0.));
#28659=CARTESIAN_POINT('',(16.,0.,100.));
#28660=CARTESIAN_POINT('Origin',(0.,0.,100.));
#28661=CARTESIAN_POINT('Origin',(0.,0.,100.));
#28662=CARTESIAN_POINT('Origin',(0.,0.,100.));
#28663=CARTESIAN_POINT('Ctrl Pts',(-7.62166314348063,15.7531022204317,98.500000610284));
#28664=CARTESIAN_POINT('Ctrl Pts',(-7.69400225181639,15.5188970106341,98.6793214334492));
#28665=CARTESIAN_POINT('Ctrl Pts',(-7.78580021647469,15.282866431888,98.8494491913713));
#28666=CARTESIAN_POINT('Ctrl Pts',(-8.01090275442514,14.8162420216974,99.1580199459299));
#28667=CARTESIAN_POINT('Ctrl Pts',(-8.14397944499903,14.5853179903069,99.2969308183713));
#28668=CARTESIAN_POINT('Ctrl Pts',(-8.38183223465004,14.242273311074,99.4748187550338));
#28669=CARTESIAN_POINT('Ctrl Pts',(-8.46796561908336,14.1280782793539,99.5290970577315));
#28670=CARTESIAN_POINT('Ctrl Pts',(-8.65039182617701,13.9063490976389,99.62326558462));
#28671=CARTESIAN_POINT('Ctrl Pts',(-8.74705976167071,13.7981959987251,99.6635148733605));
#28672=CARTESIAN_POINT('Ctrl Pts',(-9.05460506897777,13.4823163139724,99.7618768897715));
#28673=CARTESIAN_POINT('Ctrl Pts',(-9.28643675965965,13.2812823779052,99.7968963262704));
#28674=CARTESIAN_POINT('Ctrl Pts',(-9.6503936412052,13.0174883808938,99.7962149169054));
#28675=CARTESIAN_POINT('Ctrl Pts',(-9.775045002922,12.9350475934176,99.7875063317089));
#28676=CARTESIAN_POINT('Ctrl Pts',(-10.0309579794496,12.7810506313035,99.753358404991));
#28677=CARTESIAN_POINT('Ctrl Pts',(-10.1633841214783,12.708950911147,99.7275975989373));
#28678=CARTESIAN_POINT('Ctrl Pts',(-10.5613890038482,12.5136572830832,99.6277174576398));
#28679=CARTESIAN_POINT('Ctrl Pts',(-10.8257011162573,12.4115301467734,99.5324632749564));
#28680=CARTESIAN_POINT('Ctrl Pts',(-11.3534955337226,12.2529722492584,99.2974531785354));
#28681=CARTESIAN_POINT('Ctrl Pts',(-11.6189361780422,12.1966627203719,99.15615753822));
#28682=CARTESIAN_POINT('Ctrl Pts',(-12.1322393649622,12.1271244860313,98.8472990531188));
#28683=CARTESIAN_POINT('Ctrl Pts',(-12.3821304053377,12.1130390987287,98.6790582739387));
#28684=CARTESIAN_POINT('Ctrl Pts',(-12.6268678194693,12.1166087086112,98.5000000706302));
#28685=CARTESIAN_POINT('Ctrl Pts',(-15.4254975876205,8.26462497236944,98.5000000648311));
#28686=CARTESIAN_POINT('Ctrl Pts',(-15.3989615977616,8.18681012724391,98.5601400874486));
#28687=CARTESIAN_POINT('Ctrl Pts',(-15.3740814904822,8.1075208710261,98.6192489818091));
#28688=CARTESIAN_POINT('Ctrl Pts',(-15.350981847033,8.02689530039092,98.6770789349994));
#28689=CARTESIAN_POINT('Ctrl Pts',(-15.3272514958921,7.94406834653243,98.7364878647817));
#28690=CARTESIAN_POINT('Ctrl Pts',(-15.3053993169593,7.85983038415878,98.7945484303283));
#28691=CARTESIAN_POINT('Ctrl Pts',(-15.2855818246038,7.774281656423,98.8509939558039));
#28692=CARTESIAN_POINT('Ctrl Pts',(-15.2699513231154,7.70680745271355,98.8955138099879));
#28693=CARTESIAN_POINT('Ctrl Pts',(-15.2555868575626,7.63851671032234,98.9390292514823));
#28694=CARTESIAN_POINT('Ctrl Pts',(-15.2425795199652,7.56944243117125,98.981401669026));
#28695=CARTESIAN_POINT('Ctrl Pts',(-15.2403905735312,7.55781823091516,98.9885323328985));
#28696=CARTESIAN_POINT('Ctrl Pts',(-15.2382391277396,7.54617292290309,98.9956311576658));
#28697=CARTESIAN_POINT('Ctrl Pts',(-15.2361254605806,7.53450571055505,99.0026979840552));
#28698=CARTESIAN_POINT('Ctrl Pts',(-15.209459094505,7.38731027619741,99.0918542065433));
#28699=CARTESIAN_POINT('Ctrl Pts',(-15.1888463312715,7.2368487771976,99.1757821758939));
#28700=CARTESIAN_POINT('Ctrl Pts',(-15.1749739382223,7.08263617809772,99.2535679557348));
#28701=CARTESIAN_POINT('Ctrl Pts',(-15.1657087941053,6.97964010883575,99.3055198041236));
#28702=CARTESIAN_POINT('Ctrl Pts',(-15.1594497290289,6.87497109524008,99.3547324640411));
#28703=CARTESIAN_POINT('Ctrl Pts',(-15.1563931490129,6.7684890497211,99.4009428779259));
#28704=CARTESIAN_POINT('Ctrl Pts',(-15.1561145921655,6.75878496779186,99.405154194868));
#28705=CARTESIAN_POINT('Ctrl Pts',(-15.1558636606571,6.74906375936666,99.409340145667));
#28706=CARTESIAN_POINT('Ctrl Pts',(-15.1556404821766,6.73932606051682,99.4135002521259));
#28707=CARTESIAN_POINT('Ctrl Pts',(-15.1519973739088,6.58037036234059,99.4814087628382));
#28708=CARTESIAN_POINT('Ctrl Pts',(-15.1557666604111,6.41694578086669,99.5424448370954));
#28709=CARTESIAN_POINT('Ctrl Pts',(-15.1675209018535,6.25170583473857,99.5945560958749));
#28710=CARTESIAN_POINT('Ctrl Pts',(-15.1758230391991,6.13499522142745,99.6313627949514));
#28711=CARTESIAN_POINT('Ctrl Pts',(-15.1881085912407,6.01737791060435,99.6637177718552));
#28712=CARTESIAN_POINT('Ctrl Pts',(-15.2045787950897,5.89977535028896,99.6909054353086));
#28713=CARTESIAN_POINT('Ctrl Pts',(-15.2053629424751,5.89417628539394,99.6921998415835));
#28714=CARTESIAN_POINT('Ctrl Pts',(-15.2061565022706,5.88857599398075,99.6934831334187));
#28715=CARTESIAN_POINT('Ctrl Pts',(-15.2069595049574,5.8829744697482,99.694755268259));
#28716=CARTESIAN_POINT('Ctrl Pts',(-15.2273306528143,5.74087098709944,99.7270276969224));
#28717=CARTESIAN_POINT('Ctrl Pts',(-15.253773829766,5.59800970804938,99.7521123711275));
#28718=CARTESIAN_POINT('Ctrl Pts',(-15.2867992989703,5.45419637581596,99.7693348591779));
#28719=CARTESIAN_POINT('Ctrl Pts',(-15.2874528993659,5.45135019518315,99.7696757059629));
#28720=CARTESIAN_POINT('Ctrl Pts',(-15.2881090485027,5.44850399099787,99.7700133667743));
#28721=CARTESIAN_POINT('Ctrl Pts',(-15.2887677380553,5.44565779119462,99.7703478403197));
#28722=CARTESIAN_POINT('Ctrl Pts',(-15.3138490822817,5.33728121725203,99.7830838038606));
#28723=CARTESIAN_POINT('Ctrl Pts',(-15.3426027353379,5.22896570099945,99.7911914401022));
#28724=CARTESIAN_POINT('Ctrl Pts',(-15.3745952689208,5.1221752573672,99.794599167721));
#28725=CARTESIAN_POINT('Ctrl Pts',(-15.3858966024805,5.08445162971674,99.795802944421));
#28726=CARTESIAN_POINT('Ctrl Pts',(-15.3976023968509,5.04691831198085,99.7964198693814));
#28727=CARTESIAN_POINT('Ctrl Pts',(-15.4096944350009,5.00964014842566,99.7964455441609));
#28728=CARTESIAN_POINT('Ctrl Pts',(-15.4097526805227,5.00946058514124,99.7964456678324));
#28729=CARTESIAN_POINT('Ctrl Pts',(-15.4098109349276,5.00928102801947,99.7964457777851));
#28730=CARTESIAN_POINT('Ctrl Pts',(-15.4098691982134,5.00910147706792,99.7964458740184));
#28731=CARTESIAN_POINT('Ctrl Pts',(-15.452400154641,4.87803311074117,99.7965161223064));
#28732=CARTESIAN_POINT('Ctrl Pts',(-15.5000808965492,4.74882134911773,99.7893191842779));
#28733=CARTESIAN_POINT('Ctrl Pts',(-15.5525709850149,4.6220096743371,99.7751251055994));
#28734=CARTESIAN_POINT('Ctrl Pts',(-15.6056842522426,4.493692451656,99.7607625103754));
#28735=CARTESIAN_POINT('Ctrl Pts',(-15.6637220710125,4.3678319517557,99.7392354386705));
#28736=CARTESIAN_POINT('Ctrl Pts',(-15.7263585380238,4.24501089848265,99.7107825845669));
#28737=CARTESIAN_POINT('Ctrl Pts',(-15.7366180361955,4.22489350630477,99.7061221683815));
#28738=CARTESIAN_POINT('Ctrl Pts',(-15.7470009608383,4.20485771388323,99.701275858843));
#28739=CARTESIAN_POINT('Ctrl Pts',(-15.7575059376538,4.18490615157863,99.6962446073889));
#28740=CARTESIAN_POINT('Ctrl Pts',(-15.7603333207195,4.1795362483047,99.6948904611199));
#28741=CARTESIAN_POINT('Ctrl Pts',(-15.7631694550508,4.17417259583829,99.6935229664922));
#28742=CARTESIAN_POINT('Ctrl Pts',(-15.7660143095016,4.16881525076369,99.692142145394));
#28743=CARTESIAN_POINT('Ctrl Pts',(-15.8523453645961,4.00623918200715,99.6502392134979));
#28744=CARTESIAN_POINT('Ctrl Pts',(-15.945957559091,3.85094812019755,99.5964381242811));
#28745=CARTESIAN_POINT('Ctrl Pts',(-16.0446983463237,3.70416010938547,99.5332547186234));
#28746=CARTESIAN_POINT('Ctrl Pts',(-16.1016422036435,3.6195073961736,99.4968168195791));
#28747=CARTESIAN_POINT('Ctrl Pts',(-16.1602914482781,3.53768342281066,99.4572586816833));
#28748=CARTESIAN_POINT('Ctrl Pts',(-16.2202297140019,3.45892855318697,99.4150655759484));
#28749=CARTESIAN_POINT('Ctrl Pts',(-16.2263505132198,3.4508862326663,99.4107568839056));
#28750=CARTESIAN_POINT('Ctrl Pts',(-16.2324843106259,3.44287636886361,99.4064210546897));
#28751=CARTESIAN_POINT('Ctrl Pts',(-16.238630726799,3.43489911689116,99.4020585662807));
#28752=CARTESIAN_POINT('Ctrl Pts',(-16.3058910028174,3.34760399166231,99.3543198245074));
#28753=CARTESIAN_POINT('Ctrl Pts',(-16.3750790005671,3.2636136741201,99.3031450764238));
#28754=CARTESIAN_POINT('Ctrl Pts',(-16.4459839896838,3.1827936689064,99.2489133667349));
#28755=CARTESIAN_POINT('Ctrl Pts',(-16.5207937966315,3.09752281472716,99.1916950555439));
#28756=CARTESIAN_POINT('Ctrl Pts',(-16.5975155631586,3.01578072195888,99.1310729372186));
#28757=CARTESIAN_POINT('Ctrl Pts',(-16.6759149977342,2.9374575563625,99.0674634405586));
#28758=CARTESIAN_POINT('Ctrl Pts',(-16.7020156296198,2.91138231584061,99.0462866544537));
#28759=CARTESIAN_POINT('Ctrl Pts',(-16.7283022642725,2.88568641273419,99.0247785979167));
#28760=CARTESIAN_POINT('Ctrl Pts',(-16.7547663508278,2.86036698978197,99.0029542627797));
#28761=CARTESIAN_POINT('Ctrl Pts',(-16.8153481932165,2.80240552236248,98.9529937841234));
#28762=CARTESIAN_POINT('Ctrl Pts',(-16.8765673950408,2.74668841444285,98.9016192560261));
#28763=CARTESIAN_POINT('Ctrl Pts',(-16.9384055914951,2.69304838623785,98.8489571073848));
#28764=CARTESIAN_POINT('Ctrl Pts',(-17.0035287415344,2.63655890554152,98.7934974529318));
#28765=CARTESIAN_POINT('Ctrl Pts',(-17.06933900837,2.58237266537676,98.7366089356619));
#28766=CARTESIAN_POINT('Ctrl Pts',(-17.1358266349123,2.53034639929748,98.6784119085642));
#28767=CARTESIAN_POINT('Ctrl Pts',(-17.2023142614546,2.4783201332182,98.6202148814666));
#28768=CARTESIAN_POINT('Ctrl Pts',(-17.2694800239621,2.42845385999384,98.5607082197099));
#28769=CARTESIAN_POINT('Ctrl Pts',(-17.337314796066,2.38065715175377,98.5000007932762));
#28770=CARTESIAN_POINT('Ctrl Pts',(-17.3373139553419,-2.38065609737471,
98.500000610284));
#28771=CARTESIAN_POINT('Ctrl Pts',(-17.1369255782473,-2.52182806773903,
98.6793214334492));
#28772=CARTESIAN_POINT('Ctrl Pts',(-16.9408142894144,-2.68207058023464,
98.8494491913713));
#28773=CARTESIAN_POINT('Ctrl Pts',(-16.5665886131438,-3.0403506885261,99.1580199459299));
#28774=CARTESIAN_POINT('Ctrl Pts',(-16.3880897672633,-3.23827359237263,
99.2969308183713));
#28775=CARTESIAN_POINT('Ctrl Pts',(-16.1353354438601,-3.57049167360208,
99.4748187550338));
#28776=CARTESIAN_POINT('Ctrl Pts',(-16.0533461943871,-3.68769759561264,
99.5290970577315));
#28777=CARTESIAN_POINT('Ctrl Pts',(-15.8988420094755,-3.92971331391084,
99.62326558462));
#28778=CARTESIAN_POINT('Ctrl Pts',(-15.8258543348747,-4.05507112943762,
99.6635148733605));
#28779=CARTESIAN_POINT('Ctrl Pts',(-15.6204716288236,-4.44517628877436,
99.7618768897716));
#28780=CARTESIAN_POINT('Ctrl Pts',(-15.5009169261858,-4.72778423157193,
99.7968963262704));
#28781=CARTESIAN_POINT('Ctrl Pts',(-15.3625027879858,-5.15544462350693,
99.7962149169053));
#28782=CARTESIAN_POINT('Ctrl Pts',(-15.3226163289905,-5.29947071769255,
99.7875063317089));
#28783=CARTESIAN_POINT('Ctrl Pts',(-15.2552379735104,-5.59044609999894,
99.753358404991));
#28784=CARTESIAN_POINT('Ctrl Pts',(-15.2275889932189,-5.73867088412122,
99.7275975989373));
#28785=CARTESIAN_POINT('Ctrl Pts',(-15.1648439881543,-6.17754507098127,
99.6277174576398));
#28786=CARTESIAN_POINT('Ctrl Pts',(-15.14939224423,-6.46047984853023,99.5324632749564));
#28787=CARTESIAN_POINT('Ctrl Pts',(-15.1616921671213,-7.01143925344933,
99.2974531785354));
#28788=CARTESIAN_POINT('Ctrl Pts',(-15.1901642928368,-7.28128890929021,
99.15615753822));
#28789=CARTESIAN_POINT('Ctrl Pts',(-15.2826489099606,-7.79095774621569,
98.8472990531188));
#28790=CARTESIAN_POINT('Ctrl Pts',(-15.3464734888,-8.03297087257737,98.6790582739387));
#28791=CARTESIAN_POINT('Ctrl Pts',(-15.4254964096654,-8.26462691495154,
98.5000000706302));
#28792=CARTESIAN_POINT('Ctrl Pts',(-12.6268663212258,-12.1166104449802,
98.5000000648703));
#28793=CARTESIAN_POINT('Ctrl Pts',(-12.5446458774943,-12.1154191815706,
98.5601503317705));
#28794=CARTESIAN_POINT('Ctrl Pts',(-12.4615341179103,-12.1162591862576,
98.6192693642505));
#28795=CARTESIAN_POINT('Ctrl Pts',(-12.3777014366231,-12.1192061781956,
98.6771089720691));
#28796=CARTESIAN_POINT('Ctrl Pts',(-12.291574122314,-12.1222338339619,98.736531741395));
#28797=CARTESIAN_POINT('Ctrl Pts',(-12.2046849293976,-12.1274848184644,
98.7946054582262));
#28798=CARTESIAN_POINT('Ctrl Pts',(-12.117178171504,-12.1350769190544,98.8510630180339));
#28799=CARTESIAN_POINT('Ctrl Pts',(-12.0477278724933,-12.1411024383261,
98.8958709220683));
#28800=CARTESIAN_POINT('Ctrl Pts',(-11.9778875804926,-12.1486032210726,
98.9396611167543));
#28801=CARTESIAN_POINT('Ctrl Pts',(-11.9077182330857,-12.157657152302,98.9822921355006));
#28802=CARTESIAN_POINT('Ctrl Pts',(-11.8959551442278,-12.1591749403604,
98.9894387383999));
#28803=CARTESIAN_POINT('Ctrl Pts',(-11.8841835086262,-12.1607351471297,
98.9965533320491));
#28804=CARTESIAN_POINT('Ctrl Pts',(-11.872402649482,-12.1623382885869,99.0036357543382));
#28805=CARTESIAN_POINT('Ctrl Pts',(-11.7229964864066,-12.1826695064605,
99.0934558197971));
#28806=CARTESIAN_POINT('Ctrl Pts',(-11.5723364223253,-12.2098752720322,
99.1779621201775));
#28807=CARTESIAN_POINT('Ctrl Pts',(-11.4201636558614,-12.2447803502433,
99.256219095195));
#28808=CARTESIAN_POINT('Ctrl Pts',(-11.3200139898558,-12.2677524759789,
99.3077224626682));
#28809=CARTESIAN_POINT('Ctrl Pts',(-11.2192092246076,-12.2940588050411,
99.3565196706126));
#28810=CARTESIAN_POINT('Ctrl Pts',(-11.1176771661422,-12.3239257557744,
99.4023528281028));
#28811=CARTESIAN_POINT('Ctrl Pts',(-11.1083271026094,-12.3266761962865,
99.4065735928634));
#28812=CARTESIAN_POINT('Ctrl Pts',(-11.0989693146526,-12.3294584306974,
99.4107687371792));
#28813=CARTESIAN_POINT('Ctrl Pts',(-11.0896044489173,-12.332272384062,99.4149377803026));
#28814=CARTESIAN_POINT('Ctrl Pts',(-10.9368635549275,-12.3781679435612,
99.4829348441968));
#28815=CARTESIAN_POINT('Ctrl Pts',(-10.7821807783801,-12.4325386244579,
99.5439998059001));
#28816=CARTESIAN_POINT('Ctrl Pts',(-10.6282589265402,-12.4951094361099,
99.596075947797));
#28817=CARTESIAN_POINT('Ctrl Pts',(-10.5197442278578,-12.5392217742319,
99.6327895578461));
#28818=CARTESIAN_POINT('Ctrl Pts',(-10.4116066693124,-12.587410060724,99.6650361416381));
#28819=CARTESIAN_POINT('Ctrl Pts',(-10.3047803019272,-12.6395820517603,
99.6921021736602));
#28820=CARTESIAN_POINT('Ctrl Pts',(-10.2996691247951,-12.6420782546552,
99.6933971655926));
#28821=CARTESIAN_POINT('Ctrl Pts',(-10.2945597086435,-12.644583905749,99.6946809027462));
#28822=CARTESIAN_POINT('Ctrl Pts',(-10.2894520568858,-12.6470990367868,
99.6959533416379));
#28823=CARTESIAN_POINT('Ctrl Pts',(-10.1603732160565,-12.7106605743163,
99.7281099852292));
#28824=CARTESIAN_POINT('Ctrl Pts',(-10.0324732032076,-12.7802460636459,
99.753042557793));
#28825=CARTESIAN_POINT('Ctrl Pts',(-9.9057096702643,-12.8564220781232,99.7700686162087));
#28826=CARTESIAN_POINT('Ctrl Pts',(-9.78852854268104,-12.9268397373978,
99.7858076278718));
#28827=CARTESIAN_POINT('Ctrl Pts',(-9.67313030469678,-13.0025204956137,
99.7945520991956));
#28828=CARTESIAN_POINT('Ctrl Pts',(-9.56184140648273,-13.0818662612157,
99.7961709162458));
#28829=CARTESIAN_POINT('Ctrl Pts',(-9.5479606610537,-13.0917628312318,99.7963728266585));
#28830=CARTESIAN_POINT('Ctrl Pts',(-9.53414386521357,-13.1017164514468,
99.7964638312961));
#28831=CARTESIAN_POINT('Ctrl Pts',(-9.52039555682255,-13.1117240463959,
99.7964436301271));
#28832=CARTESIAN_POINT('Ctrl Pts',(-9.520267099632,-13.1118175522654,99.7964434413776));
#28833=CARTESIAN_POINT('Ctrl Pts',(-9.52013864842916,-13.11191106284,99.7964432429204));
#28834=CARTESIAN_POINT('Ctrl Pts',(-9.52001020321784,-13.1120045781169,
99.7964430347553));
#28835=CARTESIAN_POINT('Ctrl Pts',(-9.39854187906109,-13.2004402920585,
99.7962461766987));
#28836=CARTESIAN_POINT('Ctrl Pts',(-9.28143127084363,-13.2936651206149,
99.7875210116457));
#28837=CARTESIAN_POINT('Ctrl Pts',(-9.16861451193018,-13.3916016257417,
99.7704440514026));
#28838=CARTESIAN_POINT('Ctrl Pts',(-9.16621596908933,-13.3936838066649,
99.7700809863657));
#28839=CARTESIAN_POINT('Ctrl Pts',(-9.16381939232461,-13.39576809596,99.7697141495904));
#28840=CARTESIAN_POINT('Ctrl Pts',(-9.16142477903311,-13.3978544944897,
99.7693435426227));
#28841=CARTESIAN_POINT('Ctrl Pts',(-9.07547278649159,-13.4727434594413,
99.7560410158919));
#28842=CARTESIAN_POINT('Ctrl Pts',(-8.9915392882287,-13.5509036748962,99.7376874829348));
#28843=CARTESIAN_POINT('Ctrl Pts',(-8.91103700467454,-13.6308471455214,
99.7148306067551));
#28844=CARTESIAN_POINT('Ctrl Pts',(-8.88817991952993,-13.6535455664129,
99.7083408335225));
#28845=CARTESIAN_POINT('Ctrl Pts',(-8.86559966104437,-13.6763878102703,
99.7014877883099));
#28846=CARTESIAN_POINT('Ctrl Pts',(-8.84332918088635,-13.6993398531878,
99.6942835087754));
#28847=CARTESIAN_POINT('Ctrl Pts',(-8.83915122841372,-13.7036456671523,
99.692931982572));
#28848=CARTESIAN_POINT('Ctrl Pts',(-8.83498423109444,-13.707955266888,99.6915681321741));
#28849=CARTESIAN_POINT('Ctrl Pts',(-8.83082841847428,-13.712268414179,99.6901920420673));
#28850=CARTESIAN_POINT('Ctrl Pts',(-8.69127076580918,-13.8571095719862,
99.6439811267264));
#28851=CARTESIAN_POINT('Ctrl Pts',(-8.56417600543209,-14.0055185188973,
99.5845379976685));
#28852=CARTESIAN_POINT('Ctrl Pts',(-8.44794279560312,-14.1572127309531,
99.5138249402946));
#28853=CARTESIAN_POINT('Ctrl Pts',(-8.39715446235132,-14.2234958199739,
99.4829267286007));
#28854=CARTESIAN_POINT('Ctrl Pts',(-8.34843948408571,-14.2904060698911,
99.4498772977175));
#28855=CARTESIAN_POINT('Ctrl Pts',(-8.30166232922775,-14.357919515952,99.4148427913138));
#28856=CARTESIAN_POINT('Ctrl Pts',(-8.29602633367793,-14.3660539457331,
99.4106216213264));
#28857=CARTESIAN_POINT('Ctrl Pts',(-8.29041845450117,-14.3741972107076,
99.4063715743575));
#28858=CARTESIAN_POINT('Ctrl Pts',(-8.28483845220995,-14.3823492736635,
99.4020929385903));
#28859=CARTESIAN_POINT('Ctrl Pts',(-8.19855951863415,-14.5083978416683,
99.3359359530035));
#28860=CARTESIAN_POINT('Ctrl Pts',(-8.11890479704849,-14.6370031608812,
99.2625264797838));
#28861=CARTESIAN_POINT('Ctrl Pts',(-8.04618036364231,-14.7663488924165,
99.1837466668059));
#28862=CARTESIAN_POINT('Ctrl Pts',(-7.99257245587884,-14.8616944829006,
99.1256751116222));
#28863=CARTESIAN_POINT('Ctrl Pts',(-7.94273055714886,-14.9574417704728,
99.0646859940682));
#28864=CARTESIAN_POINT('Ctrl Pts',(-7.89678243508448,-15.052850115494,99.0015448475648));
#28865=CARTESIAN_POINT('Ctrl Pts',(-7.8916489520208,-15.0635094656762,98.9944905003656));
#28866=CARTESIAN_POINT('Ctrl Pts',(-7.88656339889997,-15.074165771925,98.9874085551186));
#28867=CARTESIAN_POINT('Ctrl Pts',(-7.88152602873833,-15.0848179083459,
98.9803001233707));
#28868=CARTESIAN_POINT('Ctrl Pts',(-7.82583177604172,-15.2025902297257,
98.9017077663791));
#28869=CARTESIAN_POINT('Ctrl Pts',(-7.77556907089792,-15.3204628413257,
98.8195805048243));
#28870=CARTESIAN_POINT('Ctrl Pts',(-7.7303783531495,-15.4384372752834,98.7343244488909));
#28871=CARTESIAN_POINT('Ctrl Pts',(-7.69023139128725,-15.5432445307731,
98.6585838588623));
#28872=CARTESIAN_POINT('Ctrl Pts',(-7.65408652108198,-15.6481322437112,
98.5803745642925));
#28873=CARTESIAN_POINT('Ctrl Pts',(-7.62166303813141,-15.7531031392177,
98.5000003292224));
#28874=CARTESIAN_POINT('Ctrl Pts',(-3.09338453344274,-17.2244295663994,
98.5000000648311));
#28875=CARTESIAN_POINT('Ctrl Pts',(-3.02757828977043,-17.175146230785,98.5601400874298));
#28876=CARTESIAN_POINT('Ctrl Pts',(-2.95985810196491,-17.1269821150027,
98.6192489817723));
#28877=CARTESIAN_POINT('Ctrl Pts',(-2.89031681004483,-17.0800983770824,
98.6770789349455));
#28878=CARTESIAN_POINT('Ctrl Pts',(-2.8188767776614,-17.0319345356753,98.7364878647103));
#28879=CARTESIAN_POINT('Ctrl Pts',(-2.74551440930578,-16.9851209165741,
98.7945484302403));
#28880=CARTESIAN_POINT('Ctrl Pts',(-2.67027667628172,-16.9398373506274,
98.8509939557004));
#28881=CARTESIAN_POINT('Ctrl Pts',(-2.61093498570845,-16.9041211846764,
98.8955138099206));
#28882=CARTESIAN_POINT('Ctrl Pts',(-2.55042549407967,-16.8693567661241,
98.9390292514498));
#28883=CARTESIAN_POINT('Ctrl Pts',(-2.48875143910593,-16.8356409267845,
98.9814016690262));
#28884=CARTESIAN_POINT('Ctrl Pts',(-2.47837258935355,-16.8299670395895,
98.9885323328987));
#28885=CARTESIAN_POINT('Ctrl Pts',(-2.46796207659648,-16.8243222949694,
98.995631157666));
#28886=CARTESIAN_POINT('Ctrl Pts',(-2.45751905733843,-16.8187067111521,
99.0026979840554));
#28887=CARTESIAN_POINT('Ctrl Pts',(-2.32576824024065,-16.7478595990157,
99.0918542067995));
#28888=CARTESIAN_POINT('Ctrl Pts',(-2.18904054489823,-16.6817605358573,
99.1757821763761));
#28889=CARTESIAN_POINT('Ctrl Pts',(-2.04666245239284,-16.620912792038,99.2535679564052));
#28890=CARTESIAN_POINT('Ctrl Pts',(-1.95157045694327,-16.5802735807903,
99.305519804547));
#28891=CARTESIAN_POINT('Ctrl Pts',(-1.85395846739465,-16.5419763523534,
99.3547324642399));
#28892=CARTESIAN_POINT('Ctrl Pts',(-1.75363255973665,-16.5061646105045,
99.400942877926));
#28893=CARTESIAN_POINT('Ctrl Pts',(-1.74448950818291,-16.5029009609687,
99.405154194868));
#28894=CARTESIAN_POINT('Ctrl Pts',(-1.7353216316644,-16.4996582923132,99.409340145667));
#28895=CARTESIAN_POINT('Ctrl Pts',(-1.72612949566279,-16.4964369225343,
99.4135002521259));
#28896=CARTESIAN_POINT('Ctrl Pts',(-1.57607942543336,-16.4438521085721,
99.4814087628581));
#28897=CARTESIAN_POINT('Ctrl Pts',(-1.4194886386662,-16.396935940076,99.5424448371308));
#28898=CARTESIAN_POINT('Ctrl Pts',(-1.25870385073772,-16.3570529364832,
99.5945560959203));
#28899=CARTESIAN_POINT('Ctrl Pts',(-1.14513995994311,-16.3288831753824,
99.6313627949779));
#28900=CARTESIAN_POINT('Ctrl Pts',(-1.0294828057368,-16.3042216818427,99.6637177718662));
#28901=CARTESIAN_POINT('Ctrl Pts',(-0.912546551574103,-16.283544586827,
99.6909054353085));
#28902=CARTESIAN_POINT('Ctrl Pts',(-0.906979209552365,-16.2825601491024,
99.6921998415834));
#28903=CARTESIAN_POINT('Ctrl Pts',(-0.901407792447838,-16.2815842840969,
99.6934831334186));
#28904=CARTESIAN_POINT('Ctrl Pts',(-0.89583228484855,-16.2806170188525,
99.6947552682589));
#28905=CARTESIAN_POINT('Ctrl Pts',(-0.75438881080454,-16.2560787406678,
99.7270276969224));
#28906=CARTESIAN_POINT('Ctrl Pts',(-0.610348269374357,-16.2370811333547,
99.7521123711276));
#28907=CARTESIAN_POINT('Ctrl Pts',(-0.463368231392308,-16.2240494573673,
99.7693348591778));
#28908=CARTESIAN_POINT('Ctrl Pts',(-0.460459379125149,-16.223791550098,
99.7696757059629));
#28909=CARTESIAN_POINT('Ctrl Pts',(-0.457549716853913,-16.2235360595476,
99.7700133667742));
#28910=CARTESIAN_POINT('Ctrl Pts',(-0.454639273718578,-16.2232829864302,
99.7703478403196));
#28911=CARTESIAN_POINT('Ctrl Pts',(-0.343816465256741,-16.2136465591544,
99.7830838038597));
#28912=CARTESIAN_POINT('Ctrl Pts',(-0.231916920272007,-16.2075215729844,
99.7911914401011));
#28913=CARTESIAN_POINT('Ctrl Pts',(-0.120466936414993,-16.2049482186016,
99.7945991677203));
#28914=CARTESIAN_POINT('Ctrl Pts',(-0.0810973303828984,-16.2040391834926,
99.7958029444208));
#28915=CARTESIAN_POINT('Ctrl Pts',(-0.0417837345711198,-16.2035736224711,
99.7964198693814));
#28916=CARTESIAN_POINT('Ctrl Pts',(-0.002593448913701,-16.2035542480913,
99.7964455441609));
#28917=CARTESIAN_POINT('Ctrl Pts',(-0.00240467522590323,-16.2035541547678,
99.7964456678325));
#28918=CARTESIAN_POINT('Ctrl Pts',(-0.00221590465409573,-16.2035540717971,
99.7964457777851));
#28919=CARTESIAN_POINT('Ctrl Pts',(-0.00202713720613238,-16.2035539991795,
99.7964458740185));
#28920=CARTESIAN_POINT('Ctrl Pts',(0.13576907501567,-16.2035009898142,99.7965161223064));
#28921=CARTESIAN_POINT('Ctrl Pts',(0.273390922467042,-16.2089194398948,
99.7893191842755));
#28922=CARTESIAN_POINT('Ctrl Pts',(0.410216321504649,-16.2196535179823,
99.7751251055922));
#28923=CARTESIAN_POINT('Ctrl Pts',(0.548666154514294,-16.2305150344054,
99.7607625103632));
#28924=CARTESIAN_POINT('Ctrl Pts',(0.686301275430305,-16.2468192467542,
99.7392354386506));
#28925=CARTESIAN_POINT('Ctrl Pts',(0.822466771282481,-16.2684362741424,
99.7107825845366));
#28926=CARTESIAN_POINT('Ctrl Pts',(0.844769907444301,-16.27197702066,99.7061221683605));
#28927=CARTESIAN_POINT('Ctrl Pts',(0.867033578503416,-16.275660368438,99.7012758588322));
#28928=CARTESIAN_POINT('Ctrl Pts',(0.889254858156698,-16.2794858232672,
99.696244607389));
#28929=CARTESIAN_POINT('Ctrl Pts',(0.895235649074151,-16.2805154329861,
99.69489046112));
#28930=CARTESIAN_POINT('Ctrl Pts',(0.901213199410171,-16.2815552972589,
99.6935229664923));
#28931=CARTESIAN_POINT('Ctrl Pts',(0.907187445725223,-16.2826054039495,
99.6921421453941));
#28932=CARTESIAN_POINT('Ctrl Pts',(1.08848423854067,-16.3144723483427,99.650239213483));
#28933=CARTESIAN_POINT('Ctrl Pts',(1.26510257383785,-16.3555152587659,99.596438124243));
#28934=CARTESIAN_POINT('Ctrl Pts',(1.43521884938335,-16.4040633379988,99.5332547185562));
#28935=CARTESIAN_POINT('Ctrl Pts',(1.53332498347954,-16.4320610375491,99.4968168195304));
#28936=CARTESIAN_POINT('Ctrl Pts',(1.62926781977423,-16.4625547855007,99.4572586816574));
#28937=CARTESIAN_POINT('Ctrl Pts',(1.72269009438428,-16.4952228705692,99.4150655759485));
#28938=CARTESIAN_POINT('Ctrl Pts',(1.73223022669911,-16.4985588828353,99.4107568839056));
#28939=CARTESIAN_POINT('Ctrl Pts',(1.74174350750183,-16.5019172867903,99.4064210546897));
#28940=CARTESIAN_POINT('Ctrl Pts',(1.75122967202433,-16.5052977695157,99.4020585662807));
#28941=CARTESIAN_POINT('Ctrl Pts',(1.85503683804843,-16.5422904160884,99.3543198245082));
#28942=CARTESIAN_POINT('Ctrl Pts',(1.95629664396254,-16.5821376767137,99.3031450764253));
#28943=CARTESIAN_POINT('Ctrl Pts',(2.05507188318957,-16.6245975735538,99.2489133667373));
#28944=CARTESIAN_POINT('Ctrl Pts',(2.1592867864,-16.6693957848681,99.191695055546));
#28945=CARTESIAN_POINT('Ctrl Pts',(2.26073646607868,-16.7171028250444,99.1310729372205));
#28946=CARTESIAN_POINT('Ctrl Pts',(2.35945298072967,-16.7674619289491,99.0674634405602));
#28947=CARTESIAN_POINT('Ctrl Pts',(2.39231754695952,-16.7842274125301,99.0462866544548));
#28948=CARTESIAN_POINT('Ctrl Pts',(2.42487881988457,-16.8012870169628,99.0247785979171));
#28949=CARTESIAN_POINT('Ctrl Pts',(2.45713687455928,-16.8186317269496,99.0029542627794));
#28950=CARTESIAN_POINT('Ctrl Pts',(2.53098232469012,-16.8583374044703,98.9529937841238));
#28951=CARTESIAN_POINT('Ctrl Pts',(2.60289021699092,-16.8993427920625,98.9016192560274));
#28952=CARTESIAN_POINT('Ctrl Pts',(2.67301396895445,-16.9415787314616,98.848957107387));
#28953=CARTESIAN_POINT('Ctrl Pts',(2.74686281776279,-16.9860583181297,98.7934974529337));
#28954=CARTESIAN_POINT('Ctrl Pts',(2.81873348542218,-17.031903132171,98.7366089356634));
#28955=CARTESIAN_POINT('Ctrl Pts',(2.88875921131318,-17.0790596222749,98.6784119085654));
#28956=CARTESIAN_POINT('Ctrl Pts',(2.95878493720418,-17.1262161123789,98.6202148814674));
#28957=CARTESIAN_POINT('Ctrl Pts',(3.0269659433531,-17.1746850226114,98.5607082197103));
#28958=CARTESIAN_POINT('Ctrl Pts',(3.09338541157247,-17.2244297295311,98.5000007932762));
#28959=CARTESIAN_POINT('Ctrl Pts',(7.62166314348062,-15.7531022204317,98.500000610284));
#28960=CARTESIAN_POINT('Ctrl Pts',(7.69400225181639,-15.5188970106341,98.6793214334492));
#28961=CARTESIAN_POINT('Ctrl Pts',(7.78580021647469,-15.282866431888,98.8494491913713));
#28962=CARTESIAN_POINT('Ctrl Pts',(8.01090275442513,-14.8162420216974,99.1580199459299));
#28963=CARTESIAN_POINT('Ctrl Pts',(8.14397944499903,-14.5853179903069,99.2969308183713));
#28964=CARTESIAN_POINT('Ctrl Pts',(8.38183223465004,-14.242273311074,99.4748187550338));
#28965=CARTESIAN_POINT('Ctrl Pts',(8.46796561908337,-14.1280782793539,99.5290970577316));
#28966=CARTESIAN_POINT('Ctrl Pts',(8.65039182617701,-13.9063490976389,99.62326558462));
#28967=CARTESIAN_POINT('Ctrl Pts',(8.74705976167071,-13.7981959987251,99.6635148733605));
#28968=CARTESIAN_POINT('Ctrl Pts',(9.05460506897777,-13.4823163139724,99.7618768897716));
#28969=CARTESIAN_POINT('Ctrl Pts',(9.28643675965965,-13.2812823779052,99.7968963262704));
#28970=CARTESIAN_POINT('Ctrl Pts',(9.6503936412052,-13.0174883808938,99.7962149169054));
#28971=CARTESIAN_POINT('Ctrl Pts',(9.775045002922,-12.9350475934176,99.7875063317089));
#28972=CARTESIAN_POINT('Ctrl Pts',(10.0309579794496,-12.7810506313035,99.753358404991));
#28973=CARTESIAN_POINT('Ctrl Pts',(10.1633841214783,-12.708950911147,99.7275975989373));
#28974=CARTESIAN_POINT('Ctrl Pts',(10.5613890038482,-12.5136572830832,99.6277174576398));
#28975=CARTESIAN_POINT('Ctrl Pts',(10.8257011162573,-12.4115301467734,99.5324632749563));
#28976=CARTESIAN_POINT('Ctrl Pts',(11.3534955337226,-12.2529722492584,99.2974531785354));
#28977=CARTESIAN_POINT('Ctrl Pts',(11.6189361780422,-12.1966627203719,99.15615753822));
#28978=CARTESIAN_POINT('Ctrl Pts',(12.1322393649622,-12.1271244860313,98.8472990531187));
#28979=CARTESIAN_POINT('Ctrl Pts',(12.3821304053377,-12.1130390987287,98.6790582739388));
#28980=CARTESIAN_POINT('Ctrl Pts',(12.6268678194693,-12.1166087086112,98.5000000706302));
#28981=CARTESIAN_POINT('Ctrl Pts',(15.4254975876205,-8.26462497236941,98.5000000648311));
#28982=CARTESIAN_POINT('Ctrl Pts',(15.39896159776,-8.18681012723897,98.5601400874524));
#28983=CARTESIAN_POINT('Ctrl Pts',(15.3740814904792,-8.10752087101609,98.6192489818165));
#28984=CARTESIAN_POINT('Ctrl Pts',(15.3509818470288,-8.02689530037569,98.6770789350102));
#28985=CARTESIAN_POINT('Ctrl Pts',(15.3272514958868,-7.94406834651245,98.7364878647956));
#28986=CARTESIAN_POINT('Ctrl Pts',(15.3053993169532,-7.8598303841339,98.7945484303452));
#28987=CARTESIAN_POINT('Ctrl Pts',(15.2855818245971,-7.77428165639307,98.8509939558235));
#28988=CARTESIAN_POINT('Ctrl Pts',(15.2699513231113,-7.70680745269335,98.8955138100007));
#28989=CARTESIAN_POINT('Ctrl Pts',(15.2555868575608,-7.63851671031211,98.9390292514885));
#28990=CARTESIAN_POINT('Ctrl Pts',(15.2425795199653,-7.5694424311712,98.9814016690259));
#28991=CARTESIAN_POINT('Ctrl Pts',(15.2403905735313,-7.55781823091512,98.9885323328984));
#28992=CARTESIAN_POINT('Ctrl Pts',(15.2382391277397,-7.54617292290305,98.9956311576657));
#28993=CARTESIAN_POINT('Ctrl Pts',(15.2361254605807,-7.53450571055501,99.0026979840551));
#28994=CARTESIAN_POINT('Ctrl Pts',(15.2094590945176,-7.38731027626687,99.0918542065011));
#28995=CARTESIAN_POINT('Ctrl Pts',(15.188846331291,-7.23684877733962,99.1757821758146));
#28996=CARTESIAN_POINT('Ctrl Pts',(15.174973938242,-7.08263617831606,99.2535679556245));
#28997=CARTESIAN_POINT('Ctrl Pts',(15.1657087941142,-6.97964010898367,99.305519804054));
#28998=CARTESIAN_POINT('Ctrl Pts',(15.1594497290312,-6.87497109531529,99.3547324640083));
#28999=CARTESIAN_POINT('Ctrl Pts',(15.1563931490129,-6.76848904972109,99.4009428779259));
#29000=CARTESIAN_POINT('Ctrl Pts',(15.1561145921656,-6.75878496779185,99.405154194868));
#29001=CARTESIAN_POINT('Ctrl Pts',(15.1558636606571,-6.74906375936666,99.409340145667));
#29002=CARTESIAN_POINT('Ctrl Pts',(15.1556404821766,-6.73932606051681,99.4135002521259));
#29003=CARTESIAN_POINT('Ctrl Pts',(15.1519973739076,-6.58037036229148,99.4814087628592));
#29004=CARTESIAN_POINT('Ctrl Pts',(15.1557666604135,-6.4169457807656,99.5424448371331));
#29005=CARTESIAN_POINT('Ctrl Pts',(15.1675209018644,-6.25170583458525,99.5945560959231));
#29006=CARTESIAN_POINT('Ctrl Pts',(15.17582303921,-6.1349952213244,99.6313627949797));
#29007=CARTESIAN_POINT('Ctrl Pts',(15.1881085912481,-6.01737791055278,99.663717771867));
#29008=CARTESIAN_POINT('Ctrl Pts',(15.2045787950898,-5.89977535028896,99.6909054353085));
#29009=CARTESIAN_POINT('Ctrl Pts',(15.2053629424752,-5.89417628539394,99.6921998415835));
#29010=CARTESIAN_POINT('Ctrl Pts',(15.2061565022707,-5.88857599398075,99.6934831334187));
#29011=CARTESIAN_POINT('Ctrl Pts',(15.2069595049574,-5.8829744697482,99.694755268259));
#29012=CARTESIAN_POINT('Ctrl Pts',(15.2273306528143,-5.74087098709944,99.7270276969224));
#29013=CARTESIAN_POINT('Ctrl Pts',(15.2537738297661,-5.59800970804934,99.7521123711275));
#29014=CARTESIAN_POINT('Ctrl Pts',(15.2867992989703,-5.45419637581596,99.7693348591779));
#29015=CARTESIAN_POINT('Ctrl Pts',(15.2874528993659,-5.45135019518315,99.7696757059629));
#29016=CARTESIAN_POINT('Ctrl Pts',(15.2881090485028,-5.44850399099787,99.7700133667743));
#29017=CARTESIAN_POINT('Ctrl Pts',(15.2887677380554,-5.44565779119462,99.7703478403196));
#29018=CARTESIAN_POINT('Ctrl Pts',(15.3138490822596,-5.33728121734784,99.7830838038494));
#29019=CARTESIAN_POINT('Ctrl Pts',(15.3426027352871,-5.22896570119097,99.7911914400879));
#29020=CARTESIAN_POINT('Ctrl Pts',(15.3745952688359,-5.12217525765042,99.794599167712));
#29021=CARTESIAN_POINT('Ctrl Pts',(15.3858966024219,-5.0844516299046,99.795802944418));
#29022=CARTESIAN_POINT('Ctrl Pts',(15.3976023968206,-5.04691831207414,99.7964198693814));
#29023=CARTESIAN_POINT('Ctrl Pts',(15.4096944350009,-5.00964014842565,99.7964455441609));
#29024=CARTESIAN_POINT('Ctrl Pts',(15.4097526805226,-5.00946058514123,99.7964456678325));
#29025=CARTESIAN_POINT('Ctrl Pts',(15.4098109349275,-5.00928102801946,99.7964457777851));
#29026=CARTESIAN_POINT('Ctrl Pts',(15.4098691982134,-5.00910147706791,99.7964458740185));
#29027=CARTESIAN_POINT('Ctrl Pts',(15.4524001546504,-4.87803311071218,99.7965161223064));
#29028=CARTESIAN_POINT('Ctrl Pts',(15.5000808965701,-4.74882134906045,99.789319184275));
#29029=CARTESIAN_POINT('Ctrl Pts',(15.5525709850495,-4.62200967425275,99.7751251055903));
#29030=CARTESIAN_POINT('Ctrl Pts',(15.6056842522913,-4.49369245154328,99.7607625103601));
#29031=CARTESIAN_POINT('Ctrl Pts',(15.6637220710776,-4.36783195161589,99.7392354386457));
#29032=CARTESIAN_POINT('Ctrl Pts',(15.7263585381074,-4.24501089831755,99.7107825845292));
#29033=CARTESIAN_POINT('Ctrl Pts',(15.7366180362518,-4.22489350619505,99.7061221683555));
#29034=CARTESIAN_POINT('Ctrl Pts',(15.7470009608666,-4.20485771382844,99.7012758588297));
#29035=CARTESIAN_POINT('Ctrl Pts',(15.7575059376535,-4.18490615157833,99.6962446073893));
#29036=CARTESIAN_POINT('Ctrl Pts',(15.7603333207192,-4.17953624830441,99.6948904611204));
#29037=CARTESIAN_POINT('Ctrl Pts',(15.7631694550505,-4.174172595838,99.6935229664926));
#29038=CARTESIAN_POINT('Ctrl Pts',(15.7660143095013,-4.16881525076341,99.6921421453944));
#29039=CARTESIAN_POINT('Ctrl Pts',(15.8523453647812,-4.00623918165834,99.650239213408));
#29040=CARTESIAN_POINT('Ctrl Pts',(15.9459575594927,-3.85094811953142,99.5964381240503));
#29041=CARTESIAN_POINT('Ctrl Pts',(16.0446983469592,-3.70416010844114,99.5332547182168));
#29042=CARTESIAN_POINT('Ctrl Pts',(16.1016422040798,-3.61950739556519,99.4968168192847));
#29043=CARTESIAN_POINT('Ctrl Pts',(16.1602914485011,-3.53768342251801,99.4572586815263));
#29044=CARTESIAN_POINT('Ctrl Pts',(16.220229714002,-3.45892855318715,99.4150655759483));
#29045=CARTESIAN_POINT('Ctrl Pts',(16.2263505132199,-3.45088623266648,99.4107568839055));
#29046=CARTESIAN_POINT('Ctrl Pts',(16.232484310626,-3.44287636886379,99.4064210546895));
#29047=CARTESIAN_POINT('Ctrl Pts',(16.2386307267991,-3.43489911689133,99.4020585662805));
#29048=CARTESIAN_POINT('Ctrl Pts',(16.3058910028129,-3.34760399166822,99.3543198245105));
#29049=CARTESIAN_POINT('Ctrl Pts',(16.3750790005579,-3.26361367413128,99.3031450764307));
#29050=CARTESIAN_POINT('Ctrl Pts',(16.4459839896695,-3.1827936689224,99.2489133667459));
#29051=CARTESIAN_POINT('Ctrl Pts',(16.5207937966085,-3.09752281475197,99.1916950555618));
#29052=CARTESIAN_POINT('Ctrl Pts',(16.5975155631267,-3.01578072199172,99.1310729372442));
#29053=CARTESIAN_POINT('Ctrl Pts',(16.675914997693,-2.93745755640269,99.0674634405922));
#29054=CARTESIAN_POINT('Ctrl Pts',(16.7020156295919,-2.91138231586673,99.0462866544767));
#29055=CARTESIAN_POINT('Ctrl Pts',(16.7283022642583,-2.88568641274665,99.0247785979286));
#29056=CARTESIAN_POINT('Ctrl Pts',(16.7547663508274,-2.86036698978117,99.0029542627802));
#29057=CARTESIAN_POINT('Ctrl Pts',(16.815348193217,-2.80240552236074,98.9529937841231));
#29058=CARTESIAN_POINT('Ctrl Pts',(16.8765673950423,-2.74668841444027,98.901619256025));
#29059=CARTESIAN_POINT('Ctrl Pts',(16.9384055914977,-2.69304838623452,98.8489571073828));
#29060=CARTESIAN_POINT('Ctrl Pts',(17.0035287415365,-2.6365589055387,98.7934974529301));
#29061=CARTESIAN_POINT('Ctrl Pts',(17.0693390083717,-2.58237266537445,98.7366089356605));
#29062=CARTESIAN_POINT('Ctrl Pts',(17.1358266349136,-2.5303463992957,98.6784119085632));
#29063=CARTESIAN_POINT('Ctrl Pts',(17.2023142614554,-2.47832013321695,98.6202148814659));
#29064=CARTESIAN_POINT('Ctrl Pts',(17.2694800239625,-2.42845385999314,98.5607082197096));
#29065=CARTESIAN_POINT('Ctrl Pts',(17.337314796066,-2.38065715175364,98.5000007932762));
#29066=CARTESIAN_POINT('',(16.,-1.95943487863577E-15,100.));
#29067=CARTESIAN_POINT('Ctrl Pts',(17.3373139553419,2.38065609737472,98.500000610284));
#29068=CARTESIAN_POINT('Ctrl Pts',(17.1369255782473,2.52182806773904,98.6793214334492));
#29069=CARTESIAN_POINT('Ctrl Pts',(16.9408142894144,2.68207058023465,98.8494491913713));
#29070=CARTESIAN_POINT('Ctrl Pts',(16.5665886131438,3.04035068852609,99.1580199459299));
#29071=CARTESIAN_POINT('Ctrl Pts',(16.3880897672633,3.23827359237263,99.2969308183713));
#29072=CARTESIAN_POINT('Ctrl Pts',(16.1353354438601,3.57049167360207,99.4748187550338));
#29073=CARTESIAN_POINT('Ctrl Pts',(16.0533461943871,3.68769759561264,99.5290970577315));
#29074=CARTESIAN_POINT('Ctrl Pts',(15.8988420094756,3.92971331391083,99.62326558462));
#29075=CARTESIAN_POINT('Ctrl Pts',(15.8258543348747,4.05507112943761,99.6635148733605));
#29076=CARTESIAN_POINT('Ctrl Pts',(15.6204716288236,4.44517628877436,99.7618768897715));
#29077=CARTESIAN_POINT('Ctrl Pts',(15.5009169261858,4.72778423157193,99.7968963262704));
#29078=CARTESIAN_POINT('Ctrl Pts',(15.3625027879858,5.15544462350693,99.7962149169054));
#29079=CARTESIAN_POINT('Ctrl Pts',(15.3226163289905,5.29947071769255,99.7875063317089));
#29080=CARTESIAN_POINT('Ctrl Pts',(15.2552379735104,5.59044609999894,99.753358404991));
#29081=CARTESIAN_POINT('Ctrl Pts',(15.2275889932189,5.73867088412122,99.7275975989373));
#29082=CARTESIAN_POINT('Ctrl Pts',(15.1648439881543,6.17754507098126,99.6277174576398));
#29083=CARTESIAN_POINT('Ctrl Pts',(15.14939224423,6.46047984853023,99.5324632749564));
#29084=CARTESIAN_POINT('Ctrl Pts',(15.1616921671213,7.01143925344932,99.2974531785354));
#29085=CARTESIAN_POINT('Ctrl Pts',(15.1901642928368,7.2812889092902,99.15615753822));
#29086=CARTESIAN_POINT('Ctrl Pts',(15.2826489099606,7.7909577462157,98.8472990531188));
#29087=CARTESIAN_POINT('Ctrl Pts',(15.3464734888,8.03297087257739,98.6790582739388));
#29088=CARTESIAN_POINT('Ctrl Pts',(15.4254964096654,8.26462691495157,98.5000000706303));
#29089=CARTESIAN_POINT('Ctrl Pts',(12.6268663212259,12.1166104449801,98.5000000648703));
#29090=CARTESIAN_POINT('Ctrl Pts',(12.5446458775159,12.1154191815706,98.5601503317549));
#29091=CARTESIAN_POINT('Ctrl Pts',(12.4615341179539,12.1162591862567,98.6192693642198));
#29092=CARTESIAN_POINT('Ctrl Pts',(12.3777014366889,12.1192061781927,98.677108972024));
#29093=CARTESIAN_POINT('Ctrl Pts',(12.2915741224031,12.1222338339571,98.736531741335));
#29094=CARTESIAN_POINT('Ctrl Pts',(12.2046849295102,12.1274848184563,98.7946054581518));
#29095=CARTESIAN_POINT('Ctrl Pts',(12.1171781716405,12.1350769190419,98.8510630179462));
#29096=CARTESIAN_POINT('Ctrl Pts',(12.0477278725848,12.1411024383157,98.8958709220112));
#29097=CARTESIAN_POINT('Ctrl Pts',(11.9778875805386,12.1486032210661,98.9396611167267));
#29098=CARTESIAN_POINT('Ctrl Pts',(11.9077182330858,12.1576571523016,98.9822921355009));
#29099=CARTESIAN_POINT('Ctrl Pts',(11.8959551442279,12.1591749403601,98.9894387384001));
#29100=CARTESIAN_POINT('Ctrl Pts',(11.8841835086263,12.1607351471293,98.9965533320493));
#29101=CARTESIAN_POINT('Ctrl Pts',(11.8724026494821,12.1623382885866,99.0036357543384));
#29102=CARTESIAN_POINT('Ctrl Pts',(11.7229964865901,12.1826695064354,99.0934558196869));
#29103=CARTESIAN_POINT('Ctrl Pts',(11.5723364226954,12.2098752719653,99.17796211997));
#29104=CARTESIAN_POINT('Ctrl Pts',(11.4201636564221,12.2447803501146,99.2562190949067));
#29105=CARTESIAN_POINT('Ctrl Pts',(11.3200139902322,12.2677524758806,99.3077224624861));
#29106=CARTESIAN_POINT('Ctrl Pts',(11.2192092247972,12.2940588049852,99.3565196705271));
#29107=CARTESIAN_POINT('Ctrl Pts',(11.1176771661422,12.3239257557741,99.402352828103));
#29108=CARTESIAN_POINT('Ctrl Pts',(11.1083271026094,12.3266761962862,99.4065735928636));
#29109=CARTESIAN_POINT('Ctrl Pts',(11.0989693146526,12.3294584306971,99.4107687371794));
#29110=CARTESIAN_POINT('Ctrl Pts',(11.0896044489173,12.3322723840617,99.4149377803029));
#29111=CARTESIAN_POINT('Ctrl Pts',(10.9368635548845,12.3781679435737,99.4829348442163));
#29112=CARTESIAN_POINT('Ctrl Pts',(10.782180778293,12.4325386244882,99.5439998059348));
#29113=CARTESIAN_POINT('Ctrl Pts',(10.6282589264101,12.4951094361626,99.5960759478411));
#29114=CARTESIAN_POINT('Ctrl Pts',(10.5197442277713,12.5392217742704,99.6327895578719));
#29115=CARTESIAN_POINT('Ctrl Pts',(10.4116066692697,12.5874100607449,99.6650361416488));
#29116=CARTESIAN_POINT('Ctrl Pts',(10.3047803019273,12.6395820517603,99.6921021736601));
#29117=CARTESIAN_POINT('Ctrl Pts',(10.2996691247951,12.6420782546553,99.6933971655926));
#29118=CARTESIAN_POINT('Ctrl Pts',(10.2945597086435,12.6445839057491,99.6946809027462));
#29119=CARTESIAN_POINT('Ctrl Pts',(10.2894520568858,12.6470990367868,99.6959533416378));
#29120=CARTESIAN_POINT('Ctrl Pts',(10.1603732160566,12.7106605743163,99.7281099852292));
#29121=CARTESIAN_POINT('Ctrl Pts',(10.0324732032076,12.780246063646,99.7530425577929));
#29122=CARTESIAN_POINT('Ctrl Pts',(9.9057096702643,12.8564220781232,99.7700686162087));
#29123=CARTESIAN_POINT('Ctrl Pts',(9.78852854272624,12.9268397373706,99.7858076278658));
#29124=CARTESIAN_POINT('Ctrl Pts',(9.67313030478594,13.0025204955551,99.7945520991889));
#29125=CARTESIAN_POINT('Ctrl Pts',(9.56184140661172,13.0818662611236,99.796170916244));
#29126=CARTESIAN_POINT('Ctrl Pts',(9.54796066113928,13.0917628311701,99.796372826658));
#29127=CARTESIAN_POINT('Ctrl Pts',(9.53414386525613,13.1017164514157,99.7964638312962));
#29128=CARTESIAN_POINT('Ctrl Pts',(9.52039555682251,13.1117240463958,99.7964436301271));
#29129=CARTESIAN_POINT('Ctrl Pts',(9.52026709963196,13.1118175522654,99.7964434413777));
#29130=CARTESIAN_POINT('Ctrl Pts',(9.52013864842912,13.1119110628399,99.7964432429205));
#29131=CARTESIAN_POINT('Ctrl Pts',(9.5200102032178,13.1120045781168,99.7964430347553));
#29132=CARTESIAN_POINT('Ctrl Pts',(9.39854187906108,13.2004402920585,99.7962461766987));
#29133=CARTESIAN_POINT('Ctrl Pts',(9.28143127084364,13.2936651206149,99.7875210116457));
#29134=CARTESIAN_POINT('Ctrl Pts',(9.16861451193004,13.3916016257416,99.7704440514027));
#29135=CARTESIAN_POINT('Ctrl Pts',(9.16621596908919,13.3936838066648,99.7700809863659));
#29136=CARTESIAN_POINT('Ctrl Pts',(9.16381939232447,13.3957680959599,99.7697141495905));
#29137=CARTESIAN_POINT('Ctrl Pts',(9.16142477903297,13.3978544944896,99.7693435426229));
#29138=CARTESIAN_POINT('Ctrl Pts',(9.075472786598,13.4727434593481,99.7560410159087));
#29139=CARTESIAN_POINT('Ctrl Pts',(8.9915392884372,13.5509036747022,99.7376874829802));
#29140=CARTESIAN_POINT('Ctrl Pts',(8.91103700497453,13.6308471452239,99.71483060684));
#29141=CARTESIAN_POINT('Ctrl Pts',(8.88817991972763,13.6535455662134,99.7083408335821));
#29142=CARTESIAN_POINT('Ctrl Pts',(8.86559966114202,13.6763878101702,99.7014877883411));
#29143=CARTESIAN_POINT('Ctrl Pts',(8.84332918088663,13.699339853188,99.6942835087751));
#29144=CARTESIAN_POINT('Ctrl Pts',(8.83915122841399,13.7036456671525,99.6929319825717));
#29145=CARTESIAN_POINT('Ctrl Pts',(8.83498423109471,13.7079552668881,99.6915681321738));
#29146=CARTESIAN_POINT('Ctrl Pts',(8.83082841847454,13.7122684141791,99.690192042067));
#29147=CARTESIAN_POINT('Ctrl Pts',(8.69127076550717,13.8571095722995,99.6439811266265));
#29148=CARTESIAN_POINT('Ctrl Pts',(8.56417600488204,14.0055185195395,99.5845379974113));
#29149=CARTESIAN_POINT('Ctrl Pts',(8.44794279484853,14.1572127319379,99.5138249398355));
#29150=CARTESIAN_POINT('Ctrl Pts',(8.3971544618688,14.2234958206366,99.4829267282733));
#29151=CARTESIAN_POINT('Ctrl Pts',(8.34843948385405,14.2904060702255,99.449877297544));
#29152=CARTESIAN_POINT('Ctrl Pts',(8.30166232922778,14.357919515952,99.4148427913138));
#29153=CARTESIAN_POINT('Ctrl Pts',(8.29602633367796,14.3660539457331,99.4106216213264));
#29154=CARTESIAN_POINT('Ctrl Pts',(8.2904184545012,14.3741972107076,99.4063715743575));
#29155=CARTESIAN_POINT('Ctrl Pts',(8.28483845220997,14.3823492736635,99.4020929385903));
#29156=CARTESIAN_POINT('Ctrl Pts',(8.19855951864144,14.5083978416577,99.335935953009));
#29157=CARTESIAN_POINT('Ctrl Pts',(8.118904797062,14.6370031608596,99.2625264797961));
#29158=CARTESIAN_POINT('Ctrl Pts',(8.04618036366085,14.7663488923838,99.1837466668257));
#29159=CARTESIAN_POINT('Ctrl Pts',(7.99257245589043,14.8616944828788,99.1256751116361));
#29160=CARTESIAN_POINT('Ctrl Pts',(7.94273055715436,14.9574417704619,99.0646859940753));
#29161=CARTESIAN_POINT('Ctrl Pts',(7.89678243508475,15.052850115494,99.0015448475647));
#29162=CARTESIAN_POINT('Ctrl Pts',(7.89164895202107,15.0635094656762,98.9944905003654));
#29163=CARTESIAN_POINT('Ctrl Pts',(7.88656339890024,15.074165771925,98.9874085551184));
#29164=CARTESIAN_POINT('Ctrl Pts',(7.8815260287386,15.0848179083459,98.9803001233706));
#29165=CARTESIAN_POINT('Ctrl Pts',(7.82583177602524,15.2025902297611,98.9017077663553));
#29166=CARTESIAN_POINT('Ctrl Pts',(7.7755690708679,15.3204628413966,98.8195805047748));
#29167=CARTESIAN_POINT('Ctrl Pts',(7.73037835310887,15.4384372753898,98.734324448814));
#29168=CARTESIAN_POINT('Ctrl Pts',(7.69023139126286,15.543244530844,98.6585838588093));
#29169=CARTESIAN_POINT('Ctrl Pts',(7.65408652107099,15.6481322437467,98.5803745642654));
#29170=CARTESIAN_POINT('Ctrl Pts',(7.6216630381314,15.7531031392177,98.5000003292224));
#29171=CARTESIAN_POINT('Ctrl Pts',(3.09338453344266,17.2244295663994,98.5000000648311));
#29172=CARTESIAN_POINT('Ctrl Pts',(3.02757828974897,17.1751462307692,98.5601400874492));
#29173=CARTESIAN_POINT('Ctrl Pts',(2.95985810192091,17.1269821149717,98.6192489818104));
#29174=CARTESIAN_POINT('Ctrl Pts',(2.89031680997714,17.0800983770372,98.6770789350014));
#29175=CARTESIAN_POINT('Ctrl Pts',(2.81887677757202,17.0319345356173,98.7364878647822));
#29176=CARTESIAN_POINT('Ctrl Pts',(2.74551440919362,16.9851209165041,98.7945484303274));
#29177=CARTESIAN_POINT('Ctrl Pts',(2.67027667614573,16.9398373505462,98.8509939558017));
#29178=CARTESIAN_POINT('Ctrl Pts',(2.6109349856159,16.9041211846239,98.8955138099865));
#29179=CARTESIAN_POINT('Ctrl Pts',(2.55042549403234,16.8693567660988,98.9390292514817));
#29180=CARTESIAN_POINT('Ctrl Pts',(2.4887514391056,16.8356409267848,98.981401669026));
#29181=CARTESIAN_POINT('Ctrl Pts',(2.47837258935323,16.8299670395897,98.9885323328985));
#29182=CARTESIAN_POINT('Ctrl Pts',(2.46796207659617,16.8243222949697,98.9956311576658));
#29183=CARTESIAN_POINT('Ctrl Pts',(2.45751905733814,16.8187067111523,99.0026979840552));
#29184=CARTESIAN_POINT('Ctrl Pts',(2.3257682405814,16.747859599199,99.0918542065687));
#29185=CARTESIAN_POINT('Ctrl Pts',(2.18904054560583,16.6817605361993,99.1757821759419));
#29186=CARTESIAN_POINT('Ctrl Pts',(2.04666245349801,16.6209127925103,99.2535679558014));
#29187=CARTESIAN_POINT('Ctrl Pts',(1.95157045769963,16.580273581087,99.3055198041657));
#29188=CARTESIAN_POINT('Ctrl Pts',(1.85395846778332,16.5419763524922,99.3547324640608));
#29189=CARTESIAN_POINT('Ctrl Pts',(1.75363255973655,16.5061646105046,99.4009428779258));
#29190=CARTESIAN_POINT('Ctrl Pts',(1.7444895081828,16.5029009609688,99.4051541948679));
#29191=CARTESIAN_POINT('Ctrl Pts',(1.73532163166429,16.4996582923134,99.4093401456669));
#29192=CARTESIAN_POINT('Ctrl Pts',(1.72612949566268,16.4964369225345,99.4135002521257));
#29193=CARTESIAN_POINT('Ctrl Pts',(1.5760794254653,16.4438521085836,99.4814087628433));
#29194=CARTESIAN_POINT('Ctrl Pts',(1.41948863873315,16.3969359400961,99.5424448371047));
#29195=CARTESIAN_POINT('Ctrl Pts',(1.25870385084095,16.3570529365087,99.5945560958869));
#29196=CARTESIAN_POINT('Ctrl Pts',(1.14513996001324,16.3288831753973,99.6313627949585));
#29197=CARTESIAN_POINT('Ctrl Pts',(1.0294828057723,16.3042216818488,99.6637177718581));
#29198=CARTESIAN_POINT('Ctrl Pts',(0.912546551574139,16.2835445868269,99.6909054353086));
#29199=CARTESIAN_POINT('Ctrl Pts',(0.906979209552398,16.2825601491023,99.6921998415835));
#29200=CARTESIAN_POINT('Ctrl Pts',(0.901407792447871,16.2815842840968,99.6934831334187));
#29201=CARTESIAN_POINT('Ctrl Pts',(0.89583228484858,16.2806170188524,99.694755268259));
#29202=CARTESIAN_POINT('Ctrl Pts',(0.754388810804532,16.2560787406678,99.7270276969224));
#29203=CARTESIAN_POINT('Ctrl Pts',(0.610348269374317,16.2370811333546,99.7521123711276));
#29204=CARTESIAN_POINT('Ctrl Pts',(0.463368231392301,16.2240494573673,99.7693348591779));
#29205=CARTESIAN_POINT('Ctrl Pts',(0.460459379125142,16.223791550098,99.7696757059629));
#29206=CARTESIAN_POINT('Ctrl Pts',(0.457549716853904,16.2235360595475,99.7700133667742));
#29207=CARTESIAN_POINT('Ctrl Pts',(0.454639273718568,16.2232829864302,99.7703478403196));
#29208=CARTESIAN_POINT('Ctrl Pts',(0.343816465319919,16.2136465591599,99.7830838038524));
#29209=CARTESIAN_POINT('Ctrl Pts',(0.231916920399598,16.2075215729917,99.7911914400916));
#29210=CARTESIAN_POINT('Ctrl Pts',(0.12046693660562,16.2049482186064,99.7945991677142));
#29211=CARTESIAN_POINT('Ctrl Pts',(0.0810973305097992,16.2040391834944,
99.7958029444185));
#29212=CARTESIAN_POINT('Ctrl Pts',(0.0417837346343648,16.2035736224715,
99.796419869381));
#29213=CARTESIAN_POINT('Ctrl Pts',(0.00259344891369449,16.2035542480916,
99.7964455441606));
#29214=CARTESIAN_POINT('Ctrl Pts',(0.00240467522589664,16.2035541547682,
99.7964456678321));
#29215=CARTESIAN_POINT('Ctrl Pts',(0.00221590465408674,16.2035540717975,
99.7964457777848));
#29216=CARTESIAN_POINT('Ctrl Pts',(0.00202713720612241,16.2035539991798,
99.7964458740181));
#29217=CARTESIAN_POINT('Ctrl Pts',(-0.135769074962828,16.2035009898145,
99.7965161223062));
#29218=CARTESIAN_POINT('Ctrl Pts',(-0.273390922361444,16.2089194398907,
99.789319184281));
#29219=CARTESIAN_POINT('Ctrl Pts',(-0.410216321347207,16.21965351797,99.7751251056086));
#29220=CARTESIAN_POINT('Ctrl Pts',(-0.548666154289857,16.2305150343835,
99.760762510392));
#29221=CARTESIAN_POINT('Ctrl Pts',(-0.686301275139974,16.2468192467176,
99.7392354386988));
#29222=CARTESIAN_POINT('Ctrl Pts',(-0.822466770928219,16.2684362740861,
99.7107825846107));
#29223=CARTESIAN_POINT('Ctrl Pts',(-0.844769907208554,16.2719770206209,
99.7061221684119));
#29224=CARTESIAN_POINT('Ctrl Pts',(-0.86703357838578,16.2756603684177,99.7012758588589));
#29225=CARTESIAN_POINT('Ctrl Pts',(-0.889254858156722,16.2794858232671,
99.6962446073891));
#29226=CARTESIAN_POINT('Ctrl Pts',(-0.895235649074178,16.280515432986,99.6948904611201));
#29227=CARTESIAN_POINT('Ctrl Pts',(-0.901213199410201,16.2815552972589,
99.6935229664924));
#29228=CARTESIAN_POINT('Ctrl Pts',(-0.907187445725255,16.2826054039494,
99.6921421453942));
#29229=CARTESIAN_POINT('Ctrl Pts',(-1.08848423857813,16.3144723483492,99.6502392134744));
#29230=CARTESIAN_POINT('Ctrl Pts',(-1.26510257391078,16.355515258783,99.5964381242207));
#29231=CARTESIAN_POINT('Ctrl Pts',(-1.43521884948873,16.4040633380291,99.5332547185169));
#29232=CARTESIAN_POINT('Ctrl Pts',(-1.53332498354818,16.4320610375712,99.4968168195019));
#29233=CARTESIAN_POINT('Ctrl Pts',(-1.62926781980758,16.4625547855127,99.4572586816421));
#29234=CARTESIAN_POINT('Ctrl Pts',(-1.72269009438418,16.4952228705693,99.4150655759484));
#29235=CARTESIAN_POINT('Ctrl Pts',(-1.73223022669901,16.4985588828354,99.4107568839055));
#29236=CARTESIAN_POINT('Ctrl Pts',(-1.74174350750173,16.5019172867905,99.4064210546896));
#29237=CARTESIAN_POINT('Ctrl Pts',(-1.75122967202423,16.5052977695158,99.4020585662806));
#29238=CARTESIAN_POINT('Ctrl Pts',(-1.85503683804354,16.5422904160868,99.3543198245104));
#29239=CARTESIAN_POINT('Ctrl Pts',(-1.95629664395312,16.58213767671,99.3031450764302));
#29240=CARTESIAN_POINT('Ctrl Pts',(-2.05507188317586,16.6245975735477,99.248913366745));
#29241=CARTESIAN_POINT('Ctrl Pts',(-2.15928678637812,16.669395784858,99.1916950555588));
#29242=CARTESIAN_POINT('Ctrl Pts',(-2.26073646604907,16.71710282503,99.1310729372389));
#29243=CARTESIAN_POINT('Ctrl Pts',(-2.35945298069274,16.7674619289298,99.0674634405845));
#29244=CARTESIAN_POINT('Ctrl Pts',(-2.39231754693524,16.7842274125169,99.0462866544713));
#29245=CARTESIAN_POINT('Ctrl Pts',(-2.4248788198727,16.801287016956,99.0247785979255));
#29246=CARTESIAN_POINT('Ctrl Pts',(-2.45713687455959,16.8186317269493,99.0029542627797));
#29247=CARTESIAN_POINT('Ctrl Pts',(-2.53098232468997,16.8583374044698,98.9529937841244));
#29248=CARTESIAN_POINT('Ctrl Pts',(-2.60289021699031,16.8993427920618,98.9016192560283));
#29249=CARTESIAN_POINT('Ctrl Pts',(-2.67301396895339,16.9415787314606,98.8489571073882));
#29250=CARTESIAN_POINT('Ctrl Pts',(-2.74686281776194,16.9860583181289,98.7934974529346));
#29251=CARTESIAN_POINT('Ctrl Pts',(-2.81873348542151,17.0319031321703,98.7366089356642));
#29252=CARTESIAN_POINT('Ctrl Pts',(-2.88875921131269,17.0790596222744,98.678411908566));
#29253=CARTESIAN_POINT('Ctrl Pts',(-2.95878493720387,17.1262161123785,98.6202148814678));
#29254=CARTESIAN_POINT('Ctrl Pts',(-3.02696594335296,17.1746850226112,98.5607082197105));
#29255=CARTESIAN_POINT('Ctrl Pts',(-3.0933854115725,17.2244297295311,98.5000007932762));
#29256=CARTESIAN_POINT('Origin',(-1.04083408558608E-14,0.,42.));
#29257=CARTESIAN_POINT('',(-11.35,-1.38997411703225E-15,42.));
#29258=CARTESIAN_POINT('Origin',(0.,0.,42.));
#29259=CARTESIAN_POINT('Origin',(0.,0.,0.));
#29260=CARTESIAN_POINT('',(-11.35,-1.38997411703225E-15,0.));
#29261=CARTESIAN_POINT('',(8.09660750783269,7.95408365961204,125.));
#29262=CARTESIAN_POINT('',(5.06279377892661,10.1582783557088,125.));
#29263=CARTESIAN_POINT('Ctrl Pts',(8.09660750783269,7.95408365961205,125.));
#29264=CARTESIAN_POINT('Ctrl Pts',(8.09660750783269,7.95408365961205,124.764102516373));
#29265=CARTESIAN_POINT('Ctrl Pts',(8.06323161817317,7.98850304917249,124.512783030785));
#29266=CARTESIAN_POINT('Ctrl Pts',(7.92569717624602,8.12497441557712,124.050953500858));
#29267=CARTESIAN_POINT('Ctrl Pts',(7.82129658482452,8.22665391752821,123.840405577283));
#29268=CARTESIAN_POINT('Ctrl Pts',(7.5753171261144,8.45370238070912,123.507948276706));
#29269=CARTESIAN_POINT('Ctrl Pts',(7.41718720317046,8.59426386648911,123.363717352429));
#29270=CARTESIAN_POINT('Ctrl Pts',(7.06076432561089,8.88941193496231,123.172231355143));
#29271=CARTESIAN_POINT('Ctrl Pts',(6.86220276900426,9.04368939714487,123.125));
#29272=CARTESIAN_POINT('Ctrl Pts',(6.48052245803477,9.32099637516652,123.125));
#29273=CARTESIAN_POINT('Ctrl Pts',(6.27243697688758,9.46216527979951,123.172231355143));
#29274=CARTESIAN_POINT('Ctrl Pts',(5.88159375674427,9.70993781104404,123.363717352429));
#29275=CARTESIAN_POINT('Ctrl Pts',(5.69904700624421,9.81689241682052,123.507948276706));
#29276=CARTESIAN_POINT('Ctrl Pts',(5.40709925281262,9.98067095023192,123.840405577283));
#29277=CARTESIAN_POINT('Ctrl Pts',(5.27813474293636,10.0485411189259,124.050953500858));
#29278=CARTESIAN_POINT('Ctrl Pts',(5.10584228076216,10.1371721746712,124.512783030785));
#29279=CARTESIAN_POINT('Ctrl Pts',(5.06279377892663,10.1582783557088,124.764102516373));
#29280=CARTESIAN_POINT('Ctrl Pts',(5.06279377892663,10.1582783557088,125.));
#29281=CARTESIAN_POINT('Ctrl Pts',(5.06279377892663,10.1582783557088,125.));
#29282=CARTESIAN_POINT('Ctrl Pts',(5.06279377892663,10.1582783557088,125.235897483627));
#29283=CARTESIAN_POINT('Ctrl Pts',(5.10584228076216,10.1371721746712,125.487216969215));
#29284=CARTESIAN_POINT('Ctrl Pts',(5.27813474293636,10.0485411189259,125.949046499142));
#29285=CARTESIAN_POINT('Ctrl Pts',(5.40709925281262,9.98067095023192,126.159594422717));
#29286=CARTESIAN_POINT('Ctrl Pts',(5.69904700624421,9.81689241682052,126.492051723294));
#29287=CARTESIAN_POINT('Ctrl Pts',(5.88159375674427,9.70993781104404,126.636282647571));
#29288=CARTESIAN_POINT('Ctrl Pts',(6.27243697688758,9.46216527979951,126.827768644857));
#29289=CARTESIAN_POINT('Ctrl Pts',(6.48052245803477,9.32099637516652,126.875));
#29290=CARTESIAN_POINT('Ctrl Pts',(6.86220276900426,9.04368939714487,126.875));
#29291=CARTESIAN_POINT('Ctrl Pts',(7.06076432561089,8.88941193496232,126.827768644857));
#29292=CARTESIAN_POINT('Ctrl Pts',(7.41718720317046,8.59426386648911,126.636282647571));
#29293=CARTESIAN_POINT('Ctrl Pts',(7.5753171261144,8.45370238070912,126.492051723294));
#29294=CARTESIAN_POINT('Ctrl Pts',(7.82129658482452,8.22665391752821,126.159594422717));
#29295=CARTESIAN_POINT('Ctrl Pts',(7.92569717624602,8.12497441557712,125.949046499142));
#29296=CARTESIAN_POINT('Ctrl Pts',(8.06323161817317,7.98850304917249,125.487216969215));
#29297=CARTESIAN_POINT('Ctrl Pts',(8.09660750783269,7.95408365961205,125.235897483627));
#29298=CARTESIAN_POINT('Ctrl Pts',(8.09660750783269,7.95408365961205,125.));
#29299=CARTESIAN_POINT('',(-5.06279377892678,10.1582783557087,125.));
#29300=CARTESIAN_POINT('',(-8.09660750783278,7.95408365961186,125.));
#29301=CARTESIAN_POINT('Ctrl Pts',(-5.06279377892678,10.1582783557087,125.));
#29302=CARTESIAN_POINT('Ctrl Pts',(-5.06279377892679,10.1582783557087,124.764102516373));
#29303=CARTESIAN_POINT('Ctrl Pts',(-5.10584228076231,10.1371721746711,124.512783030785));
#29304=CARTESIAN_POINT('Ctrl Pts',(-5.27813474293652,10.0485411189258,124.050953500858));
#29305=CARTESIAN_POINT('Ctrl Pts',(-5.40709925281278,9.98067095023182,123.840405577283));
#29306=CARTESIAN_POINT('Ctrl Pts',(-5.69904700624437,9.81689241682041,123.507948276706));
#29307=CARTESIAN_POINT('Ctrl Pts',(-5.88159375674444,9.70993781104394,123.363717352429));
#29308=CARTESIAN_POINT('Ctrl Pts',(-6.27243697688773,9.46216527979941,123.172231355143));
#29309=CARTESIAN_POINT('Ctrl Pts',(-6.48052245803492,9.3209963751664,123.125));
#29310=CARTESIAN_POINT('Ctrl Pts',(-6.86220276900441,9.04368939714475,123.125));
#29311=CARTESIAN_POINT('Ctrl Pts',(-7.06076432561104,8.8894119349622,123.172231355143));
#29312=CARTESIAN_POINT('Ctrl Pts',(-7.4171872031706,8.59426386648899,123.363717352429));
#29313=CARTESIAN_POINT('Ctrl Pts',(-7.57531712611454,8.45370238070899,123.507948276706));
#29314=CARTESIAN_POINT('Ctrl Pts',(-7.82129658482466,8.22665391752808,123.840405577283));
#29315=CARTESIAN_POINT('Ctrl Pts',(-7.92569717624616,8.12497441557699,124.050953500858));
#29316=CARTESIAN_POINT('Ctrl Pts',(-8.0632316181733,7.98850304917235,124.512783030785));
#29317=CARTESIAN_POINT('Ctrl Pts',(-8.09660750783282,7.95408365961192,124.764102516373));
#29318=CARTESIAN_POINT('Ctrl Pts',(-8.09660750783282,7.95408365961192,125.));
#29319=CARTESIAN_POINT('Ctrl Pts',(-8.09660750783282,7.95408365961192,125.));
#29320=CARTESIAN_POINT('Ctrl Pts',(-8.09660750783281,7.95408365961192,125.235897483627));
#29321=CARTESIAN_POINT('Ctrl Pts',(-8.0632316181733,7.98850304917235,125.487216969215));
#29322=CARTESIAN_POINT('Ctrl Pts',(-7.92569717624616,8.12497441557699,125.949046499142));
#29323=CARTESIAN_POINT('Ctrl Pts',(-7.82129658482466,8.22665391752808,126.159594422717));
#29324=CARTESIAN_POINT('Ctrl Pts',(-7.57531712611454,8.45370238070899,126.492051723294));
#29325=CARTESIAN_POINT('Ctrl Pts',(-7.4171872031706,8.59426386648899,126.636282647571));
#29326=CARTESIAN_POINT('Ctrl Pts',(-7.06076432561104,8.8894119349622,126.827768644857));
#29327=CARTESIAN_POINT('Ctrl Pts',(-6.86220276900441,9.04368939714475,126.875));
#29328=CARTESIAN_POINT('Ctrl Pts',(-6.48052245803492,9.3209963751664,126.875));
#29329=CARTESIAN_POINT('Ctrl Pts',(-6.27243697688773,9.46216527979941,126.827768644857));
#29330=CARTESIAN_POINT('Ctrl Pts',(-5.88159375674444,9.70993781104394,126.636282647571));
#29331=CARTESIAN_POINT('Ctrl Pts',(-5.69904700624437,9.81689241682041,126.492051723294));
#29332=CARTESIAN_POINT('Ctrl Pts',(-5.40709925281278,9.98067095023182,126.159594422717));
#29333=CARTESIAN_POINT('Ctrl Pts',(-5.27813474293652,10.0485411189258,125.949046499142));
#29334=CARTESIAN_POINT('Ctrl Pts',(-5.10584228076231,10.1371721746711,125.487216969215));
#29335=CARTESIAN_POINT('Ctrl Pts',(-5.06279377892678,10.1582783557087,125.235897483627));
#29336=CARTESIAN_POINT('Ctrl Pts',(-5.06279377892678,10.1582783557087,125.));
#29337=CARTESIAN_POINT('',(-11.2255861412409,-1.67592236860171,125.));
#29338=CARTESIAN_POINT('',(-10.0667724123348,-5.24238430470852,125.));
#29339=CARTESIAN_POINT('Ctrl Pts',(-11.2255861412409,-1.67592236860171,
125.));
#29340=CARTESIAN_POINT('Ctrl Pts',(-11.2255861412409,-1.67592236860171,
124.764102516373));
#29341=CARTESIAN_POINT('Ctrl Pts',(-11.2188156888805,-1.72338609541612,
124.512783030785));
#29342=CARTESIAN_POINT('Ctrl Pts',(-11.1877638445824,-1.91463446673009,
124.050953500858));
#29343=CARTESIAN_POINT('Ctrl Pts',(-11.1630677036069,-2.05826003975628,
123.840405577283));
#29344=CARTESIAN_POINT('Ctrl Pts',(-11.0975218794567,-2.38652920321304,
123.507948276706));
#29345=CARTESIAN_POINT('Ctrl Pts',(-11.0522120528577,-2.59319227061624,
123.363717352429));
#29346=CARTESIAN_POINT('Ctrl Pts',(-10.9373435696191,-3.04147218487716,
123.172231355143));
#29347=CARTESIAN_POINT('Ctrl Pts',(-10.8673859129268,-3.2829968282775,123.125));
#29348=CARTESIAN_POINT('Ctrl Pts',(-10.7215970069731,-3.73168894403405,
123.125));
#29349=CARTESIAN_POINT('Ctrl Pts',(-10.6362293166679,-3.96820656399394,
123.172231355143));
#29350=CARTESIAN_POINT('Ctrl Pts',(-10.4656675492244,-4.39839063326879,
123.363717352429));
#29351=CARTESIAN_POINT('Ctrl Pts',(-10.3808504657421,-4.59221701476649,
123.507948276706));
#29352=CARTESIAN_POINT('Ctrl Pts',(-10.2409263783277,-4.89631921551712,
123.840405577283));
#29353=CARTESIAN_POINT('Ctrl Pts',(-10.1764849823955,-5.02703077237608,
124.050953500858));
#29354=CARTESIAN_POINT('Ctrl Pts',(-10.089193479956,-5.20000577105051,124.512783030785));
#29355=CARTESIAN_POINT('Ctrl Pts',(-10.0667724123348,-5.24238430470852,
124.764102516373));
#29356=CARTESIAN_POINT('Ctrl Pts',(-10.0667724123348,-5.24238430470852,
125.));
#29357=CARTESIAN_POINT('Ctrl Pts',(-10.0667724123348,-5.24238430470852,
125.));
#29358=CARTESIAN_POINT('Ctrl Pts',(-10.0667724123348,-5.24238430470852,
125.235897483627));
#29359=CARTESIAN_POINT('Ctrl Pts',(-10.089193479956,-5.2000057710505,125.487216969215));
#29360=CARTESIAN_POINT('Ctrl Pts',(-10.1764849823955,-5.02703077237607,
125.949046499142));
#29361=CARTESIAN_POINT('Ctrl Pts',(-10.2409263783277,-4.89631921551712,
126.159594422717));
#29362=CARTESIAN_POINT('Ctrl Pts',(-10.3808504657421,-4.59221701476649,
126.492051723294));
#29363=CARTESIAN_POINT('Ctrl Pts',(-10.4656675492244,-4.39839063326879,
126.636282647571));
#29364=CARTESIAN_POINT('Ctrl Pts',(-10.6362293166679,-3.96820656399394,
126.827768644857));
#29365=CARTESIAN_POINT('Ctrl Pts',(-10.7215970069731,-3.73168894403405,
126.875));
#29366=CARTESIAN_POINT('Ctrl Pts',(-10.8673859129268,-3.2829968282775,126.875));
#29367=CARTESIAN_POINT('Ctrl Pts',(-10.9373435696191,-3.04147218487716,
126.827768644857));
#29368=CARTESIAN_POINT('Ctrl Pts',(-11.0522120528577,-2.59319227061624,
126.636282647571));
#29369=CARTESIAN_POINT('Ctrl Pts',(-11.0975218794567,-2.38652920321304,
126.492051723294));
#29370=CARTESIAN_POINT('Ctrl Pts',(-11.1630677036069,-2.05826003975628,
126.159594422717));
#29371=CARTESIAN_POINT('Ctrl Pts',(-11.1877638445824,-1.91463446673009,
125.949046499142));
#29372=CARTESIAN_POINT('Ctrl Pts',(-11.2188156888805,-1.72338609541612,
125.487216969215));
#29373=CARTESIAN_POINT('Ctrl Pts',(-11.2255861412409,-1.67592236860171,
125.235897483627));
#29374=CARTESIAN_POINT('Ctrl Pts',(-11.2255861412409,-1.67592236860171,
125.));
#29375=CARTESIAN_POINT('',(10.0667724123349,-5.24238430470838,125.));
#29376=CARTESIAN_POINT('',(11.2255861412409,-1.67592236860153,125.));
#29377=CARTESIAN_POINT('Ctrl Pts',(10.0667724123349,-5.24238430470838,125.));
#29378=CARTESIAN_POINT('Ctrl Pts',(10.0667724123349,-5.24238430470838,124.764102516373));
#29379=CARTESIAN_POINT('Ctrl Pts',(10.0891934799561,-5.20000577105036,124.512783030785));
#29380=CARTESIAN_POINT('Ctrl Pts',(10.1764849823956,-5.02703077237593,124.050953500858));
#29381=CARTESIAN_POINT('Ctrl Pts',(10.2409263783278,-4.89631921551698,123.840405577283));
#29382=CARTESIAN_POINT('Ctrl Pts',(10.3808504657422,-4.59221701476634,123.507948276706));
#29383=CARTESIAN_POINT('Ctrl Pts',(10.4656675492245,-4.39839063326864,123.363717352429));
#29384=CARTESIAN_POINT('Ctrl Pts',(10.6362293166679,-3.96820656399379,123.172231355143));
#29385=CARTESIAN_POINT('Ctrl Pts',(10.7215970069731,-3.73168894403389,123.125));
#29386=CARTESIAN_POINT('Ctrl Pts',(10.8673859129269,-3.28299682827734,123.125));
#29387=CARTESIAN_POINT('Ctrl Pts',(10.9373435696192,-3.041472184877,123.172231355143));
#29388=CARTESIAN_POINT('Ctrl Pts',(11.0522120528577,-2.59319227061608,123.363717352429));
#29389=CARTESIAN_POINT('Ctrl Pts',(11.0975218794567,-2.38652920321288,123.507948276706));
#29390=CARTESIAN_POINT('Ctrl Pts',(11.163067703607,-2.05826003975611,123.840405577283));
#29391=CARTESIAN_POINT('Ctrl Pts',(11.1877638445825,-1.91463446672993,124.050953500858));
#29392=CARTESIAN_POINT('Ctrl Pts',(11.2188156888806,-1.72338609541595,124.512783030785));
#29393=CARTESIAN_POINT('Ctrl Pts',(11.225586141241,-1.67592236860154,124.764102516373));
#29394=CARTESIAN_POINT('Ctrl Pts',(11.225586141241,-1.67592236860154,125.));
#29395=CARTESIAN_POINT('Ctrl Pts',(11.225586141241,-1.67592236860154,125.));
#29396=CARTESIAN_POINT('Ctrl Pts',(11.225586141241,-1.67592236860154,125.235897483627));
#29397=CARTESIAN_POINT('Ctrl Pts',(11.2188156888806,-1.72338609541595,125.487216969215));
#29398=CARTESIAN_POINT('Ctrl Pts',(11.1877638445825,-1.91463446672993,125.949046499142));
#29399=CARTESIAN_POINT('Ctrl Pts',(11.163067703607,-2.05826003975611,126.159594422717));
#29400=CARTESIAN_POINT('Ctrl Pts',(11.0975218794567,-2.38652920321288,126.492051723294));
#29401=CARTESIAN_POINT('Ctrl Pts',(11.0522120528577,-2.59319227061608,126.636282647571));
#29402=CARTESIAN_POINT('Ctrl Pts',(10.9373435696192,-3.041472184877,126.827768644857));
#29403=CARTESIAN_POINT('Ctrl Pts',(10.8673859129269,-3.28299682827734,126.875));
#29404=CARTESIAN_POINT('Ctrl Pts',(10.7215970069731,-3.73168894403389,126.875));
#29405=CARTESIAN_POINT('Ctrl Pts',(10.6362293166679,-3.96820656399379,126.827768644857));
#29406=CARTESIAN_POINT('Ctrl Pts',(10.4656675492245,-4.39839063326864,126.636282647571));
#29407=CARTESIAN_POINT('Ctrl Pts',(10.3808504657422,-4.59221701476634,126.492051723294));
#29408=CARTESIAN_POINT('Ctrl Pts',(10.2409263783278,-4.89631921551698,126.159594422717));
#29409=CARTESIAN_POINT('Ctrl Pts',(10.1764849823956,-5.02703077237593,125.949046499142));
#29410=CARTESIAN_POINT('Ctrl Pts',(10.0891934799561,-5.20000577105036,125.487216969215));
#29411=CARTESIAN_POINT('Ctrl Pts',(10.0667724123349,-5.24238430470838,125.235897483627));
#29412=CARTESIAN_POINT('Ctrl Pts',(10.0667724123349,-5.24238430470838,125.));
#29413=CARTESIAN_POINT('',(0.,-11.35,126.875));
#29414=CARTESIAN_POINT('',(-4.61755332615425E-16,-11.35,123.125));
#29415=CARTESIAN_POINT('Ctrl Pts',(1.66533453693773E-15,-11.35,126.875));
#29416=CARTESIAN_POINT('Ctrl Pts',(-0.235891405015774,-11.35,126.875));
#29417=CARTESIAN_POINT('Ctrl Pts',(-0.487213095772096,-11.3418984658909,
126.827768644857));
#29418=CARTESIAN_POINT('Ctrl Pts',(-0.949048942792962,-11.3126187736483,
126.636282647571));
#29419=CARTESIAN_POINT('Ctrl Pts',(-1.15959870615561,-11.2918485795503,
126.492051723294));
#29420=CARTESIAN_POINT('Ctrl Pts',(-1.49205600673265,-11.2527456124869,
126.159594422717));
#29421=CARTESIAN_POINT('Ctrl Pts',(-1.63628357112273,-11.2318502953971,
125.949046499142));
#29422=CARTESIAN_POINT('Ctrl Pts',(-1.82776712848652,-11.2022833573772,
125.487216969215));
#29423=CARTESIAN_POINT('Ctrl Pts',(-1.87499999999999,-11.1940553420108,
125.235897483627));
#29424=CARTESIAN_POINT('Ctrl Pts',(-1.87499999999999,-11.1940553420108,
125.));
#29425=CARTESIAN_POINT('Ctrl Pts',(-1.87499999999999,-11.1940553420108,
124.764102516373));
#29426=CARTESIAN_POINT('Ctrl Pts',(-1.82776712848652,-11.2022833573772,
124.512783030785));
#29427=CARTESIAN_POINT('Ctrl Pts',(-1.63628357112274,-11.2318502953971,
124.050953500858));
#29428=CARTESIAN_POINT('Ctrl Pts',(-1.49205600673265,-11.2527456124869,
123.840405577283));
#29429=CARTESIAN_POINT('Ctrl Pts',(-1.15959870615561,-11.2918485795503,
123.507948276706));
#29430=CARTESIAN_POINT('Ctrl Pts',(-0.949048942792962,-11.3126187736483,
123.363717352429));
#29431=CARTESIAN_POINT('Ctrl Pts',(-0.487213095772096,-11.3418984658909,
123.172231355143));
#29432=CARTESIAN_POINT('Ctrl Pts',(-0.235891405015776,-11.35,123.125));
#29433=CARTESIAN_POINT('Ctrl Pts',(-4.85722573273506E-16,-11.35,123.125));
#29434=CARTESIAN_POINT('Ctrl Pts',(1.38777878078145E-16,-11.35,123.125));
#29435=CARTESIAN_POINT('Ctrl Pts',(0.235891405015776,-11.35,123.125));
#29436=CARTESIAN_POINT('Ctrl Pts',(0.487213095772096,-11.3418984658909,
123.172231355143));
#29437=CARTESIAN_POINT('Ctrl Pts',(0.949048942792962,-11.3126187736483,
123.363717352429));
#29438=CARTESIAN_POINT('Ctrl Pts',(1.15959870615561,-11.2918485795503,123.507948276706));
#29439=CARTESIAN_POINT('Ctrl Pts',(1.49205600673265,-11.2527456124869,123.840405577283));
#29440=CARTESIAN_POINT('Ctrl Pts',(1.63628357112274,-11.2318502953971,124.050953500858));
#29441=CARTESIAN_POINT('Ctrl Pts',(1.82776712848652,-11.2022833573772,124.512783030785));
#29442=CARTESIAN_POINT('Ctrl Pts',(1.87499999999999,-11.1940553420108,124.764102516373));
#29443=CARTESIAN_POINT('Ctrl Pts',(1.87499999999999,-11.1940553420108,125.235897483627));
#29444=CARTESIAN_POINT('Ctrl Pts',(1.82776712848652,-11.2022833573772,125.487216969215));
#29445=CARTESIAN_POINT('Ctrl Pts',(1.63628357112274,-11.2318502953971,125.949046499142));
#29446=CARTESIAN_POINT('Ctrl Pts',(1.49205600673265,-11.2527456124869,126.159594422717));
#29447=CARTESIAN_POINT('Ctrl Pts',(1.15959870615561,-11.2918485795503,126.492051723294));
#29448=CARTESIAN_POINT('Ctrl Pts',(0.949048942792963,-11.3126187736483,
126.636282647571));
#29449=CARTESIAN_POINT('Ctrl Pts',(0.487213095772096,-11.3418984658909,
126.827768644857));
#29450=CARTESIAN_POINT('Ctrl Pts',(0.235891405015774,-11.35,126.875));
#29451=CARTESIAN_POINT('Ctrl Pts',(-1.66533453693773E-15,-11.35,126.875));
#29452=CARTESIAN_POINT('Origin',(0.,-106.,125.));
#29453=CARTESIAN_POINT('',(-2.29621274840127E-16,-106.,123.125));
#29454=CARTESIAN_POINT('Origin',(100.811990727286,-32.7558014037442,125.));
#29455=CARTESIAN_POINT('',(101.391397591739,-30.9725704356907,125.));
#29456=CARTESIAN_POINT('Origin',(-100.811990727286,-32.7558014037456,125.));
#29457=CARTESIAN_POINT('',(-100.232583862833,-34.539032371799,125.));
#29458=CARTESIAN_POINT('Origin',(-62.3052367430029,85.7558014037439,125.));
#29459=CARTESIAN_POINT('',(-63.822143607456,84.6537040556955,125.));
#29460=CARTESIAN_POINT('Origin',(62.3052367430017,85.7558014037448,125.));
#29461=CARTESIAN_POINT('',(60.7883298785487,86.8578987517932,125.));
#29462=CARTESIAN_POINT('Origin',(0.,0.,3.75));
#29463=CARTESIAN_POINT('',(15.,-1.83697019872103E-15,2.24999999999999));
#29464=CARTESIAN_POINT('Origin',(0.,0.,2.24999999999999));
#29465=CARTESIAN_POINT('',(15.,-1.83697019872103E-15,3.75));
#29466=CARTESIAN_POINT('Origin',(0.,0.,3.75));
#29467=CARTESIAN_POINT('',(13.5,-1.65327317884892E-15,3.75));
#29468=CARTESIAN_POINT('Origin',(-14.,0.,30.9));
#29469=CARTESIAN_POINT('',(-15.5,-1.8982025386784E-15,30.9));
#29470=CARTESIAN_POINT('Origin',(0.,0.,30.9));
#29471=CARTESIAN_POINT('Origin',(0.,0.,42.));
#29472=CARTESIAN_POINT('',(-15.5,-1.8982025386784E-15,32.8));
#29473=CARTESIAN_POINT('',(-15.5,-1.8982025386784E-15,42.));
#29474=CARTESIAN_POINT('Origin',(0.,0.,32.8));
#29475=CARTESIAN_POINT('Origin',(-14.,0.,32.8));
#29476=CARTESIAN_POINT('Origin',(-12.2482946431511,16.8583313034371,100.));
#29477=CARTESIAN_POINT('',(-8.00253786203375,15.4036548382545,98.2928932187211));
#29478=CARTESIAN_POINT('',(-8.00253786221767,15.4036548377177,0.5));
#29479=CARTESIAN_POINT('',(-8.00253786221767,15.4036548377177,100.));
#29480=CARTESIAN_POINT('',(-12.1768261106186,12.3708569011015,0.5));
#29481=CARTESIAN_POINT('Origin',(-12.2482946431511,16.8583313034371,0.5));
#29482=CARTESIAN_POINT('',(-12.1768414139071,12.3708281240615,98.2929155812438));
#29483=CARTESIAN_POINT('',(-12.1768261106186,12.3708569011015,100.));
#29484=CARTESIAN_POINT('Ctrl Pts',(-12.1768223332082,12.3708569612629,98.2928961772889));
#29485=CARTESIAN_POINT('Ctrl Pts',(-11.9766556305925,12.3740450279548,98.4496670611162));
#29486=CARTESIAN_POINT('Ctrl Pts',(-11.7718386279247,12.390541715911,98.5976778122645));
#29487=CARTESIAN_POINT('Ctrl Pts',(-11.3497031910366,12.455981009676,98.870667594539));
#29488=CARTESIAN_POINT('Ctrl Pts',(-11.1323782772714,12.5051975008586,98.9953666813421));
#29489=CARTESIAN_POINT('Ctrl Pts',(-10.6948166070868,12.6414901598492,99.2055148722619));
#29490=CARTESIAN_POINT('Ctrl Pts',(-10.4709805367995,12.7297564325018,99.2925877229868));
#29491=CARTESIAN_POINT('Ctrl Pts',(-10.0271356237447,12.9505917384117,99.4120512183375));
#29492=CARTESIAN_POINT('Ctrl Pts',(-9.8121776999094,13.0805177296113,99.4431642901975));
#29493=CARTESIAN_POINT('Ctrl Pts',(-9.40304146226852,13.3782342507087,99.4426185746832));
#29494=CARTESIAN_POINT('Ctrl Pts',(-9.20848272501231,13.5474714192234,99.4095817567495));
#29495=CARTESIAN_POINT('Ctrl Pts',(-8.86697618306585,13.8970925183944,99.2902945556315));
#29496=CARTESIAN_POINT('Ctrl Pts',(-8.71497133569482,14.081422575003,99.2037727159813));
#29497=CARTESIAN_POINT('Ctrl Pts',(-8.44923508864959,14.4577600834109,98.9917454068753));
#29498=CARTESIAN_POINT('Ctrl Pts',(-8.33757587869828,14.6461685366907,98.8686812585125));
#29499=CARTESIAN_POINT('Ctrl Pts',(-8.14664284052531,15.024254464469,98.5978506351621));
#29500=CARTESIAN_POINT('Ctrl Pts',(-8.0672915044469,15.2146587124184,98.4493425737989));
#29501=CARTESIAN_POINT('Ctrl Pts',(-8.00253786221767,15.4036548377177,98.2928932188135));
#29502=CARTESIAN_POINT('Origin',(-19.8181570368417,6.43930956430665,100.));
#29503=CARTESIAN_POINT('',(-15.5282646243346,7.75803424826111,98.292893216895));
#29504=CARTESIAN_POINT('',(-15.5282302736771,7.75804480287585,0.5));
#29505=CARTESIAN_POINT('',(-15.5282302736771,7.75804480287585,100.));
#29506=CARTESIAN_POINT('',(-17.122666505727,2.85087466042015,0.5));
#29507=CARTESIAN_POINT('Origin',(-19.8181570368417,6.43930956430665,0.5));
#29508=CARTESIAN_POINT('',(-17.1226921163487,2.85090171197058,98.2928992166646));
#29509=CARTESIAN_POINT('',(-17.122666505727,2.85087466042014,100.));
#29510=CARTESIAN_POINT('Ctrl Pts',(-17.1226921163487,2.85090171197058,98.2928992166646));
#29511=CARTESIAN_POINT('Ctrl Pts',(-17.0341768248206,2.91742750076187,98.3796187467357));
#29512=CARTESIAN_POINT('Ctrl Pts',(-16.9465325507274,2.98842601539338,98.4639979993741));
#29513=CARTESIAN_POINT('Ctrl Pts',(-16.8602662415713,3.06403584549534,98.5451592717705));
#29514=CARTESIAN_POINT('Ctrl Pts',(-16.779093354132,3.13518144437646,98.621528539137));
#29515=CARTESIAN_POINT('Ctrl Pts',(-16.6991399085188,3.21041016146199,98.6950495057339));
#29516=CARTESIAN_POINT('Ctrl Pts',(-16.6208399982642,3.28987088086897,98.7649644149981));
#29517=CARTESIAN_POINT('Ctrl Pts',(-16.5483443892419,3.36344124931553,98.8296965955378));
#29518=CARTESIAN_POINT('Ctrl Pts',(-16.4772659522328,3.44063971604016,98.8913379369445));
#29519=CARTESIAN_POINT('Ctrl Pts',(-16.4079655937323,3.52161023732575,98.94925502686));
#29520=CARTESIAN_POINT('Ctrl Pts',(-16.3667264774378,3.56979401033893,98.9837202108525));
#29521=CARTESIAN_POINT('Ctrl Pts',(-16.3261173458799,3.6193140120376,99.0168659278914));
#29522=CARTESIAN_POINT('Ctrl Pts',(-16.2862179546654,3.67020490800035,99.0485518299931));
#29523=CARTESIAN_POINT('Ctrl Pts',(-16.264008084157,3.69853316502344,99.0661896876446));
#29524=CARTESIAN_POINT('Ctrl Pts',(-16.2419673252237,3.72735801914113,99.0834087225827));
#29525=CARTESIAN_POINT('Ctrl Pts',(-16.2201221063559,3.75667052759835,99.1001725241583));
#29526=CARTESIAN_POINT('Ctrl Pts',(-16.1531828850613,3.84649139422363,99.1515410103338));
#29527=CARTESIAN_POINT('Ctrl Pts',(-16.0879525207372,3.94106193303834,99.1987035934502));
#29528=CARTESIAN_POINT('Ctrl Pts',(-16.0253317064903,4.04003035297009,99.2404898931802));
#29529=CARTESIAN_POINT('Ctrl Pts',(-15.9694771336334,4.12830513649192,99.2777611415784));
#29530=CARTESIAN_POINT('Ctrl Pts',(-15.9156991936721,4.22007811560318,99.3107542880724));
#29531=CARTESIAN_POINT('Ctrl Pts',(-15.8646538658275,4.3150810117854,99.338614700467));
#29532=CARTESIAN_POINT('Ctrl Pts',(-15.8558170201725,4.33152768704031,99.3434378287456));
#29533=CARTESIAN_POINT('Ctrl Pts',(-15.8470709517408,4.34805391388866,99.3481021122734));
#29534=CARTESIAN_POINT('Ctrl Pts',(-15.8384173641326,4.36465767345712,99.3526059457037));
#29535=CARTESIAN_POINT('Ctrl Pts',(-15.791242699382,4.45517236247468,99.3771584020708));
#29536=CARTESIAN_POINT('Ctrl Pts',(-15.7470132255795,4.54760825118705,99.3968131856348));
#29537=CARTESIAN_POINT('Ctrl Pts',(-15.7058800813114,4.64171660717791,99.4114442249333));
#29538=CARTESIAN_POINT('Ctrl Pts',(-15.6654834850893,4.73413981784503,99.4258132744522));
#29539=CARTESIAN_POINT('Ctrl Pts',(-15.6280730601102,4.82817661116081,99.4353369845748));
#29540=CARTESIAN_POINT('Ctrl Pts',(-15.5938154741567,4.92360774400562,99.4398549403144));
#29541=CARTESIAN_POINT('Ctrl Pts',(-15.5782983430131,4.96683371461404,99.4419013691495));
#29542=CARTESIAN_POINT('Ctrl Pts',(-15.5634284197273,5.01034594078258,99.4429202057471));
#29543=CARTESIAN_POINT('Ctrl Pts',(-15.54922304886,5.05412478637214,99.4428936080771));
#29544=CARTESIAN_POINT('Ctrl Pts',(-15.5490927096604,5.05452647244875,99.4428933640342));
#29545=CARTESIAN_POINT('Ctrl Pts',(-15.5489624219417,5.054928196245,99.4428930314822));
#29546=CARTESIAN_POINT('Ctrl Pts',(-15.5488321857355,5.05532995765703,99.4428926104257));
#29547=CARTESIAN_POINT('Ctrl Pts',(-15.520558415848,5.14255078544335,99.4428012007084));
#29548=CARTESIAN_POINT('Ctrl Pts',(-15.4947275500994,5.23150600734416,99.4385281272485));
#29549=CARTESIAN_POINT('Ctrl Pts',(-15.471706829825,5.32092879229154,99.4301496922843));
#29550=CARTESIAN_POINT('Ctrl Pts',(-15.4609854482667,5.36257543870359,99.4262476250579));
#29551=CARTESIAN_POINT('Ctrl Pts',(-15.450873222712,5.40432327523601,99.4214557128978));
#29552=CARTESIAN_POINT('Ctrl Pts',(-15.4414050589843,5.44604404739281,99.4157848279575));
#29553=CARTESIAN_POINT('Ctrl Pts',(-15.4199748253035,5.5404748073983,99.4029493518352));
#29554=CARTESIAN_POINT('Ctrl Pts',(-15.4018814394618,5.63432924109033,99.3857576708392));
#29555=CARTESIAN_POINT('Ctrl Pts',(-15.3869155759318,5.72751309909371,99.3645857641554));
#29556=CARTESIAN_POINT('Ctrl Pts',(-15.3837402684824,5.74728391939332,99.3600937204537));
#29557=CARTESIAN_POINT('Ctrl Pts',(-15.3807056347888,5.7670245688614,99.3554226501144));
#29558=CARTESIAN_POINT('Ctrl Pts',(-15.3778094961913,5.78673417175796,99.3505763727328));
#29559=CARTESIAN_POINT('Ctrl Pts',(-15.3752577835933,5.80409979164075,99.346306443435));
#29560=CARTESIAN_POINT('Ctrl Pts',(-15.3728123902272,5.82144944475451,99.3418984809087));
#29561=CARTESIAN_POINT('Ctrl Pts',(-15.3704721534173,5.83878192917335,99.3373550074188));
#29562=CARTESIAN_POINT('Ctrl Pts',(-15.3593482394804,5.92116891845956,99.3157583861446));
#29563=CARTESIAN_POINT('Ctrl Pts',(-15.3506235797195,6.00347700634779,99.2909304823459));
#29564=CARTESIAN_POINT('Ctrl Pts',(-15.3441858677526,6.0851481288972,99.2633292101836));
#29565=CARTESIAN_POINT('Ctrl Pts',(-15.3425499146296,6.10590241686122,99.2563151673647));
#29566=CARTESIAN_POINT('Ctrl Pts',(-15.3410614816306,6.12661564803922,99.2491222220216));
#29567=CARTESIAN_POINT('Ctrl Pts',(-15.3397184006096,6.14727885378191,99.2417582529879));
#29568=CARTESIAN_POINT('Ctrl Pts',(-15.3327242044555,6.2548840629056,99.2034098264312));
#29569=CARTESIAN_POINT('Ctrl Pts',(-15.3296610105928,6.36126591155503,99.160338318682));
#29570=CARTESIAN_POINT('Ctrl Pts',(-15.3302281887388,6.46556449283516,99.1134130969483));
#29571=CARTESIAN_POINT('Ctrl Pts',(-15.3302886839739,6.47668898208729,99.1084080516407));
#29572=CARTESIAN_POINT('Ctrl Pts',(-15.3303904984979,6.48778978667583,99.1033591232898));
#29573=CARTESIAN_POINT('Ctrl Pts',(-15.33053328063,6.49886587344165,99.0982673376955));
#29574=CARTESIAN_POINT('Ctrl Pts',(-15.3309963783101,6.53478990686087,99.0817527075989));
#29575=CARTESIAN_POINT('Ctrl Pts',(-15.3318903061923,6.57044546362381,99.0647972731996));
#29576=CARTESIAN_POINT('Ctrl Pts',(-15.3332026482509,6.60579801928923,99.0474373027683));
#29577=CARTESIAN_POINT('Ctrl Pts',(-15.3375368438073,6.72255484245913,98.990103541185));
#29578=CARTESIAN_POINT('Ctrl Pts',(-15.3462629212699,6.83634522428608,98.9284409581762));
#29579=CARTESIAN_POINT('Ctrl Pts',(-15.3589352465123,6.94755494288783,98.8630104837108));
#29580=CARTESIAN_POINT('Ctrl Pts',(-15.3669751681725,7.01811164091287,98.8214983003645));
#29581=CARTESIAN_POINT('Ctrl Pts',(-15.3766042177857,7.08762906317595,98.7784686514901));
#29582=CARTESIAN_POINT('Ctrl Pts',(-15.3877148061349,7.15620112277753,98.7340573318784));
#29583=CARTESIAN_POINT('Ctrl Pts',(-15.3963658244922,7.20959326797821,98.6994774222324));
#29584=CARTESIAN_POINT('Ctrl Pts',(-15.4059126278986,7.2623986669834,98.6640680699513));
#29585=CARTESIAN_POINT('Ctrl Pts',(-15.4163108690968,7.31468638761787,98.6278739858463));
#29586=CARTESIAN_POINT('Ctrl Pts',(-15.434289247329,7.40509094744193,98.5652950437535));
#29587=CARTESIAN_POINT('Ctrl Pts',(-15.4548766711216,7.49387327036431,98.500330324093));
#29588=CARTESIAN_POINT('Ctrl Pts',(-15.477753267434,7.58081992020101,98.4335380215097));
#29589=CARTESIAN_POINT('Ctrl Pts',(-15.4935322900588,7.64079095506091,98.3874683510381));
#29590=CARTESIAN_POINT('Ctrl Pts',(-15.5104013233047,7.69988835331403,98.3405281737054));
#29591=CARTESIAN_POINT('Ctrl Pts',(-15.5282646243346,7.75803424826111,98.292893216895));
#29592=CARTESIAN_POINT('Origin',(-19.8181570368417,-6.43930956430665,100.));
#29593=CARTESIAN_POINT('',(-17.1226665061807,-2.85087466007935,98.2928932187212));
#29594=CARTESIAN_POINT('',(-17.122666505727,-2.85087466042014,0.5));
#29595=CARTESIAN_POINT('',(-17.122666505727,-2.85087466042014,100.));
#29596=CARTESIAN_POINT('',(-15.5282302736771,-7.75804480287584,0.5));
#29597=CARTESIAN_POINT('Origin',(-19.8181570368417,-6.43930956430665,0.5));
#29598=CARTESIAN_POINT('',(-15.5282076340618,-7.7580682497622,98.2929155812433));
#29599=CARTESIAN_POINT('',(-15.5282302736771,-7.75804480287584,100.));
#29600=CARTESIAN_POINT('Ctrl Pts',(-15.5282291636101,-7.7580411917542,98.2928961772888));
#29601=CARTESIAN_POINT('Ctrl Pts',(-15.4694062823956,-7.56668617809925,
98.4496670611161));
#29602=CARTESIAN_POINT('Ctrl Pts',(-15.4218036304123,-7.36679587613455,
98.5976778122644));
#29603=CARTESIAN_POINT('Ctrl Pts',(-15.3535930732429,-6.94509936424973,
98.870667594539));
#29604=CARTESIAN_POINT('Ctrl Pts',(-15.3332436462368,-6.72320235668113,
98.9953666813422));
#29605=CARTESIAN_POINT('Ctrl Pts',(-15.3276516755189,-6.26493973113449,
99.2055148722619));
#29606=CARTESIAN_POINT('Ctrl Pts',(-15.3424287396213,-6.02478319962601,
99.2925877229868));
#29607=CARTESIAN_POINT('Ctrl Pts',(-15.4152999753342,-5.5344197403566,99.4120512183375));
#29608=CARTESIAN_POINT('Ctrl Pts',(-15.47244128436,-5.28983326687213,99.4431642901975));
#29609=CARTESIAN_POINT('Ctrl Pts',(-15.6291564713127,-4.80872211748601,
99.4426185746832));
#29610=CARTESIAN_POINT('Ctrl Pts',(-15.7299886270117,-4.5713886014654,99.4095817567495));
#29611=CARTESIAN_POINT('Ctrl Pts',(-15.9569667264609,-4.13855771815389,
99.2902945556315));
#29612=CARTESIAN_POINT('Ctrl Pts',(-16.0853029468825,-3.93703139748708,
99.2037727159813));
#29613=CARTESIAN_POINT('Ctrl Pts',(-16.3611041702218,-3.56800652240012,
98.9917454068753));
#29614=CARTESIAN_POINT('Ctrl Pts',(-16.5057866639851,-3.40359088922422,
98.8686812585125));
#29615=CARTESIAN_POINT('Ctrl Pts',(-16.8063661957351,-3.10516780207624,
98.5978506351621));
#29616=CARTESIAN_POINT('Ctrl Pts',(-16.9629304851031,-2.97086204840461,
98.4493425737989));
#29617=CARTESIAN_POINT('Ctrl Pts',(-17.122666505727,-2.85087466042014,98.2928932188135));
#29618=CARTESIAN_POINT('Origin',(-12.2482946431511,-16.8583313034371,100.));
#29619=CARTESIAN_POINT('',(-12.1768261122223,-12.3708569010759,98.2928932196637));
#29620=CARTESIAN_POINT('',(-12.1768261106186,-12.3708569011015,0.5));
#29621=CARTESIAN_POINT('',(-12.1768261106186,-12.3708569011015,100.));
#29622=CARTESIAN_POINT('',(-8.00253786221767,-15.4036548377177,0.5));
#29623=CARTESIAN_POINT('Origin',(-12.2482946431511,-16.8583313034371,0.5));
#29624=CARTESIAN_POINT('',(-8.00250696667693,-15.403660603589,98.2929148412897));
#29625=CARTESIAN_POINT('',(-8.00253786221767,-15.4036548377177,100.));
#29626=CARTESIAN_POINT('Ctrl Pts',(-8.00250708598546,-15.403660255427,98.2929146461939));
#29627=CARTESIAN_POINT('Ctrl Pts',(-8.04095434018313,-15.2913939276981,
98.3858632379294));
#29628=CARTESIAN_POINT('Ctrl Pts',(-8.08445379524241,-15.1789643815613,
98.4757075594532));
#29629=CARTESIAN_POINT('Ctrl Pts',(-8.13349045375881,-15.0664065104411,
98.5618687048014));
#29630=CARTESIAN_POINT('Ctrl Pts',(-8.14594002061682,-15.0378299967817,
98.5837435423622));
#29631=CARTESIAN_POINT('Ctrl Pts',(-8.15874627806111,-15.0092451974238,
98.6053811116416));
#29632=CARTESIAN_POINT('Ctrl Pts',(-8.17191669602579,-14.9806526573416,
98.6267722404462));
#29633=CARTESIAN_POINT('Ctrl Pts',(-8.19442659046237,-14.9317844239531,
98.6633323596894));
#29634=CARTESIAN_POINT('Ctrl Pts',(-8.21808777573002,-14.8827759730826,
98.6992365502331));
#29635=CARTESIAN_POINT('Ctrl Pts',(-8.24287820376329,-14.8337655789499,
98.7343285177238));
#29636=CARTESIAN_POINT('Ctrl Pts',(-8.29540418082449,-14.7299223199906,
98.8086814041273));
#29637=CARTESIAN_POINT('Ctrl Pts',(-8.35322906336708,-14.6256182642626,
98.8796681588562));
#29638=CARTESIAN_POINT('Ctrl Pts',(-8.41624979625317,-14.522181993344,98.9457243517455));
#29639=CARTESIAN_POINT('Ctrl Pts',(-8.45042299052846,-14.4660933441116,
98.9815435339307));
#29640=CARTESIAN_POINT('Ctrl Pts',(-8.48612332307116,-14.4102605388657,
99.015912405446));
#29641=CARTESIAN_POINT('Ctrl Pts',(-8.5233300376651,-14.3548990672715,99.0485791162112));
#29642=CARTESIAN_POINT('Ctrl Pts',(-8.54347127793551,-14.3249300492255,
99.0662627004123));
#29643=CARTESIAN_POINT('Ctrl Pts',(-8.56405612172788,-14.2950703500544,
99.0834771132439));
#29644=CARTESIAN_POINT('Ctrl Pts',(-8.58510094647072,-14.2653257640176,
99.1001978976778));
#29645=CARTESIAN_POINT('Ctrl Pts',(-8.64085775874582,-14.1865195339767,
99.1444984632641));
#29646=CARTESIAN_POINT('Ctrl Pts',(-8.69986277604752,-14.1084893186481,
99.1853565450778));
#29647=CARTESIAN_POINT('Ctrl Pts',(-8.76251977964325,-14.0312399826521,
99.2223453246317));
#29648=CARTESIAN_POINT('Ctrl Pts',(-8.82234975489544,-13.9574760680751,
99.2576652033095));
#29649=CARTESIAN_POINT('Ctrl Pts',(-8.88550949801275,-13.8844241448053,
99.2894572254271));
#29650=CARTESIAN_POINT('Ctrl Pts',(-8.95238110253115,-13.8120961796839,
99.3173134272134));
#29651=CARTESIAN_POINT('Ctrl Pts',(-8.96841979764084,-13.7947488139546,
99.3239945459122));
#29652=CARTESIAN_POINT('Ctrl Pts',(-8.98467216422782,-13.7774431305777,
99.3304490804178));
#29653=CARTESIAN_POINT('Ctrl Pts',(-9.00114376230899,-13.7601793662716,
99.3366710553149));
#29654=CARTESIAN_POINT('Ctrl Pts',(-9.01384496169299,-13.7468673299111,
99.3414688013102));
#29655=CARTESIAN_POINT('Ctrl Pts',(-9.02667804656013,-13.7335844186059,
99.346122084825));
#29656=CARTESIAN_POINT('Ctrl Pts',(-9.03963548955908,-13.7203394312888,
99.350626662246));
#29657=CARTESIAN_POINT('Ctrl Pts',(-9.11972744908156,-13.6384701158562,
99.378470152084));
#29658=CARTESIAN_POINT('Ctrl Pts',(-9.20426990945249,-13.5583572449624,
99.4004995600324));
#29659=CARTESIAN_POINT('Ctrl Pts',(-9.29128918150773,-13.4821421839037,
99.4158205242222));
#29660=CARTESIAN_POINT('Ctrl Pts',(-9.39222822782236,-13.39373561147,99.4335922600391));
#29661=CARTESIAN_POINT('Ctrl Pts',(-9.49729440462544,-13.3096962059213,
99.4426890000595));
#29662=CARTESIAN_POINT('Ctrl Pts',(-9.6065927128656,-13.2301161534923,99.4428904203957));
#29663=CARTESIAN_POINT('Ctrl Pts',(-9.60682851186603,-13.2299444683389,
99.4428908549378));
#29664=CARTESIAN_POINT('Ctrl Pts',(-9.60706433486258,-13.2297728014511,
99.4428912473282));
#29665=CARTESIAN_POINT('Ctrl Pts',(-9.60730018182524,-13.2296011528498,
99.4428915975688));
#29666=CARTESIAN_POINT('Ctrl Pts',(-9.68141111896221,-13.1756634698788,
99.443001654775));
#29667=CARTESIAN_POINT('Ctrl Pts',(-9.7579136919251,-13.1235161930304,99.4389375211795));
#29668=CARTESIAN_POINT('Ctrl Pts',(-9.83576642333202,-13.0738739727025,
99.4307630339894));
#29669=CARTESIAN_POINT('Ctrl Pts',(-9.87237363861166,-13.0505316517119,
99.4269192997111));
#29670=CARTESIAN_POINT('Ctrl Pts',(-9.90927903493427,-13.0277429117627,
99.4221673968399));
#29671=CARTESIAN_POINT('Ctrl Pts',(-9.94637331208393,-13.005580020478,99.4165172327954));
#29672=CARTESIAN_POINT('Ctrl Pts',(-10.0295053402403,-12.9559107387482,
99.4038546435089));
#29673=CARTESIAN_POINT('Ctrl Pts',(-10.113122012639,-12.9095945146346,99.386832149816));
#29674=CARTESIAN_POINT('Ctrl Pts',(-10.1970690548685,-12.8664609300821,
99.3658258363157));
#29675=CARTESIAN_POINT('Ctrl Pts',(-10.2150684963089,-12.857212475239,99.3613217835261));
#29676=CARTESIAN_POINT('Ctrl Pts',(-10.2330831050167,-12.8481102206571,
99.3566347314641));
#29677=CARTESIAN_POINT('Ctrl Pts',(-10.2511113268446,-12.8391523023418,
99.3517686237608));
#29678=CARTESIAN_POINT('Ctrl Pts',(-10.2669187778883,-12.8312978474447,
99.347501937893));
#29679=CARTESIAN_POINT('Ctrl Pts',(-10.282743992679,-12.8235507352674,99.3430956262505));
#29680=CARTESIAN_POINT('Ctrl Pts',(-10.2985854655186,-12.8159101990171,
99.3385522499821));
#29681=CARTESIAN_POINT('Ctrl Pts',(-10.373846061876,-12.7796110922031,99.3169673120849));
#29682=CARTESIAN_POINT('Ctrl Pts',(-10.4497789727234,-12.7456422248302,
99.2921178033657));
#29683=CARTESIAN_POINT('Ctrl Pts',(-10.5258154871132,-12.7140687420283,
99.2644650244212));
#29684=CARTESIAN_POINT('Ctrl Pts',(-10.5448521425387,-12.7061639410586,
99.2575418187937));
#29685=CARTESIAN_POINT('Ctrl Pts',(-10.5638953135564,-12.6984091102452,
99.2504430888631));
#29686=CARTESIAN_POINT('Ctrl Pts',(-10.5829361512679,-12.6908049207666,
99.2431764205676));
#29687=CARTESIAN_POINT('Ctrl Pts',(-10.6820892557964,-12.6512069258858,
99.2053360307699));
#29688=CARTESIAN_POINT('Ctrl Pts',(-10.7813009536874,-12.6156428244173,
99.1628582909476));
#29689=CARTESIAN_POINT('Ctrl Pts',(-10.8797010333698,-12.5840907770436,
99.1165798460778));
#29690=CARTESIAN_POINT('Ctrl Pts',(-10.891559547104,-12.5802883371642,99.1110026801257));
#29691=CARTESIAN_POINT('Ctrl Pts',(-10.9034062978763,-12.5765441851341,
99.1053702615889));
#29692=CARTESIAN_POINT('Ctrl Pts',(-10.9152397813687,-12.5728582981514,
99.0996840124349));
#29693=CARTESIAN_POINT('Ctrl Pts',(-10.9496077250953,-12.5621533897882,
99.0831694593816));
#29694=CARTESIAN_POINT('Ctrl Pts',(-10.9838534531502,-12.5519431297429,
99.0662118234554));
#29695=CARTESIAN_POINT('Ctrl Pts',(-11.0179405472129,-12.5422262222296,
99.0488473569643));
#29696=CARTESIAN_POINT('Ctrl Pts',(-11.1286979038751,-12.5106535986106,
98.9924259323376));
#29697=CARTESIAN_POINT('Ctrl Pts',(-11.2380248634249,-12.484033807446,98.9317993629228));
#29698=CARTESIAN_POINT('Ctrl Pts',(-11.3461476368695,-12.4618433879349,
98.8675030974997));
#29699=CARTESIAN_POINT('Ctrl Pts',(-11.4178105090686,-12.4471357630118,
98.824888069184));
#29700=CARTESIAN_POINT('Ctrl Pts',(-11.4889441178986,-12.4343747574801,
98.7806601364314));
#29701=CARTESIAN_POINT('Ctrl Pts',(-11.5596115261684,-12.4234165163235,
98.7349665698175));
#29702=CARTESIAN_POINT('Ctrl Pts',(-11.6130987298848,-12.4151223720854,
98.7003817284338));
#29703=CARTESIAN_POINT('Ctrl Pts',(-11.6663040534074,-12.4078631071804,
98.6649661331026));
#29704=CARTESIAN_POINT('Ctrl Pts',(-11.719279568674,-12.4015749360366,98.6287647534647));
#29705=CARTESIAN_POINT('Ctrl Pts',(-11.8108343641753,-12.3907074207279,
98.5661998139274));
#29706=CARTESIAN_POINT('Ctrl Pts',(-11.9016543857439,-12.3828242789111,
98.5012454209961));
#29707=CARTESIAN_POINT('Ctrl Pts',(-11.991437135553,-12.3776871588067,98.4344604661188));
#29708=CARTESIAN_POINT('Ctrl Pts',(-12.0537689069902,-12.3741207076022,
98.3880949387573));
#29709=CARTESIAN_POINT('Ctrl Pts',(-12.1156007258684,-12.3718787930038,
98.3408460596308));
#29710=CARTESIAN_POINT('Ctrl Pts',(-12.1768266918443,-12.3708930987133,
98.29289321686));
#29711=CARTESIAN_POINT('Origin',(-2.55192432461455E-15,-20.8380434782609,
100.));
#29712=CARTESIAN_POINT('',(-2.57983136337902,-17.1656216833844,98.292893216895));
#29713=CARTESIAN_POINT('',(-2.57985201635105,-17.1655922755232,0.5));
#29714=CARTESIAN_POINT('',(-2.57985201635105,-17.1655922755232,100.));
#29715=CARTESIAN_POINT('',(2.57985201635104,-17.1655922755232,0.5));
#29716=CARTESIAN_POINT('Origin',(-2.55192432461455E-15,-20.8380434782609,
0.5));
#29717=CARTESIAN_POINT('',(2.57983420291488,-17.1656249920606,98.2928992166643));
#29718=CARTESIAN_POINT('',(2.57985201635104,-17.1655922755232,100.));
#29719=CARTESIAN_POINT('Ctrl Pts',(2.57983420291488,-17.1656249920606,98.2928992166643));
#29720=CARTESIAN_POINT('Ctrl Pts',(2.4892116886444,-17.1019995465655,98.3796187467301));
#29721=CARTESIAN_POINT('Ctrl Pts',(2.3946045185082,-17.0405846361733,98.4639979993635));
#29722=CARTESIAN_POINT('Ctrl Pts',(2.29603754132888,-16.9819052231602,98.5451592717554));
#29723=CARTESIAN_POINT('Ctrl Pts',(2.20329025421175,-16.9266904187466,98.6215285391179));
#29724=CARTESIAN_POINT('Ctrl Pts',(2.10703651916783,-16.8738971253428,98.6950495057112));
#29725=CARTESIAN_POINT('Ctrl Pts',(2.0072688812662,-16.8239841981541,98.7649644149723));
#29726=CARTESIAN_POINT('Ctrl Pts',(1.91489692774978,-16.7777712709252,98.8296965955089));
#29727=CARTESIAN_POINT('Ctrl Pts',(1.8195123779607,-16.7340272983991,98.891337936913));
#29728=CARTESIAN_POINT('Ctrl Pts',(1.72108984757851,-16.6931400079876,98.9492550268265));
#29729=CARTESIAN_POINT('Ctrl Pts',(1.66252076848856,-16.6688088824152,98.983720210831));
#29730=CARTESIAN_POINT('Ctrl Pts',(1.60287553638916,-16.6454898253045,99.0168659278811));
#29731=CARTESIAN_POINT('Ctrl Pts',(1.54214582819377,-16.6232694009981,99.048551829993));
#29732=CARTESIAN_POINT('Ctrl Pts',(1.50834082732673,-16.6109004717661,99.0661896876445));
#29733=CARTESIAN_POINT('Ctrl Pts',(1.47411579290756,-16.5988458341413,99.0834087225826));
#29734=CARTESIAN_POINT('Ctrl Pts',(1.43948739685436,-16.5871278596483,99.1001725241582));
#29735=CARTESIAN_POINT('Ctrl Pts',(1.33337731939881,-16.551221051283,99.151541010325));
#29736=CARTESIAN_POINT('Ctrl Pts',(1.22327810110348,-16.5184071918983,99.1987035934342));
#29737=CARTESIAN_POINT('Ctrl Pts',(1.10980264463643,-16.489434182122,99.240489893159));
#29738=CARTESIAN_POINT('Ctrl Pts',(1.00858832429893,-16.4635917349186,99.2777611415658));
#29739=CARTESIAN_POINT('Ctrl Pts',(0.904688737105505,-16.4408052848502,
99.3107542880671));
#29740=CARTESIAN_POINT('Ctrl Pts',(0.798561739816924,-16.4216158026087,
99.338614700467));
#29741=CARTESIAN_POINT('Ctrl Pts',(0.780189286660287,-16.4182937651197,
99.3434378287456));
#29742=CARTESIAN_POINT('Ctrl Pts',(0.761769227147023,-16.4150826446948,
99.3481021122734));
#29743=CARTESIAN_POINT('Ctrl Pts',(0.743304007781208,-16.4119834376879,
99.3526059457037));
#29744=CARTESIAN_POINT('Ctrl Pts',(0.642641649851918,-16.3950882425186,
99.3771584020724));
#29745=CARTESIAN_POINT('Ctrl Pts',(0.541062236488303,-16.3815877737481,
99.3968131856375));
#29746=CARTESIAN_POINT('Ctrl Pts',(0.438849030667434,-16.3715489101698,
99.4114442249363));
#29747=CARTESIAN_POINT('Ctrl Pts',(0.338466099151273,-16.3616898068673,
99.4258132744554));
#29748=CARTESIAN_POINT('Ctrl Pts',(0.23747133700468,-16.3551693456449,99.4353369845777));
#29749=CARTESIAN_POINT('Ctrl Pts',(0.13612476000251,-16.3520782871335,99.4398549403163));
#29750=CARTESIAN_POINT('Ctrl Pts',(0.0902193617685212,-16.3506781779624,
99.4419013691501));
#29751=CARTESIAN_POINT('Ctrl Pts',(0.0442417165457677,-16.3499820578742,
99.4429202057471));
#29752=CARTESIAN_POINT('Ctrl Pts',(-0.00178414082371589,-16.3500003546257,
99.4428936080771));
#29753=CARTESIAN_POINT('Ctrl Pts',(-0.00220644401206383,-16.3500005225047,
99.4428933640343));
#29754=CARTESIAN_POINT('Ctrl Pts',(-0.00262876716548478,-16.3500007510009,
99.4428930314822));
#29755=CARTESIAN_POINT('Ctrl Pts',(-0.00305111017540327,-16.3500010401123,
99.4428926104257));
#29756=CARTESIAN_POINT('Ctrl Pts',(-0.0947401221997488,-16.35006380507,
99.4428012007084));
#29757=CARTESIAN_POINT('Ctrl Pts',(-0.18732374215409,-16.3529858671848,
99.4385281272474));
#29758=CARTESIAN_POINT('Ctrl Pts',(-0.279483658282253,-16.3587250213924,
99.4301496922812));
#29759=CARTESIAN_POINT('Ctrl Pts',(-0.322405061827636,-16.3613979030974,
99.4262476250554));
#29760=CARTESIAN_POINT('Ctrl Pts',(-0.365234463339091,-16.3646813960556,
99.4214557128963));
#29761=CARTESIAN_POINT('Ctrl Pts',(-0.407839099049934,-16.3685690648589,
99.4157848279575));
#29762=CARTESIAN_POINT('Ctrl Pts',(-0.504270395105379,-16.3773684111056,
99.4029493518336));
#29763=CARTESIAN_POINT('Ctrl Pts',(-0.599122429574534,-16.3891631936093,
99.3857576708347));
#29764=CARTESIAN_POINT('Ctrl Pts',(-0.69237025112029,-16.4037252073042,
99.3645857641471));
#29765=CARTESIAN_POINT('Ctrl Pts',(-0.712154642550585,-16.4068148299267,
99.3600937204479));
#29766=CARTESIAN_POINT('Ctrl Pts',(-0.731866869233836,-16.4100289179416,
99.3554226501115));
#29767=CARTESIAN_POINT('Ctrl Pts',(-0.751506771534701,-16.4133651287016,
99.3505763727328));
#29768=CARTESIAN_POINT('Ctrl Pts',(-0.768810980041281,-16.4163045774693,
99.346306443435));
#29769=CARTESIAN_POINT('Ctrl Pts',(-0.786067148798637,-16.4193402078322,
99.3418984809088));
#29770=CARTESIAN_POINT('Ctrl Pts',(-0.803274493993886,-16.4224705426046,
99.3373550074189));
#29771=CARTESIAN_POINT('Ctrl Pts',(-0.885066655462472,-16.437350051573,
99.3157583861447));
#29772=CARTESIAN_POINT('Ctrl Pts',(-0.966042366928278,-16.4544870049868,
99.2909304823462));
#29773=CARTESIAN_POINT('Ctrl Pts',(-1.04570558262436,-16.473602141888,99.2633292101841));
#29774=CARTESIAN_POINT('Ctrl Pts',(-1.06594962075099,-16.4784596856972,
99.256315167365));
#29775=CARTESIAN_POINT('Ctrl Pts',(-1.0861090253284,-16.4834448422369,99.2491222220218));
#29776=CARTESIAN_POINT('Ctrl Pts',(-1.10617593665822,-16.4885527780128,
99.241758252988));
#29777=CARTESIAN_POINT('Ctrl Pts',(-1.21067589741909,-16.5151527404773,
99.2034098264448));
#29778=CARTESIAN_POINT('Ctrl Pts',(-1.31279762671789,-16.5451132691073,
99.1603383187126));
#29779=CARTESIAN_POINT('Ctrl Pts',(-1.41181620436576,-16.5778827216701,
99.1134130969983));
#29780=CARTESIAN_POINT('Ctrl Pts',(-1.42237752833916,-16.5813779123017,
99.1084080516743));
#29781=CARTESIAN_POINT('Ctrl Pts',(-1.4329035584962,-16.5849050809489,99.1033591233068));
#29782=CARTESIAN_POINT('Ctrl Pts',(-1.44339342091949,-16.5884635738797,
99.0982673376955));
#29783=CARTESIAN_POINT('Ctrl Pts',(-1.47741610194129,-16.6000051427791,
99.0817527075989));
#29784=CARTESIAN_POINT('Ctrl Pts',(-1.51105031263546,-16.6118734917002,
99.0647972731995));
#29785=CARTESIAN_POINT('Ctrl Pts',(-1.54426705507015,-16.6240461436618,
99.0474373027682));
#29786=CARTESIAN_POINT('Ctrl Pts',(-1.65397005242361,-16.6642480511353,
98.9901035412164));
#29787=CARTESIAN_POINT('Ctrl Pts',(-1.7594946302662,-16.7077102057232,98.9284409582433));
#29788=CARTESIAN_POINT('Ctrl Pts',(-1.86134539390795,-16.7541279961806,
98.8630104838176));
#29789=CARTESIAN_POINT('Ctrl Pts',(-1.92596432896475,-16.7835776348461,
98.821498300438));
#29790=CARTESIAN_POINT('Ctrl Pts',(-1.98910378648957,-16.8142174701363,
98.7784686515277));
#29791=CARTESIAN_POINT('Ctrl Pts',(-2.05088633004532,-16.8459741993693,
98.7340573318779));
#29792=CARTESIAN_POINT('Ctrl Pts',(-2.09899196596652,-16.8707008869837,
98.699477422232));
#29793=CARTESIAN_POINT('Ctrl Pts',(-2.14626276029159,-16.8960982022606,
98.6640680699512));
#29794=CARTESIAN_POINT('Ctrl Pts',(-2.19277810448147,-16.9221453115834,
98.6278739858466));
#29795=CARTESIAN_POINT('Ctrl Pts',(-2.2732023258176,-16.9671803107181,98.5652950437409));
#29796=CARTESIAN_POINT('Ctrl Pts',(-2.35127746875916,-17.0141953608637,
98.5003303240652));
#29797=CARTESIAN_POINT('Ctrl Pts',(-2.42689938963798,-17.0628202892722,
98.433538021466));
#29798=CARTESIAN_POINT('Ctrl Pts',(-2.4790592469673,-17.096359100492,98.3874683510083));
#29799=CARTESIAN_POINT('Ctrl Pts',(-2.53005139470365,-17.1306646048568,
98.3405281736901));
#29800=CARTESIAN_POINT('Ctrl Pts',(-2.57983136337902,-17.1656216833844,
98.292893216895));
#29801=CARTESIAN_POINT('Origin',(12.2482946431511,-16.8583313034371,100.));
#29802=CARTESIAN_POINT('',(12.1768414139071,-12.3708281240615,98.2929155812437));
#29803=CARTESIAN_POINT('',(8.00253786203375,-15.4036548382545,98.2928932187212));
#29804=CARTESIAN_POINT('Ctrl Pts',(12.1768223332082,-12.3708569612629,98.2928961772889));
#29805=CARTESIAN_POINT('Ctrl Pts',(11.9766556305925,-12.3740450279548,98.4496670611162));
#29806=CARTESIAN_POINT('Ctrl Pts',(11.7718386279247,-12.390541715911,98.5976778122645));
#29807=CARTESIAN_POINT('Ctrl Pts',(11.3497031910366,-12.455981009676,98.870667594539));
#29808=CARTESIAN_POINT('Ctrl Pts',(11.1323782772714,-12.5051975008586,98.9953666813422));
#29809=CARTESIAN_POINT('Ctrl Pts',(10.6948166070868,-12.6414901598492,99.2055148722619));
#29810=CARTESIAN_POINT('Ctrl Pts',(10.4709805367995,-12.7297564325018,99.2925877229868));
#29811=CARTESIAN_POINT('Ctrl Pts',(10.0271356237447,-12.9505917384117,99.4120512183375));
#29812=CARTESIAN_POINT('Ctrl Pts',(9.8121776999094,-13.0805177296113,99.4431642901975));
#29813=CARTESIAN_POINT('Ctrl Pts',(9.40304146226851,-13.3782342507087,99.4426185746832));
#29814=CARTESIAN_POINT('Ctrl Pts',(9.2084827250123,-13.5474714192234,99.4095817567495));
#29815=CARTESIAN_POINT('Ctrl Pts',(8.86697618306584,-13.8970925183944,99.2902945556315));
#29816=CARTESIAN_POINT('Ctrl Pts',(8.71497133569482,-14.081422575003,99.2037727159813));
#29817=CARTESIAN_POINT('Ctrl Pts',(8.44923508864959,-14.4577600834109,98.9917454068753));
#29818=CARTESIAN_POINT('Ctrl Pts',(8.33757587869828,-14.6461685366907,98.8686812585125));
#29819=CARTESIAN_POINT('Ctrl Pts',(8.1466428405253,-15.024254464469,98.5978506351621));
#29820=CARTESIAN_POINT('Ctrl Pts',(8.0672915044469,-15.2146587124184,98.4493425737989));
#29821=CARTESIAN_POINT('Ctrl Pts',(8.00253786221766,-15.4036548377177,98.2928932188135));
#29822=CARTESIAN_POINT('',(8.00253786221767,-15.4036548377177,0.5));
#29823=CARTESIAN_POINT('',(8.00253786221767,-15.4036548377177,100.));
#29824=CARTESIAN_POINT('',(12.1768261106186,-12.3708569011015,0.5));
#29825=CARTESIAN_POINT('Origin',(12.2482946431511,-16.8583313034371,0.5));
#29826=CARTESIAN_POINT('',(12.1768261106186,-12.3708569011015,100.));
#29827=CARTESIAN_POINT('Origin',(19.8181570368417,-6.43930956430665,100.));
#29828=CARTESIAN_POINT('',(15.5282646243346,-7.75803424826115,98.2928932168951));
#29829=CARTESIAN_POINT('',(15.5282302736771,-7.75804480287585,0.5));
#29830=CARTESIAN_POINT('',(15.5282302736771,-7.75804480287585,100.));
#29831=CARTESIAN_POINT('',(17.122666505727,-2.85087466042014,0.5));
#29832=CARTESIAN_POINT('Origin',(19.8181570368417,-6.43930956430665,0.5));
#29833=CARTESIAN_POINT('',(17.1226921163488,-2.8509017119705,98.2928992166648));
#29834=CARTESIAN_POINT('',(17.122666505727,-2.85087466042014,100.));
#29835=CARTESIAN_POINT('Ctrl Pts',(17.1226921163488,-2.8509017119705,98.2928992166648));
#29836=CARTESIAN_POINT('Ctrl Pts',(17.0341768248214,-2.91742750076124,98.3796187467353));
#29837=CARTESIAN_POINT('Ctrl Pts',(16.9465325507289,-2.98842601539211,98.4639979993731));
#29838=CARTESIAN_POINT('Ctrl Pts',(16.8602662415735,-3.06403584549337,98.5451592717689));
#29839=CARTESIAN_POINT('Ctrl Pts',(16.7790933541347,-3.13518144437395,98.621528539135));
#29840=CARTESIAN_POINT('Ctrl Pts',(16.6991399085219,-3.21041016145889,98.6950495057316));
#29841=CARTESIAN_POINT('Ctrl Pts',(16.6208399982677,-3.28987088086528,98.7649644149954));
#29842=CARTESIAN_POINT('Ctrl Pts',(16.5483443892456,-3.36344124931151,98.829696595535));
#29843=CARTESIAN_POINT('Ctrl Pts',(16.4772659522367,-3.44063971603582,98.8913379369416));
#29844=CARTESIAN_POINT('Ctrl Pts',(16.4079655937362,-3.52161023732113,98.9492550268571));
#29845=CARTESIAN_POINT('Ctrl Pts',(16.3667264774404,-3.56979401033572,98.9837202108507));
#29846=CARTESIAN_POINT('Ctrl Pts',(16.3261173458813,-3.61931401203589,99.0168659278907));
#29847=CARTESIAN_POINT('Ctrl Pts',(16.2862179546655,-3.67020490800025,99.0485518299934));
#29848=CARTESIAN_POINT('Ctrl Pts',(16.264008084157,-3.69853316502337,99.0661896876449));
#29849=CARTESIAN_POINT('Ctrl Pts',(16.2419673252237,-3.72735801914106,99.0834087225829));
#29850=CARTESIAN_POINT('Ctrl Pts',(16.220122106356,-3.75667052759827,99.1001725241585));
#29851=CARTESIAN_POINT('Ctrl Pts',(16.1531828850337,-3.84649139426061,99.1515410103551));
#29852=CARTESIAN_POINT('Ctrl Pts',(16.0879525206834,-3.94106193311628,99.1987035934887));
#29853=CARTESIAN_POINT('Ctrl Pts',(16.0253317064128,-4.04003035309249,99.2404898932312));
#29854=CARTESIAN_POINT('Ctrl Pts',(15.9694771335837,-4.12830513657678,99.2777611416079));
#29855=CARTESIAN_POINT('Ctrl Pts',(15.9156991936484,-4.22007811564716,99.3107542880842));
#29856=CARTESIAN_POINT('Ctrl Pts',(15.8646538658274,-4.31508101178553,99.3386147004664));
#29857=CARTESIAN_POINT('Ctrl Pts',(15.8558170201725,-4.33152768704044,99.343437828745));
#29858=CARTESIAN_POINT('Ctrl Pts',(15.8470709517407,-4.34805391388877,99.3481021122728));
#29859=CARTESIAN_POINT('Ctrl Pts',(15.8384173641326,-4.3646576734572,99.3526059457032));
#29860=CARTESIAN_POINT('Ctrl Pts',(15.7912426993732,-4.45517236249152,99.3771584020751));
#29861=CARTESIAN_POINT('Ctrl Pts',(15.7470132255631,-4.54760825122134,99.396813185642));
#29862=CARTESIAN_POINT('Ctrl Pts',(15.7058800812885,-4.64171660723027,99.4114442249414));
#29863=CARTESIAN_POINT('Ctrl Pts',(15.6654834850592,-4.73413981791697,99.4258132744614));
#29864=CARTESIAN_POINT('Ctrl Pts',(15.6280730600742,-4.82817661125299,99.4353369845832));
#29865=CARTESIAN_POINT('Ctrl Pts',(15.5938154741162,-4.92360774411853,99.4398549403198));
#29866=CARTESIAN_POINT('Ctrl Pts',(15.5782983429872,-4.96683371468982,99.4419013691512));
#29867=CARTESIAN_POINT('Ctrl Pts',(15.5634284197149,-5.0103459408207,99.442920205747));
#29868=CARTESIAN_POINT('Ctrl Pts',(15.54922304886,-5.05412478637214,99.4428936080771));
#29869=CARTESIAN_POINT('Ctrl Pts',(15.5490927096604,-5.05452647244875,99.4428933640342));
#29870=CARTESIAN_POINT('Ctrl Pts',(15.5489624219417,-5.05492819624499,99.4428930314822));
#29871=CARTESIAN_POINT('Ctrl Pts',(15.5488321857355,-5.05532995765703,99.4428926104257));
#29872=CARTESIAN_POINT('Ctrl Pts',(15.5205584158414,-5.14255078546346,99.4428012007084));
#29873=CARTESIAN_POINT('Ctrl Pts',(15.4947275500875,-5.23150600738526,99.4385281272465));
#29874=CARTESIAN_POINT('Ctrl Pts',(15.471706829809,-5.32092879235345,99.4301496922785));
#29875=CARTESIAN_POINT('Ctrl Pts',(15.4609854482567,-5.36257543874499,99.4262476250531));
#29876=CARTESIAN_POINT('Ctrl Pts',(15.4508732227073,-5.40432327525671,99.421455712895));
#29877=CARTESIAN_POINT('Ctrl Pts',(15.4414050589843,-5.44604404739281,99.4157848279575));
#29878=CARTESIAN_POINT('Ctrl Pts',(15.4199748252984,-5.54047480742042,99.4029493518322));
#29879=CARTESIAN_POINT('Ctrl Pts',(15.4018814394533,-5.63432924113464,99.3857576708312));
#29880=CARTESIAN_POINT('Ctrl Pts',(15.3869155759212,-5.72751309915976,99.3645857641404));
#29881=CARTESIAN_POINT('Ctrl Pts',(15.3837402684756,-5.7472839194373,99.3600937204433));
#29882=CARTESIAN_POINT('Ctrl Pts',(15.3807056347856,-5.76702456888336,99.3554226501091));
#29883=CARTESIAN_POINT('Ctrl Pts',(15.3778094961913,-5.78673417175797,99.3505763727328));
#29884=CARTESIAN_POINT('Ctrl Pts',(15.3752577835933,-5.80409979164077,99.346306443435));
#29885=CARTESIAN_POINT('Ctrl Pts',(15.3728123902272,-5.82144944475452,99.3418984809087));
#29886=CARTESIAN_POINT('Ctrl Pts',(15.3704721534172,-5.83878192917335,99.3373550074188));
#29887=CARTESIAN_POINT('Ctrl Pts',(15.3593482394826,-5.92116891844311,99.3157583861489));
#29888=CARTESIAN_POINT('Ctrl Pts',(15.350623579723,-6.00347700631512,99.2909304823557));
#29889=CARTESIAN_POINT('Ctrl Pts',(15.3441858677564,-6.08514812884863,99.2633292102));
#29890=CARTESIAN_POINT('Ctrl Pts',(15.342549914632,-6.10590241682891,99.2563151673759));
#29891=CARTESIAN_POINT('Ctrl Pts',(15.3410614816317,-6.1266156480231,99.2491222220274));
#29892=CARTESIAN_POINT('Ctrl Pts',(15.3397184006096,-6.1472788537819,99.2417582529879));
#29893=CARTESIAN_POINT('Ctrl Pts',(15.3327242044575,-6.25488406287628,99.2034098264416));
#29894=CARTESIAN_POINT('Ctrl Pts',(15.3296610105945,-6.36126591149707,99.1603383187055));
#29895=CARTESIAN_POINT('Ctrl Pts',(15.3302281887384,-6.46556449274991,99.1134130969867));
#29896=CARTESIAN_POINT('Ctrl Pts',(15.3302886839734,-6.47668898203059,99.1084080516665));
#29897=CARTESIAN_POINT('Ctrl Pts',(15.3303904984975,-6.48778978664755,99.1033591233028));
#29898=CARTESIAN_POINT('Ctrl Pts',(15.33053328063,-6.49886587344166,99.0982673376955));
#29899=CARTESIAN_POINT('Ctrl Pts',(15.3309963783101,-6.53478990686088,99.081752707599));
#29900=CARTESIAN_POINT('Ctrl Pts',(15.3318903061923,-6.57044546362382,99.0647972731996));
#29901=CARTESIAN_POINT('Ctrl Pts',(15.3332026482509,-6.60579801928925,99.0474373027683));
#29902=CARTESIAN_POINT('Ctrl Pts',(15.3375368438081,-6.72255484247992,98.9901035411749));
#29903=CARTESIAN_POINT('Ctrl Pts',(15.346262921273,-6.83634522432656,98.9284409581542));
#29904=CARTESIAN_POINT('Ctrl Pts',(15.3589352465191,-6.94755494294715,98.8630104836759));
#29905=CARTESIAN_POINT('Ctrl Pts',(15.3669751681779,-7.01811164095182,98.8214983003403));
#29906=CARTESIAN_POINT('Ctrl Pts',(15.3766042177888,-7.08762906319514,98.7784686514776));
#29907=CARTESIAN_POINT('Ctrl Pts',(15.3877148061349,-7.15620112277751,98.7340573318784));
#29908=CARTESIAN_POINT('Ctrl Pts',(15.3963658244922,-7.20959326797818,98.6994774222324));
#29909=CARTESIAN_POINT('Ctrl Pts',(15.4059126278986,-7.26239866698339,98.6640680699514));
#29910=CARTESIAN_POINT('Ctrl Pts',(15.4163108690968,-7.31468638761793,98.6278739858464));
#29911=CARTESIAN_POINT('Ctrl Pts',(15.4342892473289,-7.40509094744151,98.565295043754));
#29912=CARTESIAN_POINT('Ctrl Pts',(15.4548766711213,-7.49387327036325,98.500330324094));
#29913=CARTESIAN_POINT('Ctrl Pts',(15.4777532674335,-7.5808199201993,98.4335380215112));
#29914=CARTESIAN_POINT('Ctrl Pts',(15.4935322900585,-7.6407909550598,98.3874683510391));
#29915=CARTESIAN_POINT('Ctrl Pts',(15.5104013233044,-7.69988835331348,98.3405281737059));
#29916=CARTESIAN_POINT('Ctrl Pts',(15.5282646243346,-7.75803424826115,98.2928932168951));
#29917=CARTESIAN_POINT('Origin',(19.8181570368417,6.43930956430664,100.));
#29918=CARTESIAN_POINT('',(17.1226665061807,2.85087466007934,98.2928932187211));
#29919=CARTESIAN_POINT('',(17.122666505727,2.85087466042014,0.5));
#29920=CARTESIAN_POINT('',(17.122666505727,2.85087466042014,100.));
#29921=CARTESIAN_POINT('',(15.5282302736771,7.75804480287584,0.5));
#29922=CARTESIAN_POINT('Origin',(19.8181570368417,6.43930956430664,0.5));
#29923=CARTESIAN_POINT('',(15.528207634062,7.7580682497625,98.2929155812437));
#29924=CARTESIAN_POINT('',(15.5282302736771,7.75804480287584,100.));
#29925=CARTESIAN_POINT('Ctrl Pts',(15.5282291636101,7.75804119175414,98.2928961772889));
#29926=CARTESIAN_POINT('Ctrl Pts',(15.4694062823956,7.56668617809921,98.4496670611162));
#29927=CARTESIAN_POINT('Ctrl Pts',(15.4218036304123,7.36679587613452,98.5976778122644));
#29928=CARTESIAN_POINT('Ctrl Pts',(15.3535930732429,6.94509936424972,98.870667594539));
#29929=CARTESIAN_POINT('Ctrl Pts',(15.3332436462368,6.72320235668112,98.9953666813422));
#29930=CARTESIAN_POINT('Ctrl Pts',(15.3276516755189,6.26493973113448,99.2055148722619));
#29931=CARTESIAN_POINT('Ctrl Pts',(15.3424287396213,6.02478319962601,99.2925877229867));
#29932=CARTESIAN_POINT('Ctrl Pts',(15.4152999753342,5.5344197403566,99.4120512183375));
#29933=CARTESIAN_POINT('Ctrl Pts',(15.47244128436,5.28983326687212,99.4431642901975));
#29934=CARTESIAN_POINT('Ctrl Pts',(15.6291564713127,4.80872211748601,99.4426185746832));
#29935=CARTESIAN_POINT('Ctrl Pts',(15.7299886270117,4.5713886014654,99.4095817567495));
#29936=CARTESIAN_POINT('Ctrl Pts',(15.9569667264609,4.13855771815389,99.2902945556315));
#29937=CARTESIAN_POINT('Ctrl Pts',(16.0853029468825,3.93703139748707,99.2037727159813));
#29938=CARTESIAN_POINT('Ctrl Pts',(16.3611041702218,3.56800652240011,98.9917454068753));
#29939=CARTESIAN_POINT('Ctrl Pts',(16.5057866639851,3.40359088922421,98.8686812585125));
#29940=CARTESIAN_POINT('Ctrl Pts',(16.8063661957351,3.10516780207624,98.5978506351621));
#29941=CARTESIAN_POINT('Ctrl Pts',(16.9629304851031,2.97086204840461,98.4493425737988));
#29942=CARTESIAN_POINT('Ctrl Pts',(17.122666505727,2.85087466042014,98.2928932188135));
#29943=CARTESIAN_POINT('Origin',(12.2482946431511,16.8583313034371,100.));
#29944=CARTESIAN_POINT('',(12.1768261122223,12.3708569010759,98.2928932196637));
#29945=CARTESIAN_POINT('',(12.1768261106186,12.3708569011015,0.5));
#29946=CARTESIAN_POINT('',(12.1768261106186,12.3708569011015,100.));
#29947=CARTESIAN_POINT('',(8.00253786221767,15.4036548377177,0.5));
#29948=CARTESIAN_POINT('Origin',(12.2482946431511,16.8583313034371,0.5));
#29949=CARTESIAN_POINT('',(8.00250696667699,15.4036606035888,98.2929148412894));
#29950=CARTESIAN_POINT('',(8.00253786221767,15.4036548377177,100.));
#29951=CARTESIAN_POINT('Ctrl Pts',(8.00250708598551,15.4036602554268,98.2929146461936));
#29952=CARTESIAN_POINT('Ctrl Pts',(8.04095434018177,15.291393927702,98.3858632379257));
#29953=CARTESIAN_POINT('Ctrl Pts',(8.08445379523924,15.1789643815694,98.4757075594465));
#29954=CARTESIAN_POINT('Ctrl Pts',(8.13349045375344,15.0664065104534,98.5618687047919));
#29955=CARTESIAN_POINT('Ctrl Pts',(8.14594002061313,15.0378299967899,98.583743542356));
#29956=CARTESIAN_POINT('Ctrl Pts',(8.15874627805921,15.0092451974279,98.6053811116386));
#29957=CARTESIAN_POINT('Ctrl Pts',(8.17191669602578,14.9806526573416,98.6267722404462));
#29958=CARTESIAN_POINT('Ctrl Pts',(8.19442659046237,14.9317844239531,98.6633323596894));
#29959=CARTESIAN_POINT('Ctrl Pts',(8.21808777573002,14.8827759730826,98.6992365502331));
#29960=CARTESIAN_POINT('Ctrl Pts',(8.24287820376329,14.8337655789499,98.7343285177238));
#29961=CARTESIAN_POINT('Ctrl Pts',(8.29540418081832,14.7299223200028,98.8086814041185));
#29962=CARTESIAN_POINT('Ctrl Pts',(8.35322906335348,14.6256182642871,98.8796681588396));
#29963=CARTESIAN_POINT('Ctrl Pts',(8.41624979623094,14.5221819933805,98.9457243517224));
#29964=CARTESIAN_POINT('Ctrl Pts',(8.45042299051297,14.4660933441359,98.981543533916));
#29965=CARTESIAN_POINT('Ctrl Pts',(8.48612332306307,14.4102605388777,99.0159124054391));
#29966=CARTESIAN_POINT('Ctrl Pts',(8.52333003766506,14.3548990672716,99.0485791162114));
#29967=CARTESIAN_POINT('Ctrl Pts',(8.54347127793547,14.3249300492255,99.0662627004124));
#29968=CARTESIAN_POINT('Ctrl Pts',(8.56405612172782,14.2950703500545,99.0834771132441));
#29969=CARTESIAN_POINT('Ctrl Pts',(8.58510094647066,14.2653257640177,99.100197897678));
#29970=CARTESIAN_POINT('Ctrl Pts',(8.64085775874532,14.1865195339774,99.1444984632641));
#29971=CARTESIAN_POINT('Ctrl Pts',(8.69986277604658,14.1084893186493,99.1853565450778));
#29972=CARTESIAN_POINT('Ctrl Pts',(8.76251977964181,14.0312399826539,99.2223453246317));
#29973=CARTESIAN_POINT('Ctrl Pts',(8.82234975489255,13.9574760680786,99.257665203309));
#29974=CARTESIAN_POINT('Ctrl Pts',(8.88550949800824,13.8844241448105,99.289457225426));
#29975=CARTESIAN_POINT('Ctrl Pts',(8.95238110252481,13.8120961796908,99.3173134272115));
#29976=CARTESIAN_POINT('Ctrl Pts',(8.96841979763654,13.7947488139592,99.3239945459111));
#29977=CARTESIAN_POINT('Ctrl Pts',(8.98467216422562,13.77744313058,99.3304490804175));
#29978=CARTESIAN_POINT('Ctrl Pts',(9.00114376230894,13.7601793662716,99.3366710553152));
#29979=CARTESIAN_POINT('Ctrl Pts',(9.01384496169295,13.7468673299112,99.3414688013104));
#29980=CARTESIAN_POINT('Ctrl Pts',(9.0266780465601,13.733584418606,99.3461220848251));
#29981=CARTESIAN_POINT('Ctrl Pts',(9.03963548955907,13.7203394312888,99.3506266622461));
#29982=CARTESIAN_POINT('Ctrl Pts',(9.11972744908153,13.6384701158563,99.3784701520841));
#29983=CARTESIAN_POINT('Ctrl Pts',(9.2042699094525,13.5583572449624,99.4004995600338));
#29984=CARTESIAN_POINT('Ctrl Pts',(9.29128918150769,13.4821421839037,99.4158205242226));
#29985=CARTESIAN_POINT('Ctrl Pts',(9.39222822782232,13.39373561147,99.4335922600383));
#29986=CARTESIAN_POINT('Ctrl Pts',(9.49729440462541,13.3096962059213,99.4426890000595));
#29987=CARTESIAN_POINT('Ctrl Pts',(9.60659271286559,13.2301161534923,99.4428904203957));
#29988=CARTESIAN_POINT('Ctrl Pts',(9.60682851186603,13.2299444683389,99.4428908549378));
#29989=CARTESIAN_POINT('Ctrl Pts',(9.60706433486258,13.2297728014511,99.4428912473282));
#29990=CARTESIAN_POINT('Ctrl Pts',(9.60730018182523,13.2296011528498,99.4428915975688));
#29991=CARTESIAN_POINT('Ctrl Pts',(9.68141111896967,13.1756634698734,99.443001654775));
#29992=CARTESIAN_POINT('Ctrl Pts',(9.75791369194048,13.1235161930199,99.4389375211787));
#29993=CARTESIAN_POINT('Ctrl Pts',(9.83576642335548,13.0738739726876,99.4307630339869));
#29994=CARTESIAN_POINT('Ctrl Pts',(9.87237363862743,13.0505316517021,99.4269192997091));
#29995=CARTESIAN_POINT('Ctrl Pts',(9.90927903494219,13.027742911758,99.4221673968387));
#29996=CARTESIAN_POINT('Ctrl Pts',(9.94637331208392,13.005580020478,99.4165172327955));
#29997=CARTESIAN_POINT('Ctrl Pts',(10.0295053402483,12.9559107387434,99.4038546435077));
#29998=CARTESIAN_POINT('Ctrl Pts',(10.1131220126551,12.9095945146256,99.3868321498127));
#29999=CARTESIAN_POINT('Ctrl Pts',(10.1970690548928,12.8664609300696,99.3658258363096));
#30000=CARTESIAN_POINT('Ctrl Pts',(10.2150684963252,12.8572124752308,99.3613217835219));
#30001=CARTESIAN_POINT('Ctrl Pts',(10.2330831050249,12.848110220653,99.356634731462));
#30002=CARTESIAN_POINT('Ctrl Pts',(10.2511113268446,12.8391523023418,99.3517686237608));
#30003=CARTESIAN_POINT('Ctrl Pts',(10.2669187778883,12.8312978474447,99.347501937893));
#30004=CARTESIAN_POINT('Ctrl Pts',(10.282743992679,12.8235507352674,99.3430956262505));
#30005=CARTESIAN_POINT('Ctrl Pts',(10.2985854655186,12.8159101990171,99.338552249982));
#30006=CARTESIAN_POINT('Ctrl Pts',(10.3738460618529,12.7796110922143,99.3169673120915));
#30007=CARTESIAN_POINT('Ctrl Pts',(10.4497789726769,12.7456422248509,99.2921178033808));
#30008=CARTESIAN_POINT('Ctrl Pts',(10.5258154870433,12.7140687420573,99.2644650244466));
#30009=CARTESIAN_POINT('Ctrl Pts',(10.5448521424921,12.7061639410775,99.257541818811));
#30010=CARTESIAN_POINT('Ctrl Pts',(10.5638953135331,12.6984091102545,99.250443088872));
#30011=CARTESIAN_POINT('Ctrl Pts',(10.5829361512678,12.6908049207666,99.2431764205676));
#30012=CARTESIAN_POINT('Ctrl Pts',(10.6820892558461,12.6512069258659,99.2053360307508));
#30013=CARTESIAN_POINT('Ctrl Pts',(10.7813009537869,12.6156428243816,99.162858290905));
#30014=CARTESIAN_POINT('Ctrl Pts',(10.8797010335179,12.5840907769962,99.1165798460081));
#30015=CARTESIAN_POINT('Ctrl Pts',(10.8915595472027,12.580288337133,99.1110026800788));
#30016=CARTESIAN_POINT('Ctrl Pts',(10.9034062979255,12.5765441851188,99.1053702615652));
#30017=CARTESIAN_POINT('Ctrl Pts',(10.9152397813687,12.5728582981514,99.0996840124348));
#30018=CARTESIAN_POINT('Ctrl Pts',(10.9496077250952,12.5621533897882,99.0831694593815));
#30019=CARTESIAN_POINT('Ctrl Pts',(10.9838534531501,12.5519431297429,99.0662118234553));
#30020=CARTESIAN_POINT('Ctrl Pts',(11.0179405472128,12.5422262222296,99.0488473569641));
#30021=CARTESIAN_POINT('Ctrl Pts',(11.1286979038281,12.510653598624,98.9924259323609));
#30022=CARTESIAN_POINT('Ctrl Pts',(11.2380248633315,12.4840338074687,98.9317993629735));
#30023=CARTESIAN_POINT('Ctrl Pts',(11.3461476367307,12.4618433879634,98.867503097581));
#30024=CARTESIAN_POINT('Ctrl Pts',(11.4178105089765,12.4471357630283,98.82488806924));
#30025=CARTESIAN_POINT('Ctrl Pts',(11.4889441178525,12.4343747574872,98.78066013646));
#30026=CARTESIAN_POINT('Ctrl Pts',(11.559611526168,12.4234165163235,98.7349665698168));
#30027=CARTESIAN_POINT('Ctrl Pts',(11.6130987298846,12.4151223720855,98.7003817284332));
#30028=CARTESIAN_POINT('Ctrl Pts',(11.6663040534072,12.4078631071804,98.6649661331023));
#30029=CARTESIAN_POINT('Ctrl Pts',(11.719279568674,12.4015749360366,98.6287647534646));
#30030=CARTESIAN_POINT('Ctrl Pts',(11.8108343641639,12.3907074207293,98.5661998139358));
#30031=CARTESIAN_POINT('Ctrl Pts',(11.9016543857213,12.3828242789131,98.5012454210128));
#30032=CARTESIAN_POINT('Ctrl Pts',(11.9914371355195,12.3776871588086,98.434460466144));
#30033=CARTESIAN_POINT('Ctrl Pts',(12.053768906968,12.3741207076031,98.3880949387745));
#30034=CARTESIAN_POINT('Ctrl Pts',(12.1156007258574,12.371878793004,98.3408460596394));
#30035=CARTESIAN_POINT('Ctrl Pts',(12.1768266918443,12.3708930987134,98.2928932168601));
#30036=CARTESIAN_POINT('Origin',(0.,20.8380434782609,100.));
#30037=CARTESIAN_POINT('',(2.57983136337907,17.1656216833844,98.292893216895));
#30038=CARTESIAN_POINT('',(2.57985201635105,17.1655922755232,0.5));
#30039=CARTESIAN_POINT('',(2.57985201635105,17.1655922755232,100.));
#30040=CARTESIAN_POINT('',(-2.57985201635105,17.1655922755232,0.5));
#30041=CARTESIAN_POINT('Origin',(0.,20.8380434782609,0.5));
#30042=CARTESIAN_POINT('',(-2.57983420291524,17.1656249920608,98.292899216665));
#30043=CARTESIAN_POINT('',(-2.57985201635105,17.1655922755232,100.));
#30044=CARTESIAN_POINT('Ctrl Pts',(-2.57983420291524,17.1656249920608,98.292899216665));
#30045=CARTESIAN_POINT('Ctrl Pts',(-2.48921168864423,17.1019995465654,98.3796187467316));
#30046=CARTESIAN_POINT('Ctrl Pts',(-2.39460451850736,17.0405846361727,98.4639979993656));
#30047=CARTESIAN_POINT('Ctrl Pts',(-2.29603754132725,16.9819052231592,98.5451592717579));
#30048=CARTESIAN_POINT('Ctrl Pts',(-2.20329025420896,16.9266904187451,98.6215285391212));
#30049=CARTESIAN_POINT('Ctrl Pts',(-2.10703651916376,16.8738971253407,98.6950495057151));
#30050=CARTESIAN_POINT('Ctrl Pts',(-2.00726888126077,16.8239841981514,98.7649644149767));
#30051=CARTESIAN_POINT('Ctrl Pts',(-1.91489692774296,16.7777712709219,98.829696595514));
#30052=CARTESIAN_POINT('Ctrl Pts',(-1.81951237795242,16.7340272983954,98.8913379369186));
#30053=CARTESIAN_POINT('Ctrl Pts',(-1.72108984756871,16.6931400079835,98.9492550268325));
#30054=CARTESIAN_POINT('Ctrl Pts',(-1.6625207684819,16.6688088824126,98.9837202108348));
#30055=CARTESIAN_POINT('Ctrl Pts',(-1.60287553638577,16.6454898253033,99.0168659278829));
#30056=CARTESIAN_POINT('Ctrl Pts',(-1.54214582819379,16.6232694009981,99.048551829993));
#30057=CARTESIAN_POINT('Ctrl Pts',(-1.50834082732675,16.6109004717661,99.0661896876445));
#30058=CARTESIAN_POINT('Ctrl Pts',(-1.47411579290757,16.5988458341413,99.0834087225826));
#30059=CARTESIAN_POINT('Ctrl Pts',(-1.43948739685437,16.5871278596483,99.1001725241582));
#30060=CARTESIAN_POINT('Ctrl Pts',(-1.33337731940238,16.5512210512842,99.1515410103233));
#30061=CARTESIAN_POINT('Ctrl Pts',(-1.22327810111083,16.5184071919005,99.198703593431));
#30062=CARTESIAN_POINT('Ctrl Pts',(-1.10980264464779,16.4894341821249,99.2404898931548));
#30063=CARTESIAN_POINT('Ctrl Pts',(-1.00858832430666,16.4635917349203,99.2777611415633));
#30064=CARTESIAN_POINT('Ctrl Pts',(-0.904688737109412,16.4408052848509,
99.310754288066));
#30065=CARTESIAN_POINT('Ctrl Pts',(-0.798561739816899,16.4216158026087,
99.3386147004669));
#30066=CARTESIAN_POINT('Ctrl Pts',(-0.780189286660266,16.4182937651197,
99.3434378287455));
#30067=CARTESIAN_POINT('Ctrl Pts',(-0.761769227147002,16.4150826446948,
99.3481021122732));
#30068=CARTESIAN_POINT('Ctrl Pts',(-0.743304007781183,16.4119834376879,
99.3526059457036));
#30069=CARTESIAN_POINT('Ctrl Pts',(-0.64264164986231,16.3950882425204,99.3771584020698));
#30070=CARTESIAN_POINT('Ctrl Pts',(-0.541062236509303,16.3815877737509,
99.3968131856337));
#30071=CARTESIAN_POINT('Ctrl Pts',(-0.438849030699141,16.371548910173,99.4114442249324));
#30072=CARTESIAN_POINT('Ctrl Pts',(-0.33846609919671,16.361689806871,99.4258132744509));
#30073=CARTESIAN_POINT('Ctrl Pts',(-0.237471337063981,16.3551693456484,
99.4353369845739));
#30074=CARTESIAN_POINT('Ctrl Pts',(-0.136124760075694,16.3520782871358,
99.4398549403142));
#30075=CARTESIAN_POINT('Ctrl Pts',(-0.0902193618173922,16.3506781779631,
99.4419013691502));
#30076=CARTESIAN_POINT('Ctrl Pts',(-0.0442417165702345,16.3499820578742,
99.4429202057482));
#30077=CARTESIAN_POINT('Ctrl Pts',(0.0017841408237108,16.3500003546257,
99.4428936080781));
#30078=CARTESIAN_POINT('Ctrl Pts',(0.00220644401206086,16.3500005225047,
99.4428933640352));
#30079=CARTESIAN_POINT('Ctrl Pts',(0.00262876716548417,16.3500007510009,
99.4428930314832));
#30080=CARTESIAN_POINT('Ctrl Pts',(0.00305111017540478,16.3500010401123,
99.4428926104267));
#30081=CARTESIAN_POINT('Ctrl Pts',(0.0947401221956442,16.35006380507,99.442801200709));
#30082=CARTESIAN_POINT('Ctrl Pts',(0.187323742145935,16.3529858671845,99.4385281272487));
#30083=CARTESIAN_POINT('Ctrl Pts',(0.279483658270004,16.3587250213916,99.4301496922833));
#30084=CARTESIAN_POINT('Ctrl Pts',(0.322405061819553,16.3613979030968,99.4262476250572));
#30085=CARTESIAN_POINT('Ctrl Pts',(0.365234463335138,16.3646813960552,99.4214557128977));
#30086=CARTESIAN_POINT('Ctrl Pts',(0.407839099050017,16.3685690648589,99.4157848279582));
#30087=CARTESIAN_POINT('Ctrl Pts',(0.504270395098256,16.3773684111049,99.402949351835));
#30088=CARTESIAN_POINT('Ctrl Pts',(0.599122429560623,16.3891631936075,99.3857576708374));
#30089=CARTESIAN_POINT('Ctrl Pts',(0.692370251099814,16.403725207301,99.3645857641517));
#30090=CARTESIAN_POINT('Ctrl Pts',(0.712154642536984,16.4068148299245,99.3600937204511));
#30091=CARTESIAN_POINT('Ctrl Pts',(0.731866869227064,16.4100289179404,99.3554226501132));
#30092=CARTESIAN_POINT('Ctrl Pts',(0.751506771534702,16.4133651287016,99.3505763727328));
#30093=CARTESIAN_POINT('Ctrl Pts',(0.768810980041277,16.4163045774693,99.346306443435));
#30094=CARTESIAN_POINT('Ctrl Pts',(0.786067148798632,16.4193402078322,99.3418984809087));
#30095=CARTESIAN_POINT('Ctrl Pts',(0.803274493993878,16.4224705426046,99.3373550074188));
#30096=CARTESIAN_POINT('Ctrl Pts',(0.885066655452863,16.4373500515712,99.3157583861473));
#30097=CARTESIAN_POINT('Ctrl Pts',(0.96604236690926,16.4544870049828,99.290930482352));
#30098=CARTESIAN_POINT('Ctrl Pts',(1.0457055825963,16.4736021418813,99.2633292101938));
#30099=CARTESIAN_POINT('Ctrl Pts',(1.06594962073236,16.4784596856926,99.2563151673717));
#30100=CARTESIAN_POINT('Ctrl Pts',(1.08610902531913,16.4834448422345,99.2491222220252));
#30101=CARTESIAN_POINT('Ctrl Pts',(1.10617593665823,16.4885527780128,99.241758252988));
#30102=CARTESIAN_POINT('Ctrl Pts',(1.21067589744461,16.5151527404838,99.2034098264354));
#30103=CARTESIAN_POINT('Ctrl Pts',(1.31279762676775,16.5451132691219,99.1603383186916));
#30104=CARTESIAN_POINT('Ctrl Pts',(1.41181620443827,16.5778827216941,99.113413096964));
#30105=CARTESIAN_POINT('Ctrl Pts',(1.42237752838734,16.5813779123178,99.1084080516512));
#30106=CARTESIAN_POINT('Ctrl Pts',(1.43290355852021,16.584905080957,99.1033591232951));
#30107=CARTESIAN_POINT('Ctrl Pts',(1.4433934209195,16.5884635738797,99.0982673376954));
#30108=CARTESIAN_POINT('Ctrl Pts',(1.47741610194125,16.6000051427791,99.0817527075989));
#30109=CARTESIAN_POINT('Ctrl Pts',(1.51105031263543,16.6118734917002,99.0647972731996));
#30110=CARTESIAN_POINT('Ctrl Pts',(1.54426705507019,16.6240461436619,99.0474373027683));
#30111=CARTESIAN_POINT('Ctrl Pts',(1.65397005247796,16.6642480511552,98.9901035411882));
#30112=CARTESIAN_POINT('Ctrl Pts',(1.75949463037048,16.7077102057661,98.928440958183));
#30113=CARTESIAN_POINT('Ctrl Pts',(1.86134539405867,16.7541279962493,98.8630104837217));
#30114=CARTESIAN_POINT('Ctrl Pts',(1.92596432906305,16.7835776348937,98.821498300372));
#30115=CARTESIAN_POINT('Ctrl Pts',(1.98910378653781,16.814217470161,98.778468651494));
#30116=CARTESIAN_POINT('Ctrl Pts',(2.05088633004559,16.8459741993694,98.7340573318784));
#30117=CARTESIAN_POINT('Ctrl Pts',(2.09899196596664,16.8707008869838,98.6994774222324));
#30118=CARTESIAN_POINT('Ctrl Pts',(2.14626276029161,16.8960982022606,98.6640680699515));
#30119=CARTESIAN_POINT('Ctrl Pts',(2.19277810448148,16.9221453115834,98.6278739858466));
#30120=CARTESIAN_POINT('Ctrl Pts',(2.2732023258085,16.967180310713,98.5652950437475));
#30121=CARTESIAN_POINT('Ctrl Pts',(2.35127746874125,17.0141953608528,98.5003303240798));
#30122=CARTESIAN_POINT('Ctrl Pts',(2.42689938961185,17.0628202892553,98.4335380214889));
#30123=CARTESIAN_POINT('Ctrl Pts',(2.47905924695026,17.0963591004805,98.3874683510239));
#30124=CARTESIAN_POINT('Ctrl Pts',(2.53005139469532,17.1306646048509,98.3405281736981));
#30125=CARTESIAN_POINT('Ctrl Pts',(2.57983136337907,17.1656216833844,98.292893216895));
#30126=CARTESIAN_POINT('Ctrl Pts',(7.61153061250581,15.7863147967496,98.4745004885114));
#30127=CARTESIAN_POINT('Ctrl Pts',(7.88836095469125,15.7787835827682,98.3610536502059));
#30128=CARTESIAN_POINT('Ctrl Pts',(7.9381581147024,15.6072288420487,98.1209470979181));
#30129=CARTESIAN_POINT('Ctrl Pts',(7.68185024283006,15.5529265513645,98.6541872523935));
#30130=CARTESIAN_POINT('Ctrl Pts',(7.94367437493435,15.5575146677548,98.5339912542893));
#30131=CARTESIAN_POINT('Ctrl Pts',(7.99873405832662,15.3985404288948,98.3006281519141));
#30132=CARTESIAN_POINT('Ctrl Pts',(7.77058558273983,15.3193429185922,98.8238114502906));
#30133=CARTESIAN_POINT('Ctrl Pts',(8.01739572281313,15.3332616605645,98.6995854322395));
#30134=CARTESIAN_POINT('Ctrl Pts',(8.07554514465371,15.1898709314151,98.4702580602194));
#30135=CARTESIAN_POINT('Ctrl Pts',(7.99242980712988,14.8502894771665,99.1368088098188));
#30136=CARTESIAN_POINT('Ctrl Pts',(8.20881182371915,14.8837031652933,99.0046294469941));
#30137=CARTESIAN_POINT('Ctrl Pts',(8.26829617652396,14.7714171710724,98.7832554187034));
#30138=CARTESIAN_POINT('Ctrl Pts',(8.12737169382821,14.6123994681448,99.2813501417123));
#30139=CARTESIAN_POINT('Ctrl Pts',(8.327762510152,14.6553398972786,99.1461712456963));
#30140=CARTESIAN_POINT('Ctrl Pts',(8.38583875689921,14.5594769234819,98.9277967516668));
#30141=CARTESIAN_POINT('Ctrl Pts',(8.44228186665902,14.1522925726334,99.5228530262281));
#30142=CARTESIAN_POINT('Ctrl Pts',(8.61067658867425,14.2156092191238,99.3819067332058));
#30143=CARTESIAN_POINT('Ctrl Pts',(8.66083652547866,14.1502985880832,99.1692996350871));
#30144=CARTESIAN_POINT('Ctrl Pts',(8.622381227697,13.9285751457638,99.6211970158389));
#30145=CARTESIAN_POINT('Ctrl Pts',(8.77477430608659,14.0016497079293,99.4784987699955));
#30146=CARTESIAN_POINT('Ctrl Pts',(8.81839581871033,13.9517156783975,99.2676436259638));
#30147=CARTESIAN_POINT('Ctrl Pts',(8.93504150578053,13.6041086188711,99.7247006505005));
#30148=CARTESIAN_POINT('Ctrl Pts',(9.062909374557,13.6933479875451,99.5798189693937));
#30149=CARTESIAN_POINT('Ctrl Pts',(9.09252380741147,13.6644048462732,99.3711472595481));
#30150=CARTESIAN_POINT('Ctrl Pts',(9.04643201266469,13.4980463524892,99.7515464581428));
#30151=CARTESIAN_POINT('Ctrl Pts',(9.16590083805353,13.5929484631972,99.6061008493641));
#30152=CARTESIAN_POINT('Ctrl Pts',(9.19027681092598,13.5706128359882,99.397993067634));
#30153=CARTESIAN_POINT('Ctrl Pts',(9.27641719553063,13.2976623200444,99.7871410858034));
#30154=CARTESIAN_POINT('Ctrl Pts',(9.37920676320414,13.4041562061325,99.6408876188391));
#30155=CARTESIAN_POINT('Ctrl Pts',(9.39230696146117,13.3936667965264,99.4335876951257));
#30156=CARTESIAN_POINT('Ctrl Pts',(9.3959224352673,13.2023470673548,99.7962421951754));
#30157=CARTESIAN_POINT('Ctrl Pts',(9.49053581390408,13.314627456823,99.6498002056397));
#30158=CARTESIAN_POINT('Ctrl Pts',(9.4973820058399,13.3096324234838,99.4426888046372));
#30159=CARTESIAN_POINT('Ctrl Pts',(9.64409776558328,13.0216618073134,99.7966442229662));
#30160=CARTESIAN_POINT('Ctrl Pts',(9.72219875439392,13.1459331194971,99.6501931431456));
#30161=CARTESIAN_POINT('Ctrl Pts',(9.71580342119465,13.1505998825527,99.4430908323178));
#30162=CARTESIAN_POINT('Ctrl Pts',(9.77381197449083,12.9356824620425,99.7877849805069));
#30163=CARTESIAN_POINT('Ctrl Pts',(9.84373626500592,13.066044592077,99.6415170968012));
#30164=CARTESIAN_POINT('Ctrl Pts',(9.83007072703063,13.0750678730396,99.4342315896588));
#30165=CARTESIAN_POINT('Ctrl Pts',(10.0376062905058,12.7771593103382,99.7523547967176));
#30166=CARTESIAN_POINT('Ctrl Pts',(10.0912047848047,12.9199070101992,99.606890957529));
#30167=CARTESIAN_POINT('Ctrl Pts',(10.0626757487172,12.9360922565949,99.3988014063792));
#30168=CARTESIAN_POINT('Ctrl Pts',(10.1706575690794,12.7050827268414,99.7260859669308));
#30169=CARTESIAN_POINT('Ctrl Pts',(10.2163999615547,12.8539677361419,99.581174605592));
#30170=CARTESIAN_POINT('Ctrl Pts',(10.1801044201997,12.8730550738083,99.3725325760877));
#30171=CARTESIAN_POINT('Ctrl Pts',(10.5730247519988,12.5085765171446,99.6241384720945));
#30172=CARTESIAN_POINT('Ctrl Pts',(10.5959433339676,12.6756716426711,99.4813799591424));
#30173=CARTESIAN_POINT('Ctrl Pts',(10.5355461919893,12.7016211074059,99.2705850820007));
#30174=CARTESIAN_POINT('Ctrl Pts',(10.8489658974355,12.4029669023367,99.5236562902281));
#30175=CARTESIAN_POINT('Ctrl Pts',(10.8572640774196,12.5825975767439,99.3826839740385));
#30176=CARTESIAN_POINT('Ctrl Pts',(10.7797437745,12.610127671606,99.1701028989522));
#30177=CARTESIAN_POINT('Ctrl Pts',(11.386390404632,12.2448379356151,99.281082704477));
#30178=CARTESIAN_POINT('Ctrl Pts',(11.3652836467711,12.4487162064099,99.1459030339923));
#30179=CARTESIAN_POINT('Ctrl Pts',(11.256110836745,12.4743323246936,98.9275293145664));
#30180=CARTESIAN_POINT('Ctrl Pts',(11.6491602608155,12.1909944678527,99.1393951997099));
#30181=CARTESIAN_POINT('Ctrl Pts',(11.6143348897634,12.4069069268349,99.0071411174895));
#30182=CARTESIAN_POINT('Ctrl Pts',(11.489403766598,12.4288617015343,98.7858418086567));
#30183=CARTESIAN_POINT('Ctrl Pts',(12.1662817650119,12.1242950353392,98.825202900069));
#30184=CARTESIAN_POINT('Ctrl Pts',(12.1033811314414,12.3632333592681,98.7009299069312));
#30185=CARTESIAN_POINT('Ctrl Pts',(11.9491322142495,12.3742909202748,98.4716495099356));
#30186=CARTESIAN_POINT('Ctrl Pts',(12.4202878510312,12.1120529425571,98.6524117207793));
#30187=CARTESIAN_POINT('Ctrl Pts',(12.3435537205772,12.3625816382562,98.5323055644749));
#30188=CARTESIAN_POINT('Ctrl Pts',(12.1752607824306,12.3657340555541,98.2988642625951));
#30189=CARTESIAN_POINT('Ctrl Pts',(12.6613982812294,12.1172313198433,98.4746383405503));
#30190=CARTESIAN_POINT('Ctrl Pts',(12.5687009849841,12.378177146358,98.3611876972422));
#30191=CARTESIAN_POINT('Ctrl Pts',(12.3901642949232,12.3725306764959,98.121084949957));
#30192=CARTESIAN_POINT('Ctrl Pts',(12.1768261122223,12.3708569010759,98.2928932196637));
#30193=CARTESIAN_POINT('Ctrl Pts',(12.2099878174149,12.3703287601505,98.3104738976694));
#30194=CARTESIAN_POINT('Ctrl Pts',(12.2429433132094,12.366507919976,98.327944020444));
#30195=CARTESIAN_POINT('Ctrl Pts',(12.2752735670645,12.3594661072471,98.3450378051381));
#30196=CARTESIAN_POINT('Ctrl Pts',(12.3046862235392,12.3530597728063,98.360588985754));
#30197=CARTESIAN_POINT('Ctrl Pts',(12.3335840639558,12.3439862285568,98.3758286876098));
#30198=CARTESIAN_POINT('Ctrl Pts',(12.3616325402612,12.3322664746469,98.3905567852375));
#30199=CARTESIAN_POINT('Ctrl Pts',(12.3872721168772,12.3215532535428,98.404019983146));
#30200=CARTESIAN_POINT('Ctrl Pts',(12.4122030444781,12.3086274763191,98.4170556799153));
#30201=CARTESIAN_POINT('Ctrl Pts',(12.4361292621088,12.2934948895151,98.429511010888));
#30202=CARTESIAN_POINT('Ctrl Pts',(12.4577825179125,12.2797998802121,98.4407831004357));
#30203=CARTESIAN_POINT('Ctrl Pts',(12.4786130500859,12.2642963979525,98.4515798546202));
#30204=CARTESIAN_POINT('Ctrl Pts',(12.4983593286873,12.2469958685832,98.4617879670104));
#30205=CARTESIAN_POINT('Ctrl Pts',(12.5081070139959,12.2384555193169,98.4668271680256));
#30206=CARTESIAN_POINT('Ctrl Pts',(12.5175897865895,12.2294774556221,98.4717229246488));
#30207=CARTESIAN_POINT('Ctrl Pts',(12.5267717721302,12.2200650149237,98.4764616066469));
#30208=CARTESIAN_POINT('Origin',(7.52738542590446,15.2389652387019,98.280871015943));
#30209=CARTESIAN_POINT('Origin',(12.1688640072122,11.8709203002116,100.));
#30210=CARTESIAN_POINT('Ctrl Pts',(12.1768261106186,12.3708569011015,0.5));
#30211=CARTESIAN_POINT('Ctrl Pts',(12.1778203104535,12.37084106725,0.498951748855235));
#30212=CARTESIAN_POINT('Ctrl Pts',(12.1788144663232,12.3708222676705,0.497903494267714));
#30213=CARTESIAN_POINT('Ctrl Pts',(12.2687615400859,12.3688529339418,0.403057585612054));
#30214=CARTESIAN_POINT('Ctrl Pts',(12.3562405730693,12.3432084553889,0.310543821638481));
#30215=CARTESIAN_POINT('Ctrl Pts',(12.467152867614,12.2742120695516,0.195519413317804));
#30216=CARTESIAN_POINT('Ctrl Pts',(12.4986401261746,12.2489027263458,0.1632025467695));
#30217=CARTESIAN_POINT('Ctrl Pts',(12.5267717721302,12.2200650149237,0.134720657333169));
#30218=CARTESIAN_POINT('Origin',(7.52953032547043,15.2415935216047,100.));
#30219=CARTESIAN_POINT('Ctrl Pts',(7.75098709974897,15.6898756840048,0.134720657333167));
#30220=CARTESIAN_POINT('Ctrl Pts',(7.78710654979212,15.6720322417129,0.163202546769546));
#30221=CARTESIAN_POINT('Ctrl Pts',(7.82090726357265,15.6499070964456,0.195519413317857));
#30222=CARTESIAN_POINT('Ctrl Pts',(7.92080050982121,15.5657442917577,0.310543821635948));
#30223=CARTESIAN_POINT('Ctrl Pts',(7.97222236610058,15.4904713670851,0.403057585608259));
#30224=CARTESIAN_POINT('Ctrl Pts',(8.00189048816382,15.4055351740487,0.4979034942676));
#30225=CARTESIAN_POINT('Ctrl Pts',(8.00221557868522,15.4045954850201,0.498951748855171));
#30226=CARTESIAN_POINT('Ctrl Pts',(8.00253786221767,15.4036548377177,0.5));
#30227=CARTESIAN_POINT('Origin',(12.2482946431511,16.8583313034371,0.5));
#30228=CARTESIAN_POINT('Ctrl Pts',(17.3143275674006,2.71461308502431,98.1029310400785));
#30229=CARTESIAN_POINT('Ctrl Pts',(17.4636977396689,2.61423858413124,98.3435819247051));
#30230=CARTESIAN_POINT('Ctrl Pts',(17.3857742403068,2.34690286052699,98.4565369100693));
#30231=CARTESIAN_POINT('Ctrl Pts',(17.1296512858619,2.83873298501121,98.287884067932));
#30232=CARTESIAN_POINT('Ctrl Pts',(17.2651608223732,2.73703317193548,98.5214982032519));
#30233=CARTESIAN_POINT('Ctrl Pts',(17.1800764226929,2.48819271337626,98.641483434387));
#30234=CARTESIAN_POINT('Ctrl Pts',(16.9451136614474,2.98310069417807,98.4673409000312));
#30235=CARTESIAN_POINT('Ctrl Pts',(17.0639661472453,2.88326764438849,98.6966806272835));
#30236=CARTESIAN_POINT('Ctrl Pts',(16.9743943558493,2.65255720272719,98.8209468545489));
#30237=CARTESIAN_POINT('Ctrl Pts',(16.5997101391575,3.30279942760431,98.786605947879));
#30238=CARTESIAN_POINT('Ctrl Pts',(16.6878268341946,3.21163443205183,99.007927768118));
#30239=CARTESIAN_POINT('Ctrl Pts',(16.5890378089607,3.01654651232656,99.1402125820164));
#30240=CARTESIAN_POINT('Ctrl Pts',(16.4374762686561,3.47698561123582,98.9284804941304));
#30241=CARTESIAN_POINT('Ctrl Pts',(16.5106768516082,3.39212226298075,99.1468659074354));
#30242=CARTESIAN_POINT('Ctrl Pts',(16.4078485131262,3.21487371577908,99.28208744884));
#30243=CARTESIAN_POINT('Ctrl Pts',(16.2075579278768,3.77068327953469,99.1108598027282));
#30244=CARTESIAN_POINT('Ctrl Pts',(16.2598042688104,3.69971142057243,99.3254864613232));
#30245=CARTESIAN_POINT('Ctrl Pts',(16.1506324221162,3.54922452427067,99.4644671720462));
#30246=CARTESIAN_POINT('Ctrl Pts',(16.1328338869385,3.87465067488052,99.1667281040791));
#30247=CARTESIAN_POINT('Ctrl Pts',(16.1785346664591,3.80861210815899,99.3801095631261));
#30248=CARTESIAN_POINT('Ctrl Pts',(16.0669575425481,3.66757422893044,99.5203355960162));
#30249=CARTESIAN_POINT('Ctrl Pts',(15.9919866048144,4.08994756745576,99.2638527346785));
#30250=CARTESIAN_POINT('Ctrl Pts',(16.0257056636235,4.03466861210541,99.4749661095219));
#30251=CARTESIAN_POINT('Ctrl Pts',(15.9090517391356,3.91261572849131,99.6174604374823));
#30252=CARTESIAN_POINT('Ctrl Pts',(15.9254898327247,4.20166713029547,99.305439932531));
#30253=CARTESIAN_POINT('Ctrl Pts',(15.953587399343,4.15233969324182,99.5156582141651));
#30254=CARTESIAN_POINT('Ctrl Pts',(15.8344036945523,4.03975173211327,99.6590477275202));
#30255=CARTESIAN_POINT('Ctrl Pts',(15.7386039884752,4.55006349017908,99.4071746058889));
#30256=CARTESIAN_POINT('Ctrl Pts',(15.7519852189442,4.51914563857043,99.6148745113223));
#30257=CARTESIAN_POINT('Ctrl Pts',(15.6242698911525,4.43612723332498,99.7607826165547));
#30258=CARTESIAN_POINT('Ctrl Pts',(15.6300705661688,4.80379339451689,99.4435386777496));
#30259=CARTESIAN_POINT('Ctrl Pts',(15.6349263242122,4.78871307695064,99.6506668510312));
#30260=CARTESIAN_POINT('Ctrl Pts',(15.5017253412089,4.72466850699764,99.7971467765045));
#30261=CARTESIAN_POINT('Ctrl Pts',(15.5059824861585,5.18799157661501,99.442502700397));
#30262=CARTESIAN_POINT('Ctrl Pts',(15.5033523953774,5.19622875259004,99.6496543232893));
#30263=CARTESIAN_POINT('Ctrl Pts',(15.3607119866152,5.16119508122743,99.7961107967628));
#30264=CARTESIAN_POINT('Ctrl Pts',(15.4705223787628,5.31743764272476,99.4333242900205));
#30265=CARTESIAN_POINT('Ctrl Pts',(15.466074874266,5.333778711027,99.6406660872408));
#30266=CARTESIAN_POINT('Ctrl Pts',(15.3202268375056,5.30821065016257,99.7869323657971));
#30267=CARTESIAN_POINT('Ctrl Pts',(15.4112870235324,5.57906517882989,99.3975703058088));
#30268=CARTESIAN_POINT('Ctrl Pts',(15.4046994857704,5.61160402086349,99.605723827768));
#30269=CARTESIAN_POINT('Ctrl Pts',(15.2521751775211,5.6051982497642,99.751178303339));
#30270=CARTESIAN_POINT('Ctrl Pts',(15.3873774999491,5.71249818528157,99.3706193994188));
#30271=CARTESIAN_POINT('Ctrl Pts',(15.3804432938943,5.75346933726163,99.5793392014518));
#30272=CARTESIAN_POINT('Ctrl Pts',(15.2244484235508,5.75658897920106,99.7242273368567));
#30273=CARTESIAN_POINT('Ctrl Pts',(15.3346696945248,6.10616299653768,99.2668124456041));
#30274=CARTESIAN_POINT('Ctrl Pts',(15.3287678592424,6.17236078267489,99.4777222783444));
#30275=CARTESIAN_POINT('Ctrl Pts',(15.1624256089297,6.20298061454619,99.6204201490477));
#30276=CARTESIAN_POINT('Ctrl Pts',(15.3240667024475,6.35937968875434,99.1683014346687));
#30277=CARTESIAN_POINT('Ctrl Pts',(15.3219320743537,6.4418547297802,99.3809681438969));
#30278=CARTESIAN_POINT('Ctrl Pts',(15.1483769580277,6.48977650021848,99.5219089068378));
#30279=CARTESIAN_POINT('Ctrl Pts',(15.3423230787144,6.8517981468714,98.9266153300884));
#30280=CARTESIAN_POINT('Ctrl Pts',(15.3517693972099,6.96362633911536,99.1450562468822));
#30281=CARTESIAN_POINT('Ctrl Pts',(15.1643067184422,7.04682949241163,99.2802222813138));
#30282=CARTESIAN_POINT('Ctrl Pts',(15.3719403060826,7.09247220631589,98.7818489409675));
#30283=CARTESIAN_POINT('Ctrl Pts',(15.3899215235328,7.21841417521577,99.0032991843689));
#30284=CARTESIAN_POINT('Ctrl Pts',(15.1951156833261,7.31874252774784,99.1354555654036));
#30285=CARTESIAN_POINT('Ctrl Pts',(15.4635565836047,7.55131386473068,98.4637529208263));
#30286=CARTESIAN_POINT('Ctrl Pts',(15.5012645827149,7.70215187781829,98.6931970174467));
#30287=CARTESIAN_POINT('Ctrl Pts',(15.2930580254608,7.83652577457457,98.817358868105));
#30288=CARTESIAN_POINT('Ctrl Pts',(15.5265390080798,7.771324565253,98.288422358758));
#30289=CARTESIAN_POINT('Ctrl Pts',(15.5763509023311,7.93321211466989,98.5220290043357));
#30290=CARTESIAN_POINT('Ctrl Pts',(15.3612680514934,8.08445864294548,98.6420342839988));
#30291=CARTESIAN_POINT('Ctrl Pts',(15.6032141429119,7.98099597100254,98.1028819381727));
#30292=CARTESIAN_POINT('Ctrl Pts',(15.6650624954954,8.15000252629558,98.3435328809189));
#30293=CARTESIAN_POINT('Ctrl Pts',(15.4448833406996,8.32048399603211,98.4564865387793));
#30294=CARTESIAN_POINT('Ctrl Pts',(17.1226665060507,2.85087466017704,98.292893219028));
#30295=CARTESIAN_POINT('Ctrl Pts',(17.1491844558261,2.83095542391965,98.3104738971227));
#30296=CARTESIAN_POINT('Ctrl Pts',(17.1736001786239,2.80849354482898,98.3279440199826));
#30297=CARTESIAN_POINT('Ctrl Pts',(17.1956168298849,2.78379335217174,98.3450378047574));
#30298=CARTESIAN_POINT('Ctrl Pts',(17.2156466199956,2.76132219301346,98.3605889854151));
#30299=CARTESIAN_POINT('Ctrl Pts',(17.2336921685704,2.73699581706788,98.37582868731));
#30300=CARTESIAN_POINT('Ctrl Pts',(17.2494951641239,2.71102785622515,98.3905567849746));
#30301=CARTESIAN_POINT('Ctrl Pts',(17.2639409440128,2.68729011326205,98.4040199829058));
#30302=CARTESIAN_POINT('Ctrl Pts',(17.2765129069447,2.66217890823152,98.4170556796967));
#30303=CARTESIAN_POINT('Ctrl Pts',(17.2869749123056,2.63587291044608,98.4295110106904));
#30304=CARTESIAN_POINT('Ctrl Pts',(17.2964430397672,2.61206595074306,98.4407831002524));
#30305=CARTESIAN_POINT('Ctrl Pts',(17.3041825760947,2.58727949049788,98.4515798544512));
#30306=CARTESIAN_POINT('Ctrl Pts',(17.3099886550643,2.56167649685877,98.4617879668562));
#30307=CARTESIAN_POINT('Ctrl Pts',(17.3128548068259,2.54903766337002,98.4668271679255));
#30308=CARTESIAN_POINT('Ctrl Pts',(17.3152493576036,2.53620042325289,98.4717229246001));
#30309=CARTESIAN_POINT('Ctrl Pts',(17.3171452461371,2.52318856294818,98.4764616066469));
#30310=CARTESIAN_POINT('Origin',(15.0469618583329,7.90408080223432,98.2808650734389));
#30311=CARTESIAN_POINT('Origin',(16.822369667676,2.45109746114966,100.));
#30312=CARTESIAN_POINT('Ctrl Pts',(17.122666505727,2.85087466042014,0.5));
#30313=CARTESIAN_POINT('Ctrl Pts',(17.1234615233843,2.85027747456484,0.498951748855993));
#30314=CARTESIAN_POINT('Ctrl Pts',(17.1242547622613,2.84967791522767,0.497903494266448));
#30315=CARTESIAN_POINT('Ctrl Pts',(17.1958659280646,2.79521512743788,0.403057585878129));
#30316=CARTESIAN_POINT('Ctrl Pts',(17.2515645061738,2.72304942307884,0.31054382181288));
#30317=CARTESIAN_POINT('Ctrl Pts',(17.3007393793639,2.60203756316583,0.195519413314306));
#30318=CARTESIAN_POINT('Ctrl Pts',(17.3113366479633,2.56305412818084,0.163202546767945));
#30319=CARTESIAN_POINT('Ctrl Pts',(17.3171452461371,2.52318856294818,0.134720657333154));
#30320=CARTESIAN_POINT('Origin',(15.0503018864028,7.90496129833282,100.));
#30321=CARTESIAN_POINT('Ctrl Pts',(15.4929578242382,8.13746016004849,0.134720657333155));
#30322=CARTESIAN_POINT('Ctrl Pts',(15.5116909609202,8.10179403194187,0.163202546767978));
#30323=CARTESIAN_POINT('Ctrl Pts',(15.5260314786972,8.06402685234251,0.195519413314386));
#30324=CARTESIAN_POINT('Ctrl Pts',(15.557377157194,7.93722193592991,0.310543821792654));
#30325=CARTESIAN_POINT('Ctrl Pts',(15.5547339976961,7.84609985190388,0.403057585847384));
#30326=CARTESIAN_POINT('Ctrl Pts',(15.5288117710301,7.75994654384289,0.497903494266064));
#30327=CARTESIAN_POINT('Ctrl Pts',(15.5285224394342,7.75899523603605,0.498951748855763));
#30328=CARTESIAN_POINT('Ctrl Pts',(15.5282302736771,7.75804480287584,0.5));
#30329=CARTESIAN_POINT('Origin',(19.8181570368417,6.43930956430664,0.5));
#30330=CARTESIAN_POINT('Ctrl Pts',(17.3656407514415,-2.36084587016586,98.4746163542476));
#30331=CARTESIAN_POINT('Ctrl Pts',(17.4440265737737,-2.62644363351055,98.3611663178014));
#30332=CARTESIAN_POINT('Ctrl Pts',(17.2962665385767,-2.72681679293049,98.1210629636544));
#30333=CARTESIAN_POINT('Ctrl Pts',(16.9690963360069,-2.63613637636299,98.8304618827584));
#30334=CARTESIAN_POINT('Ctrl Pts',(17.0649442889613,-2.86366294455655,98.7002300650184));
#30335=CARTESIAN_POINT('Ctrl Pts',(16.9402678976059,-2.96864610960458,98.4769098403642));
#30336=CARTESIAN_POINT('Ctrl Pts',(16.579352085484,-2.99263453637889,99.1602382875981));
#30337=CARTESIAN_POINT('Ctrl Pts',(16.6807262887858,-3.184238518665,99.0255494138259));
#30338=CARTESIAN_POINT('Ctrl Pts',(16.5907862689851,-3.28173103979709,98.8066848982746));
#30339=CARTESIAN_POINT('Ctrl Pts',(16.06825893873,-3.65601467024647,99.5229830380903));
#30340=CARTESIAN_POINT('Ctrl Pts',(16.1805213417482,-3.79657900263654,99.3820315078356));
#30341=CARTESIAN_POINT('Ctrl Pts',(16.1339186653847,-3.8644611469686,99.1694296468622));
#30342=CARTESIAN_POINT('Ctrl Pts',(15.9074663690947,-3.90241128133998,99.6234913693261));
#30343=CARTESIAN_POINT('Ctrl Pts',(16.0241813784631,-4.02429095582515,99.480742609552));
#30344=CARTESIAN_POINT('Ctrl Pts',(15.9904645360934,-4.08092818635296,99.2699379792835));
#30345=CARTESIAN_POINT('Ctrl Pts',(15.6245522069462,-4.43521068708324,99.7608048122965));
#30346=CARTESIAN_POINT('Ctrl Pts',(15.7522284341321,-4.51825273440788,99.6149071958598));
#30347=CARTESIAN_POINT('Ctrl Pts',(15.738838796464,-4.54924202639042,99.4072514211525));
#30348=CARTESIAN_POINT('Ctrl Pts',(15.5044462303209,-4.71763971050874,99.7966027452518));
#30349=CARTESIAN_POINT('Ctrl Pts',(15.637469741455,-4.7821404952998,99.6501526042829));
#30350=CARTESIAN_POINT('Ctrl Pts',(15.6324601989204,-4.79760023853972,99.4430493547679));
#30351=CARTESIAN_POINT('Ctrl Pts',(15.3625803721861,-5.15483225994623,99.79636776423));
#30352=CARTESIAN_POINT('Ctrl Pts',(15.5050490252728,-5.19027311193596,99.6499229371967));
#30353=CARTESIAN_POINT('Ctrl Pts',(15.5076044740505,-5.18238705961208,99.442814373582));
#30354=CARTESIAN_POINT('Ctrl Pts',(15.3211549463132,-5.30458937654577,99.7872514480855));
#30355=CARTESIAN_POINT('Ctrl Pts',(15.4668882655262,-5.33038662434131,99.6409952531274));
#30356=CARTESIAN_POINT('Ctrl Pts',(15.4713150290528,-5.31424796399517,99.4336980572382));
#30357=CARTESIAN_POINT('Ctrl Pts',(15.2524387792612,-5.60380285207576,99.7514230350794));
#30358=CARTESIAN_POINT('Ctrl Pts',(15.4048955461524,-5.61029467639232,99.6059800049562));
#30359=CARTESIAN_POINT('Ctrl Pts',(15.4114951404923,-5.57783990353114,99.3978696447402));
#30360=CARTESIAN_POINT('Ctrl Pts',(15.225232210421,-5.75229303761941,99.7250021223377));
#30361=CARTESIAN_POINT('Ctrl Pts',(15.3810929371293,-5.74943839640601,99.580115086457));
#30362=CARTESIAN_POINT('Ctrl Pts',(15.3880333336981,-5.70871875235854,99.3714487314956));
#30363=CARTESIAN_POINT('Ctrl Pts',(15.1632690619364,-6.19474020261596,99.6227146850679));
#30364=CARTESIAN_POINT('Ctrl Pts',(15.3293788683914,-6.16461669902609,99.4799874409064));
#30365=CARTESIAN_POINT('Ctrl Pts',(15.335349988799,-6.09890683169226,99.2691612949723));
#30366=CARTESIAN_POINT('Ctrl Pts',(15.1483715649769,-6.48916504798079,99.522165658859));
#30367=CARTESIAN_POINT('Ctrl Pts',(15.3218719375042,-6.44129651453827,99.3812294188918));
#30368=CARTESIAN_POINT('Ctrl Pts',(15.3240366258068,-6.35885837698108,99.1686122675856));
#30369=CARTESIAN_POINT('Ctrl Pts',(15.1643710385717,-7.047829358343,99.279753346815));
#30370=CARTESIAN_POINT('Ctrl Pts',(15.3518153879027,-6.96458278973335,99.1446071116389));
#30371=CARTESIAN_POINT('Ctrl Pts',(15.3423676517735,-6.8527101484055,98.9261999569019));
#30372=CARTESIAN_POINT('Ctrl Pts',(15.1944125118879,-7.31378505933127,99.138252154167));
#30373=CARTESIAN_POINT('Ctrl Pts',(15.3890461250774,-7.21380562024091,99.0060308920462));
#30374=CARTESIAN_POINT('Ctrl Pts',(15.371253945164,-7.08811389017374,98.7846987631153));
#30375=CARTESIAN_POINT('Ctrl Pts',(15.290724890162,-7.8251126253835,98.8245648611892));
#30376=CARTESIAN_POINT('Ctrl Pts',(15.4985537486393,-7.69138492458423,98.7003130263028));
#30377=CARTESIAN_POINT('Ctrl Pts',(15.461363297308,-7.54123627293857,98.4710114710543));
#30378=CARTESIAN_POINT('Ctrl Pts',(15.3574639152262,-8.06994831582715,98.6521093612505));
#30379=CARTESIAN_POINT('Ctrl Pts',(15.5720250893885,-7.91951631844379,98.5320184901569));
#30380=CARTESIAN_POINT('Ctrl Pts',(15.5230000877303,-7.75847929885463,98.2985618527043));
#30381=CARTESIAN_POINT('Ctrl Pts',(15.4367365239838,-8.29721036780905,98.4746887503082));
#30382=CARTESIAN_POINT('Ctrl Pts',(15.6562640576654,-8.12841791648205,98.3612367156073));
#30383=CARTESIAN_POINT('Ctrl Pts',(15.5957265901482,-7.96036688919461,98.1211353597149));
#30384=CARTESIAN_POINT('Ctrl Pts',(15.5282302741409,-7.75804480438455,98.2928932196501));
#30385=CARTESIAN_POINT('Ctrl Pts',(15.5379755127592,-7.78974666478008,98.3104738976971));
#30386=CARTESIAN_POINT('Ctrl Pts',(15.5445254860806,-7.82226990841396,98.3279440205092));
#30387=CARTESIAN_POINT('Ctrl Pts',(15.5478189220675,-7.8551938468868,98.3450378052369));
#30388=CARTESIAN_POINT('Ctrl Pts',(15.5508151466442,-7.88514661172166,98.3605889858622));
#30389=CARTESIAN_POINT('Ctrl Pts',(15.5511156170379,-7.91543397054887,98.3758286877249));
#30390=CARTESIAN_POINT('Ctrl Pts',(15.548636924542,-7.94573125985883,98.3905567853577));
#30391=CARTESIAN_POINT('Ctrl Pts',(15.5463711106901,-7.97342651366893,98.4040199832666));
#30392=CARTESIAN_POINT('Ctrl Pts',(15.5417820463325,-8.00113151965715,98.4170556800349));
#30393=CARTESIAN_POINT('Ctrl Pts',(15.5347837088864,-8.02856293134369,98.429511011006));
#30394=CARTESIAN_POINT('Ctrl Pts',(15.5284502050597,-8.0533883919943,98.4407831005523));
#30395=CARTESIAN_POINT('Ctrl Pts',(15.5201425056581,-8.07799024485183,98.451579854735));
#30396=CARTESIAN_POINT('Ctrl Pts',(15.5097906601113,-8.10211622937918,98.4617879671231));
#30397=CARTESIAN_POINT('Ctrl Pts',(15.5046805057368,-8.11402594198207,98.4668271680985));
#30398=CARTESIAN_POINT('Ctrl Pts',(15.4990721976791,-8.12581896881945,98.471722924684));
#30399=CARTESIAN_POINT('Ctrl Pts',(15.4929578242382,-8.13746016004849,98.4764616066469));
#30400=CARTESIAN_POINT('Ctrl Pts',(17.3171452461371,-2.52318856294819,98.4764616066469));
#30401=CARTESIAN_POINT('Ctrl Pts',(17.3132089417597,-2.55020420325235,98.4666230035039));
#30402=CARTESIAN_POINT('Ctrl Pts',(17.307113237115,-2.57652769355605,98.4560730110188));
#30403=CARTESIAN_POINT('Ctrl Pts',(17.2990811363586,-2.6019158142319,98.4449543865012));
#30404=CARTESIAN_POINT('Ctrl Pts',(17.2902502712352,-2.62982869483757,98.4327300536087));
#30405=CARTESIAN_POINT('Ctrl Pts',(17.2790794105449,-2.65661115931836,98.4198183681966));
#30406=CARTESIAN_POINT('Ctrl Pts',(17.2658576960617,-2.68200516712457,98.4064090535635));
#30407=CARTESIAN_POINT('Ctrl Pts',(17.2516730980635,-2.70924851689978,98.392023193262));
#30408=CARTESIAN_POINT('Ctrl Pts',(17.2351284858505,-2.73489473602574,98.3770645838946));
#30409=CARTESIAN_POINT('Ctrl Pts',(17.2165633719675,-2.75868699851548,98.3617674910173));
#30410=CARTESIAN_POINT('Ctrl Pts',(17.194826807983,-2.78654365693436,98.3438572190847));
#30411=CARTESIAN_POINT('Ctrl Pts',(17.1703205947608,-2.81185976444954,98.3254829406478));
#30412=CARTESIAN_POINT('Ctrl Pts',(17.1435596961152,-2.83429057908266,98.307020656073));
#30413=CARTESIAN_POINT('Ctrl Pts',(17.1367405895733,-2.84000631071152,98.302316169606));
#30414=CARTESIAN_POINT('Ctrl Pts',(17.1297749579395,-2.84553494378639,98.297605968793));
#30415=CARTESIAN_POINT('Ctrl Pts',(17.1226711151597,-2.85087119795487,98.2928962747547));
#30416=CARTESIAN_POINT('Origin',(15.0503018864028,-7.90496129833282,100.));
#30417=CARTESIAN_POINT('Ctrl Pts',(15.5282302736771,-7.75804480287558,0.49999999999973));
#30418=CARTESIAN_POINT('Ctrl Pts',(15.5285224394342,-7.75899523603614,0.498951748855111));
#30419=CARTESIAN_POINT('Ctrl Pts',(15.5288117710303,-7.75994654384333,0.497903494267013));
#30420=CARTESIAN_POINT('Ctrl Pts',(15.5547339977176,-7.84609985197566,0.403057585737619));
#30421=CARTESIAN_POINT('Ctrl Pts',(15.5573771571738,-7.93722193600944,0.310543821720739));
#30422=CARTESIAN_POINT('Ctrl Pts',(15.526031478698,-8.06402685234064,0.195519413315996));
#30423=CARTESIAN_POINT('Ctrl Pts',(15.5116909609207,-8.10179403194099,0.16320254676869));
#30424=CARTESIAN_POINT('Ctrl Pts',(15.4929578242382,-8.13746016004849,0.134720657333159));
#30425=CARTESIAN_POINT('Origin',(16.822369667676,-2.45109746114967,100.));
#30426=CARTESIAN_POINT('Ctrl Pts',(17.3171452461371,-2.52318856294818,0.134720657333158));
#30427=CARTESIAN_POINT('Ctrl Pts',(17.3113366479632,-2.56305412818187,0.163202546768687));
#30428=CARTESIAN_POINT('Ctrl Pts',(17.3007393793634,-2.6020375631678,0.195519413315945));
#30429=CARTESIAN_POINT('Ctrl Pts',(17.2515645062122,-2.72304942298316,0.310543821722463));
#30430=CARTESIAN_POINT('Ctrl Pts',(17.1958659281393,-2.79521512738078,0.403057585740282));
#30431=CARTESIAN_POINT('Ctrl Pts',(17.1242547622625,-2.84967791522681,0.497903494266715));
#30432=CARTESIAN_POINT('Ctrl Pts',(17.1234615233847,-2.85027747456458,0.498951748855534));
#30433=CARTESIAN_POINT('Ctrl Pts',(17.122666505727,-2.85087466042014,0.5));
#30434=CARTESIAN_POINT('Origin',(19.8181570368417,-6.43930956430665,0.5));
#30435=CARTESIAN_POINT('Ctrl Pts',(7.93217192832153,-15.6280424815125,98.1029310403445));
#30436=CARTESIAN_POINT('Ctrl Pts',(7.88286802685372,-15.8011193837442,98.3435819249637));
#30437=CARTESIAN_POINT('Ctrl Pts',(7.6045369593389,-15.8096210136862,98.4565369103351));
#30438=CARTESIAN_POINT('Ctrl Pts',(7.99314885854194,-15.4140497422101,98.2878840681048));
#30439=CARTESIAN_POINT('Ctrl Pts',(7.93830133828976,-15.5743539404758,98.5214982034216));
#30440=CARTESIAN_POINT('Ctrl Pts',(7.67534747321689,-15.5703297983009,98.6414834345591));
#30441=CARTESIAN_POINT('Ctrl Pts',(8.07342544701253,-15.1939319565459,98.4673409001091));
#30442=CARTESIAN_POINT('Ctrl Pts',(8.01520601240404,-15.3378174966169,98.6966806273606));
#30443=CARTESIAN_POINT('Ctrl Pts',(7.76810813773369,-15.3239231079837,98.8209468546265));
#30444=CARTESIAN_POINT('Ctrl Pts',(8.27074145233723,-14.766641344314,98.7866059478792));
#30445=CARTESIAN_POINT('Ctrl Pts',(8.21126794551389,-14.8786168342413,99.007927768118));
#30446=CARTESIAN_POINT('Ctrl Pts',(7.99520082055391,-14.8449483706468,99.1402125820164));
#30447=CARTESIAN_POINT('Ctrl Pts',(8.38626933427988,-14.5585212736834,98.9284804941306));
#30448=CARTESIAN_POINT('Ctrl Pts',(8.32817971805786,-14.6543633819064,99.1468659074354));
#30449=CARTESIAN_POINT('Ctrl Pts',(8.12783062814372,-14.6113406338471,99.2820874488401));
#30450=CARTESIAN_POINT('Ctrl Pts',(8.59454374091697,-14.2490983667568,99.1108598027283));
#30451=CARTESIAN_POINT('Ctrl Pts',(8.54319049921963,-14.3207191002961,99.3254864613231));
#30452=CARTESIAN_POINT('Ctrl Pts',(8.3663329999392,-14.2633935124896,99.464467172046));
#30453=CARTESIAN_POINT('Ctrl Pts',(8.67033161120457,-14.1459038886756,99.1667281040793));
#30454=CARTESIAN_POINT('Ctrl Pts',(8.62164751952522,-14.2097749522395,99.3801095631261));
#30455=CARTESIAN_POINT('Ctrl Pts',(8.45303329796877,-14.1472419030066,99.5203355960163));
#30456=CARTESIAN_POINT('Ctrl Pts',(8.83156692003841,-13.9454197645673,99.2638527346786));
#30457=CARTESIAN_POINT('Ctrl Pts',(8.78941327154489,-13.9945706318056,99.4749661095218));
#30458=CARTESIAN_POINT('Ctrl Pts',(8.63728603612383,-13.9213425720194,99.617460437482));
#30459=CARTESIAN_POINT('Ctrl Pts',(8.91726990562806,-13.8476543326371,99.30543993253));
#30460=CARTESIAN_POINT('Ctrl Pts',(8.87903935077169,-13.8896197227996,99.5156582141639));
#30461=CARTESIAN_POINT('Ctrl Pts',(8.73513204645164,-13.8110608770739,99.6590477275195));
#30462=CARTESIAN_POINT('Ctrl Pts',(9.19086363206755,-13.562254936678,99.4071746058911));
#30463=CARTESIAN_POINT('Ctrl Pts',(9.16559403544582,-13.5845353846886,99.6148745113244));
#30464=CARTESIAN_POINT('Ctrl Pts',(9.04717263343429,-13.4887249880271,99.7607826165557));
#30465=CARTESIAN_POINT('Ctrl Pts',(9.39863643901659,-13.3806266657362,99.4435386777497));
#30466=CARTESIAN_POINT('Ctrl Pts',(9.38579471648297,-13.3899048404733,99.6506668510312));
#30467=CARTESIAN_POINT('Ctrl Pts',(9.28372334348073,-13.2830140381241,99.7971467765045));
#30468=CARTESIAN_POINT('Ctrl Pts',(9.72568529812741,-13.1438881211714,99.4425027003972));
#30469=CARTESIAN_POINT('Ctrl Pts',(9.73270657526636,-13.1388413288337,99.6496543232893));
#30470=CARTESIAN_POINT('Ctrl Pts',(9.6553092634351,-13.0140082384199,99.7961107967625));
#30471=CARTESIAN_POINT('Ctrl Pts',(9.83783804700212,-13.0701625206813,99.4333242900206));
#30472=CARTESIAN_POINT('Ctrl Pts',(9.85200497202214,-13.0608830247368,99.6406660872408));
#30473=CARTESIAN_POINT('Ctrl Pts',(9.78261877917292,-12.9300742643074,99.786932365797));
#30474=CARTESIAN_POINT('Ctrl Pts',(10.0683558886232,-12.9329789952414,99.3975703058089));
#30475=CARTESIAN_POINT('Ctrl Pts',(10.0972665052523,-12.9166588193609,99.605723827768));
#30476=CARTESIAN_POINT('Ctrl Pts',(10.0440416516022,-12.7735790742389,99.7511783033389));
#30477=CARTESIAN_POINT('Ctrl Pts',(10.1878697697833,-12.869006620432,99.3706193994189));
#30478=CARTESIAN_POINT('Ctrl Pts',(10.2246928633403,-12.8497510163372,99.5793392014518));
#30479=CARTESIAN_POINT('Ctrl Pts',(10.1794547531642,-12.7004270560129,99.7242273368565));
#30480=CARTESIAN_POINT('Ctrl Pts',(10.5459796461522,-12.697229401858,99.2668124456042));
#30481=CARTESIAN_POINT('Ctrl Pts',(10.6071137146224,-12.6711601820482,99.4777222783443));
#30482=CARTESIAN_POINT('Ctrl Pts',(10.5848323230218,-12.5034972525401,99.6204201490476));
#30483=CARTESIAN_POINT('Ctrl Pts',(10.7835265265762,-12.6088970959964,99.1683014346688));
#30484=CARTESIAN_POINT('Ctrl Pts',(10.8613053154178,-12.5813807547492,99.3809681438969));
#30485=CARTESIAN_POINT('Ctrl Pts',(10.8532501470603,-12.4015113889649,99.5219089068378));
#30486=CARTESIAN_POINT('Ctrl Pts',(11.2574858404352,-12.4740942697067,98.9266153300885));
#30487=CARTESIAN_POINT('Ctrl Pts',(11.3667598443235,-12.4485214406132,99.1450562468822));
#30488=CARTESIAN_POINT('Ctrl Pts',(11.3879615918918,-12.2445226500553,99.2802222813136));
#30489=CARTESIAN_POINT('Ctrl Pts',(11.4955326995555,-12.4278895523164,98.7818489409676));
#30490=CARTESIAN_POINT('Ctrl Pts',(11.6208671315241,-12.406072497649,99.0032991843688));
#30491=CARTESIAN_POINT('Ctrl Pts',(11.6560867497417,-12.1897979679578,99.1354555654035));
#30492=CARTESIAN_POINT('Ctrl Pts',(11.9602280353417,-12.3732319398884,98.4637529209039));
#30493=CARTESIAN_POINT('Ctrl Pts',(12.1153359231333,-12.3624828687134,98.6931970175235));
#30494=CARTESIAN_POINT('Ctrl Pts',(12.1787937287267,-12.1229428480096,98.8173588681825));
#30495=CARTESIAN_POINT('Ctrl Pts',(12.1889332851312,-12.3651447396863,98.2884223589262));
#30496=CARTESIAN_POINT('Ctrl Pts',(12.3582902157402,-12.362492662348,98.522029004501));
#30497=CARTESIAN_POINT('Ctrl Pts',(12.4356699559058,-12.1111989679491,98.6420342841671));
#30498=CARTESIAN_POINT('Ctrl Pts',(12.412036561458,-12.3732750986756,98.1028819384397));
#30499=CARTESIAN_POINT('Ctrl Pts',(12.5918835391696,-12.3798704796622,98.3435328811783));
#30500=CARTESIAN_POINT('Ctrl Pts',(12.6859819512106,-12.1177859883829,98.456486539046));
#30501=CARTESIAN_POINT('Ctrl Pts',(8.00253786208648,-15.4036548381007,98.292893219028));
#30502=CARTESIAN_POINT('Ctrl Pts',(7.99178803981921,-15.4350302894399,98.3104738970446));
#30503=CARTESIAN_POINT('Ctrl Pts',(7.97797039667762,-15.4651921239651,98.3279440198334));
#30504=CARTESIAN_POINT('Ctrl Pts',(7.9612826369793,-15.4937639828144,98.3450378045448));
#30505=CARTESIAN_POINT('Ctrl Pts',(7.94610084020688,-15.5197574152645,98.3605889851856));
#30506=CARTESIAN_POINT('Ctrl Pts',(7.92854146306982,-15.54443701539,98.3758286870684));
#30507=CARTESIAN_POINT('Ctrl Pts',(7.90872785893013,-15.5674910984875,98.3905567847244));
#30508=CARTESIAN_POINT('Ctrl Pts',(7.89061591531714,-15.5885652175708,98.404019982656));
#30509=CARTESIAN_POINT('Ctrl Pts',(7.87061869037307,-15.6082816539495,98.4170556794497));
#30510=CARTESIAN_POINT('Ctrl Pts',(7.84883313724825,-15.626360612701,98.4295110104475));
#30511=CARTESIAN_POINT('Ctrl Pts',(7.82911718541249,-15.6427220921615,98.4407831000128));
#30512=CARTESIAN_POINT('Ctrl Pts',(7.80793550916779,-15.6577422660767,98.4515798542159));
#30513=CARTESIAN_POINT('Ctrl Pts',(7.78537979233681,-15.6711759354721,98.4617879666255));
#30514=CARTESIAN_POINT('Ctrl Pts',(7.77424523683315,-15.677807422231,98.4668271677764));
#30515=CARTESIAN_POINT('Ctrl Pts',(7.76277625268364,-15.6840517008099,98.4717229245282));
#30516=CARTESIAN_POINT('Ctrl Pts',(7.75098709974897,-15.6898756840048,98.4764616066469));
#30517=CARTESIAN_POINT('Origin',(12.1669944796941,-11.8680158320171,98.2808650733939));
#30518=CARTESIAN_POINT('Origin',(7.52953032547043,-15.2415935216047,100.));
#30519=CARTESIAN_POINT('Ctrl Pts',(8.00253786221767,-15.4036548377177,0.5));
#30520=CARTESIAN_POINT('Ctrl Pts',(8.00221557868522,-15.4045954850201,0.498951748855171));
#30521=CARTESIAN_POINT('Ctrl Pts',(8.00189048816382,-15.4055351740487,0.4979034942676));
#30522=CARTESIAN_POINT('Ctrl Pts',(7.97222236610058,-15.4904713670851,0.403057585608257));
#30523=CARTESIAN_POINT('Ctrl Pts',(7.92080050982121,-15.5657442917577,0.310543821635946));
#30524=CARTESIAN_POINT('Ctrl Pts',(7.82090726357263,-15.6499070964456,0.19551941331783));
#30525=CARTESIAN_POINT('Ctrl Pts',(7.78710654979209,-15.6720322417129,0.163202546769525));
#30526=CARTESIAN_POINT('Ctrl Pts',(7.75098709974897,-15.6898756840048,0.134720657333167));
#30527=CARTESIAN_POINT('Origin',(12.1688640072122,-11.8709203002116,100.));
#30528=CARTESIAN_POINT('Ctrl Pts',(12.5267717721302,-12.2200650149237,0.134720657333168));
#30529=CARTESIAN_POINT('Ctrl Pts',(12.4986401261746,-12.2489027263458,0.163202546769506));
#30530=CARTESIAN_POINT('Ctrl Pts',(12.467152867614,-12.2742120695516,0.195519413317813));
#30531=CARTESIAN_POINT('Ctrl Pts',(12.3562405730693,-12.3432084553889,0.310543821638501));
#30532=CARTESIAN_POINT('Ctrl Pts',(12.2687615400859,-12.3688529339418,0.403057585612081));
#30533=CARTESIAN_POINT('Ctrl Pts',(12.1788144663232,-12.3708222676705,0.497903494267714));
#30534=CARTESIAN_POINT('Ctrl Pts',(12.1778203104535,-12.37084106725,0.498951748855235));
#30535=CARTESIAN_POINT('Ctrl Pts',(12.1768261106186,-12.3708569011015,0.5));
#30536=CARTESIAN_POINT('Origin',(12.2482946431511,-16.8583313034371,0.5));
#30537=CARTESIAN_POINT('Ctrl Pts',(3.12098026161582,-17.2452472912803,98.4746163542476));
#30538=CARTESIAN_POINT('Ctrl Pts',(2.89260432929213,-17.4018708609359,98.3611663178014));
#30539=CARTESIAN_POINT('Ctrl Pts',(2.75148341999934,-17.2923597286537,98.1210629636544));
#30540=CARTESIAN_POINT('Ctrl Pts',(2.73662446842811,-16.9531805857874,98.8304618827569));
#30541=CARTESIAN_POINT('Ctrl Pts',(2.54985248945744,-17.1146469822609,98.7002300650182));
#30542=CARTESIAN_POINT('Ctrl Pts',(2.41148044251108,-17.0285142699567,98.4769098403624));
#30543=CARTESIAN_POINT('Ctrl Pts',(2.2771369734248,-16.6926757665459,99.1602382875981));
#30544=CARTESIAN_POINT('Ctrl Pts',(2.1262371091352,-16.8482972498973,99.0255494138259));
#30545=CARTESIAN_POINT('Ctrl Pts',(2.00572321702946,-16.7928860538427,98.8066848982746));
#30546=CARTESIAN_POINT('Ctrl Pts',(1.48828850627735,-16.4115930339871,99.5229830380903));
#30547=CARTESIAN_POINT('Ctrl Pts',(1.3892948723609,-16.5617976914238,99.3820315078356));
#30548=CARTESIAN_POINT('Ctrl Pts',(1.31033409767429,-16.5384526486055,99.1694296468622));
#30549=CARTESIAN_POINT('Ctrl Pts',(1.20426376711607,-16.3348109530474,99.6234913693268));
#30550=CARTESIAN_POINT('Ctrl Pts',(1.12441622988636,-16.4834764139428,99.4807426095521));
#30551=CARTESIAN_POINT('Ctrl Pts',(1.06013194543906,-16.468911658045,99.2699379792856));
#30552=CARTESIAN_POINT('Ctrl Pts',(0.610116136352582,-16.2303876665528,
99.7608048122958));
#30553=CARTESIAN_POINT('Ctrl Pts',(0.570592580096315,-16.3774763782636,
99.6149071958598));
#30554=CARTESIAN_POINT('Ctrl Pts',(0.536982386432902,-16.3743182939754,
99.4072514211504));
#30555=CARTESIAN_POINT('Ctrl Pts',(0.304395385329841,-16.2034354627799,
99.7966027452517));
#30556=CARTESIAN_POINT('Ctrl Pts',(0.284158019240025,-16.3498801785155,
99.6501526042829));
#30557=CARTESIAN_POINT('Ctrl Pts',(0.267906895914237,-16.3498931438339,
99.4430493547679));
#30558=CARTESIAN_POINT('Ctrl Pts',(-0.155238398773932,-16.2036129415512,
99.79636776423));
#30559=CARTESIAN_POINT('Ctrl Pts',(-0.144919417032331,-16.350060507997,
99.6499229371967));
#30560=CARTESIAN_POINT('Ctrl Pts',(-0.136629658481305,-16.3500539600226,
99.442814373582));
#30561=CARTESIAN_POINT('Ctrl Pts',(-0.310467040971084,-16.2104925143924,
99.7872514480855));
#30562=CARTESIAN_POINT('Ctrl Pts',(-0.289967609306084,-16.3570649252483,
99.6409952531274));
#30563=CARTESIAN_POINT('Ctrl Pts',(-0.273250886059789,-16.3562879072327,
99.4336980572382));
#30564=CARTESIAN_POINT('Ctrl Pts',(-0.616270430045099,-16.2376016048274,
99.7514230350795));
#30565=CARTESIAN_POINT('Ctrl Pts',(-0.575332789987141,-16.3846026904707,
99.6059800049562));
#30566=CARTESIAN_POINT('Ctrl Pts',(-0.542427079965611,-16.3808502013102,
99.3978696447402));
#30567=CARTESIAN_POINT('Ctrl Pts',(-0.765900280742026,-16.2576126110768,
99.7250021223378));
#30568=CARTESIAN_POINT('Ctrl Pts',(-0.715021742305809,-16.4049628381993,
99.580115086457));
#30569=CARTESIAN_POINT('Ctrl Pts',(-0.674150359005859,-16.3989804855663,
99.3714487314956));
#30570=CARTESIAN_POINT('Ctrl Pts',(-1.20584020603565,-16.3354058480377,
99.6227146850676));
#30571=CARTESIAN_POINT('Ctrl Pts',(-1.12586029852611,-16.484076987348,99.4799874409064));
#30572=CARTESIAN_POINT('Ctrl Pts',(-1.06152132333177,-16.4694503946166,
99.2691612949723));
#30573=CARTESIAN_POINT('Ctrl Pts',(-1.49045845351357,-16.4122197672618,
99.5221656588586));
#30574=CARTESIAN_POINT('Ctrl Pts',(-1.39131820921651,-16.5624362368043,
99.3812294188917));
#30575=CARTESIAN_POINT('Ctrl Pts',(-1.31224595582822,-16.5390201922301,
99.1686122675856));
#30576=CARTESIAN_POINT('Ctrl Pts',(-2.01683567706171,-16.6000729369335,
99.2797533468154));
#30577=CARTESIAN_POINT('Ctrl Pts',(-1.87973999608329,-16.7526185023833,
99.1446071116388));
#30578=CARTESIAN_POINT('Ctrl Pts',(-1.77626230257574,-16.7090626239978,
98.9261999569019));
#30579=CARTESIAN_POINT('Ctrl Pts',(-2.26049125374327,-16.7108289072482,
99.1382521541653));
#30580=CARTESIAN_POINT('Ctrl Pts',(-2.10526006254958,-16.8650411275935,
99.0060308920462));
#30581=CARTESIAN_POINT('Ctrl Pts',(-1.99121820958417,-16.8092788783051,
98.7846987631132));
#30582=CARTESIAN_POINT('Ctrl Pts',(-2.71703050574155,-16.960436329805,98.8245648611909));
#30583=CARTESIAN_POINT('Ctrl Pts',(-2.52562525529546,-17.11676918777,98.7003130263028));
#30584=CARTESIAN_POINT('Ctrl Pts',(-2.39431788322546,-17.0350004816458,
98.4710114710564));
#30585=CARTESIAN_POINT('Ctrl Pts',(-2.92925959162701,-17.0995673036637,
98.6521093612485));
#30586=CARTESIAN_POINT('Ctrl Pts',(-2.71988721110581,-17.2571410628046,
98.5320184901546));
#30587=CARTESIAN_POINT('Ctrl Pts',(-2.58188146292343,-17.1607523397378,
98.2985618527006));
#30588=CARTESIAN_POINT('Ctrl Pts',(-3.12090206377705,-17.2451878710232,
98.4746887503082));
#30589=CARTESIAN_POINT('Ctrl Pts',(-2.89253316440024,-17.4018112264551,
98.3612367156073));
#30590=CARTESIAN_POINT('Ctrl Pts',(-2.75141424608767,-17.2923060501388,
98.1211353597149));
#30591=CARTESIAN_POINT('Ctrl Pts',(-2.57985201764259,-17.1655922764305,
98.2928932196501));
#30592=CARTESIAN_POINT('Ctrl Pts',(-2.60699083422014,-17.1846569627487,
98.3104738977108));
#30593=CARTESIAN_POINT('Ctrl Pts',(-2.63589822395985,-17.2009365925614,
98.3279440205353));
#30594=CARTESIAN_POINT('Ctrl Pts',(-2.66619302251831,-17.2142428928325,
98.3450378052742));
#30595=CARTESIAN_POINT('Ctrl Pts',(-2.69375391038932,-17.2263483851018,
98.3605889859024));
#30596=CARTESIAN_POINT('Ctrl Pts',(-2.72246604991279,-17.235993458018,98.3758286877673));
#30597=CARTESIAN_POINT('Ctrl Pts',(-2.75204644244987,-17.2429984586447,
98.3905567854016));
#30598=CARTESIAN_POINT('Ctrl Pts',(-2.77908636904687,-17.2494018457033,
98.4040199833104));
#30599=CARTESIAN_POINT('Ctrl Pts',(-2.80685349440489,-17.2535987038177,
98.4170556800783));
#30600=CARTESIAN_POINT('Ctrl Pts',(-2.83510492244771,-17.2554196617721,
98.4295110110486));
#30601=CARTESIAN_POINT('Ctrl Pts',(-2.86067249888962,-17.2570676309165,
98.4407831005944));
#30602=CARTESIAN_POINT('Ctrl Pts',(-2.88663747166555,-17.2567689298861,
98.4515798547762));
#30603=CARTESIAN_POINT('Ctrl Pts',(-2.91278154266259,-17.2543790789424,
98.4617879671636));
#30604=CARTESIAN_POINT('Ctrl Pts',(-2.9256874769523,-17.253199336918,98.4668271681246));
#30605=CARTESIAN_POINT('Ctrl Pts',(-2.93863637443791,-17.2515097647054,
98.4717229246966));
#30606=CARTESIAN_POINT('Ctrl Pts',(-2.95159725048241,-17.2492919759318,
98.4764616066469));
#30607=CARTESIAN_POINT('Ctrl Pts',(2.95159725048241,-17.2492919759318,98.4764616066469));
#30608=CARTESIAN_POINT('Ctrl Pts',(2.92468746478112,-17.2538966199715,98.4666230035037));
#30609=CARTESIAN_POINT('Ctrl Pts',(2.89776866146762,-17.256233666203,98.4560730110187));
#30610=CARTESIAN_POINT('Ctrl Pts',(2.87114106822738,-17.2564400451831,98.4449543865015));
#30611=CARTESIAN_POINT('Ctrl Pts',(2.84186545384406,-17.2566669478319,98.432730053611));
#30612=CARTESIAN_POINT('Ctrl Pts',(2.81294183068533,-17.254319064656,98.4198183682014));
#30613=CARTESIAN_POINT('Ctrl Pts',(2.78470495961941,-17.2495916469085,98.4064090535707));
#30614=CARTESIAN_POINT('Ctrl Pts',(2.75441171245854,-17.2445199506175,98.3920231932742));
#30615=CARTESIAN_POINT('Ctrl Pts',(2.72490814230923,-17.2367102069175,98.377064583912));
#30616=CARTESIAN_POINT('Ctrl Pts',(2.69654342034601,-17.2264059478322,98.3617674910395));
#30617=CARTESIAN_POINT('Ctrl Pts',(2.66333319619532,-17.2143414278847,98.3438572191246));
#30618=CARTESIAN_POINT('Ctrl Pts',(2.63168331085079,-17.1988577415842,98.3254829407057));
#30619=CARTESIAN_POINT('Ctrl Pts',(2.60208076598617,-17.1803381174911,98.3070206561472));
#30620=CARTESIAN_POINT('Ctrl Pts',(2.59453756232716,-17.1756190199655,98.3023161696555));
#30621=CARTESIAN_POINT('Ctrl Pts',(2.58712702122499,-17.1707027521616,98.2976059688177));
#30622=CARTESIAN_POINT('Ctrl Pts',(2.57985673374387,-17.1655955893933,98.2928962747544));
#30623=CARTESIAN_POINT('Origin',(-2.86726590046863,-16.7564550623337,100.));
#30624=CARTESIAN_POINT('Ctrl Pts',(-2.57985201635105,-17.1655922755232,
0.5));
#30625=CARTESIAN_POINT('Ctrl Pts',(-2.58066564781719,-17.1661638416687,
0.49895174885588));
#30626=CARTESIAN_POINT('Ctrl Pts',(-2.58148098692633,-17.166732982648,0.497903494266524));
#30627=CARTESIAN_POINT('Ctrl Pts',(-2.65540724343409,-17.2180093215811,
0.403057585761194));
#30628=CARTESIAN_POINT('Ctrl Pts',(-2.74125271403769,-17.2486813881429,
0.310543821736212));
#30629=CARTESIAN_POINT('Ctrl Pts',(-2.87153770337987,-17.2580547504885,
0.195519413315782));
#30630=CARTESIAN_POINT('Ctrl Pts',(-2.911887889342,-17.2560868079355,0.163202546768621));
#30631=CARTESIAN_POINT('Ctrl Pts',(-2.95159725048241,-17.2492919759318,
0.134720657333156));
#30632=CARTESIAN_POINT('Origin',(2.86726590046862,-16.7564550623337,100.));
#30633=CARTESIAN_POINT('Ctrl Pts',(2.95159725048241,-17.2492919759318,0.134720657333157));
#30634=CARTESIAN_POINT('Ctrl Pts',(2.91188788934223,-17.2560868079355,0.163202546768453));
#30635=CARTESIAN_POINT('Ctrl Pts',(2.8715377033803,-17.2580547504885,0.195519413315438));
#30636=CARTESIAN_POINT('Ctrl Pts',(2.74125271402536,-17.2486813881421,0.310543821747035));
#30637=CARTESIAN_POINT('Ctrl Pts',(2.65540724342468,-17.2180093215746,0.403057585777651));
#30638=CARTESIAN_POINT('Ctrl Pts',(2.58148098692613,-17.1667329826479,0.49790349426656));
#30639=CARTESIAN_POINT('Ctrl Pts',(2.58066564781731,-17.1661638416688,0.498951748855718));
#30640=CARTESIAN_POINT('Ctrl Pts',(2.57985201635104,-17.1655922755232,0.5));
#30641=CARTESIAN_POINT('Origin',(-2.55192432461455E-15,-20.8380434782609,
0.5));
#30642=CARTESIAN_POINT('Ctrl Pts',(-7.61153061250582,-15.7863147967496,
98.4745004885114));
#30643=CARTESIAN_POINT('Ctrl Pts',(-7.88836095469125,-15.7787835827682,
98.3610536502059));
#30644=CARTESIAN_POINT('Ctrl Pts',(-7.9381581147024,-15.6072288420487,98.1209470979181));
#30645=CARTESIAN_POINT('Ctrl Pts',(-7.68185024282998,-15.5529265513644,
98.6541872523937));
#30646=CARTESIAN_POINT('Ctrl Pts',(-7.94367437493447,-15.5575146677549,
98.5339912542897));
#30647=CARTESIAN_POINT('Ctrl Pts',(-7.99873405832647,-15.3985404288953,
98.3006281519147));
#30648=CARTESIAN_POINT('Ctrl Pts',(-7.77058558274001,-15.3193429185923,
98.8238114502904));
#30649=CARTESIAN_POINT('Ctrl Pts',(-8.01739572281288,-15.3332616605647,
98.6995854322395));
#30650=CARTESIAN_POINT('Ctrl Pts',(-8.07554514465372,-15.1898709314151,
98.4702580602194));
#30651=CARTESIAN_POINT('Ctrl Pts',(-7.9924298071297,-14.8502894771664,99.1368088098189));
#30652=CARTESIAN_POINT('Ctrl Pts',(-8.20881182371942,-14.883703165293,99.0046294469941));
#30653=CARTESIAN_POINT('Ctrl Pts',(-8.26829617652396,-14.7714171710724,
98.7832554187034));
#30654=CARTESIAN_POINT('Ctrl Pts',(-8.12737169382821,-14.6123994681448,
99.2813501417123));
#30655=CARTESIAN_POINT('Ctrl Pts',(-8.32776251015203,-14.6553398972789,
99.1461712456963));
#30656=CARTESIAN_POINT('Ctrl Pts',(-8.38583875689921,-14.5594769234819,
98.9277967516668));
#30657=CARTESIAN_POINT('Ctrl Pts',(-8.44228186665902,-14.1522925726334,
99.5228530262281));
#30658=CARTESIAN_POINT('Ctrl Pts',(-8.61067658867427,-14.2156092191235,
99.3819067332058));
#30659=CARTESIAN_POINT('Ctrl Pts',(-8.66083652547866,-14.1502985880832,
99.1692996350871));
#30660=CARTESIAN_POINT('Ctrl Pts',(-8.62238122769751,-13.9285751457649,
99.6211970158378));
#30661=CARTESIAN_POINT('Ctrl Pts',(-8.77477430608758,-14.0016497079299,
99.4784987699913));
#30662=CARTESIAN_POINT('Ctrl Pts',(-8.81839581871021,-13.9517156783976,
99.2676436259617));
#30663=CARTESIAN_POINT('Ctrl Pts',(-8.93504150578028,-13.6041086188705,
99.724700650501));
#30664=CARTESIAN_POINT('Ctrl Pts',(-9.06290937455646,-13.6933479875448,
99.5798189693958));
#30665=CARTESIAN_POINT('Ctrl Pts',(-9.09252380741154,-13.6644048462732,
99.3711472595492));
#30666=CARTESIAN_POINT('Ctrl Pts',(-9.04643201266491,-13.4980463524896,
99.7515464581424));
#30667=CARTESIAN_POINT('Ctrl Pts',(-9.1659008380529,-13.5929484631966,99.6061008493641));
#30668=CARTESIAN_POINT('Ctrl Pts',(-9.19027681092597,-13.5706128359882,
99.3979930676329));
#30669=CARTESIAN_POINT('Ctrl Pts',(-9.27641719553042,-13.297662320044,99.7871410858038));
#30670=CARTESIAN_POINT('Ctrl Pts',(-9.37920676320481,-13.404156206133,99.6408876188391));
#30671=CARTESIAN_POINT('Ctrl Pts',(-9.39230696146118,-13.3936667965263,
99.4335876951267));
#30672=CARTESIAN_POINT('Ctrl Pts',(-9.39592243526722,-13.2023470673547,
99.7962421951755));
#30673=CARTESIAN_POINT('Ctrl Pts',(-9.49053581390396,-13.3146274568229,
99.6498002056397));
#30674=CARTESIAN_POINT('Ctrl Pts',(-9.49738200583989,-13.3096324234838,
99.4426888046372));
#30675=CARTESIAN_POINT('Ctrl Pts',(-9.64409776558335,-13.0216618073135,
99.7966442229661));
#30676=CARTESIAN_POINT('Ctrl Pts',(-9.72219875439405,-13.1459331194972,
99.6501931431456));
#30677=CARTESIAN_POINT('Ctrl Pts',(-9.71580342119468,-13.1505998825526,
99.4430908323178));
#30678=CARTESIAN_POINT('Ctrl Pts',(-9.77381197449095,-12.9356824620425,
99.7877849805069));
#30679=CARTESIAN_POINT('Ctrl Pts',(-9.84373626500581,-13.0660445920766,
99.6415170968033));
#30680=CARTESIAN_POINT('Ctrl Pts',(-9.83007072703063,-13.0750678730396,
99.4342315896588));
#30681=CARTESIAN_POINT('Ctrl Pts',(-10.0376062905057,-12.7771593103382,
99.7523547967177));
#30682=CARTESIAN_POINT('Ctrl Pts',(-10.0912047848049,-12.9199070101996,
99.6068909575268));
#30683=CARTESIAN_POINT('Ctrl Pts',(-10.0626757487172,-12.9360922565949,
99.3988014063792));
#30684=CARTESIAN_POINT('Ctrl Pts',(-10.1706575690792,-12.7050827268415,
99.7260859669308));
#30685=CARTESIAN_POINT('Ctrl Pts',(-10.2163999615544,-12.8539677361418,
99.581174605591));
#30686=CARTESIAN_POINT('Ctrl Pts',(-10.1801044201994,-12.8730550738084,
99.3725325760877));
#30687=CARTESIAN_POINT('Ctrl Pts',(-10.5730247519993,-12.5085765171443,
99.6241384720944));
#30688=CARTESIAN_POINT('Ctrl Pts',(-10.5959433339685,-12.6756716426713,
99.4813799591445));
#30689=CARTESIAN_POINT('Ctrl Pts',(-10.5355461919898,-12.7016211074057,
99.2705850820007));
#30690=CARTESIAN_POINT('Ctrl Pts',(-10.8489658974378,-12.4029669023366,
99.5236562902266));
#30691=CARTESIAN_POINT('Ctrl Pts',(-10.8572640774209,-12.5825975767434,
99.3826839740364));
#30692=CARTESIAN_POINT('Ctrl Pts',(-10.7797437745015,-12.6101276716056,
99.1701028989501));
#30693=CARTESIAN_POINT('Ctrl Pts',(-11.3863904046298,-12.2448379356151,
99.2810827044785));
#30694=CARTESIAN_POINT('Ctrl Pts',(-11.3652836467698,-12.4487162064104,
99.1459030339944));
#30695=CARTESIAN_POINT('Ctrl Pts',(-11.2561108367434,-12.474332324694,98.9275293145685));
#30696=CARTESIAN_POINT('Ctrl Pts',(-11.6491602608148,-12.1909944678519,
99.1393951997109));
#30697=CARTESIAN_POINT('Ctrl Pts',(-11.6143348897636,-12.4069069268349,
99.0071411174915));
#30698=CARTESIAN_POINT('Ctrl Pts',(-11.489403766598,-12.4288617015343,98.7858418086588));
#30699=CARTESIAN_POINT('Ctrl Pts',(-12.1662817650126,-12.1242950353399,
98.8252029000679));
#30700=CARTESIAN_POINT('Ctrl Pts',(-12.1033811314411,-12.3632333592681,
98.7009299069291));
#30701=CARTESIAN_POINT('Ctrl Pts',(-11.9491322142495,-12.3742909202748,
98.4716495099335));
#30702=CARTESIAN_POINT('Ctrl Pts',(-12.4202878510302,-12.1120529425579,
98.6524117207795));
#30703=CARTESIAN_POINT('Ctrl Pts',(-12.3435537205759,-12.362581638257,98.5323055644746));
#30704=CARTESIAN_POINT('Ctrl Pts',(-12.1752607824295,-12.365734055554,98.2988642625954));
#30705=CARTESIAN_POINT('Ctrl Pts',(-12.6613982812294,-12.1172313198433,
98.4746383405503));
#30706=CARTESIAN_POINT('Ctrl Pts',(-12.5687009849841,-12.378177146358,98.3611876972422));
#30707=CARTESIAN_POINT('Ctrl Pts',(-12.3901642949233,-12.3725306764959,
98.121084949957));
#30708=CARTESIAN_POINT('Ctrl Pts',(-12.1768261122223,-12.3708569010759,
98.2928932196637));
#30709=CARTESIAN_POINT('Ctrl Pts',(-12.2099878174022,-12.3703287601507,
98.310473897661));
#30710=CARTESIAN_POINT('Ctrl Pts',(-12.2429433131837,-12.366507919979,98.3279440204279));
#30711=CARTESIAN_POINT('Ctrl Pts',(-12.2752735670263,-12.3594661072555,
98.3450378051151));
#30712=CARTESIAN_POINT('Ctrl Pts',(-12.304686223498,-12.3530597728176,98.3605889857293));
#30713=CARTESIAN_POINT('Ctrl Pts',(-12.3335840639116,-12.3439862285719,
98.3758286875838));
#30714=CARTESIAN_POINT('Ctrl Pts',(-12.3616325402144,-12.3322664746665,
98.3905567852105));
#30715=CARTESIAN_POINT('Ctrl Pts',(-12.3872721168296,-12.3215532535657,
98.4040199831191));
#30716=CARTESIAN_POINT('Ctrl Pts',(-12.4122030444301,-12.3086274763456,
98.4170556798887));
#30717=CARTESIAN_POINT('Ctrl Pts',(-12.4361292620607,-12.2934948895455,
98.4295110108618));
#30718=CARTESIAN_POINT('Ctrl Pts',(-12.4577825178641,-12.2797998802462,
98.4407831004098));
#30719=CARTESIAN_POINT('Ctrl Pts',(-12.4786130500376,-12.2642963979904,
98.4515798545948));
#30720=CARTESIAN_POINT('Ctrl Pts',(-12.4983593286395,-12.2469958686251,
98.4617879669855));
#30721=CARTESIAN_POINT('Ctrl Pts',(-12.5081070139649,-12.2384555193463,
98.4668271680095));
#30722=CARTESIAN_POINT('Ctrl Pts',(-12.5175897865744,-12.2294774556375,
98.471722924641));
#30723=CARTESIAN_POINT('Ctrl Pts',(-12.5267717721302,-12.2200650149237,
98.4764616066469));
#30724=CARTESIAN_POINT('Origin',(-7.5273854258457,-15.2389652386414,98.2808710159383));
#30725=CARTESIAN_POINT('Origin',(-12.1688640072122,-11.8709203002116,100.));
#30726=CARTESIAN_POINT('Ctrl Pts',(-12.1768261106186,-12.3708569011015,
0.5));
#30727=CARTESIAN_POINT('Ctrl Pts',(-12.1778203104535,-12.37084106725,0.498951748855216));
#30728=CARTESIAN_POINT('Ctrl Pts',(-12.1788144663228,-12.3708222676705,
0.497903494267674));
#30729=CARTESIAN_POINT('Ctrl Pts',(-12.2687615400609,-12.3688529339424,
0.403057585648595));
#30730=CARTESIAN_POINT('Ctrl Pts',(-12.3562405730462,-12.3432084554035,
0.31054382166245));
#30731=CARTESIAN_POINT('Ctrl Pts',(-12.4671528676144,-12.2742120695513,
0.19551941331738));
#30732=CARTESIAN_POINT('Ctrl Pts',(-12.4986401261748,-12.2489027263456,
0.163202546769333));
#30733=CARTESIAN_POINT('Ctrl Pts',(-12.5267717721302,-12.2200650149237,
0.134720657333167));
#30734=CARTESIAN_POINT('Origin',(-7.52953032547043,-15.2415935216047,100.));
#30735=CARTESIAN_POINT('Ctrl Pts',(-7.75098709974897,-15.6898756840048,
0.134720657333167));
#30736=CARTESIAN_POINT('Ctrl Pts',(-7.7871065497921,-15.6720322417129,0.163202546769531));
#30737=CARTESIAN_POINT('Ctrl Pts',(-7.82090726357263,-15.6499070964456,
0.195519413317832));
#30738=CARTESIAN_POINT('Ctrl Pts',(-7.92080050981464,-15.5657442917632,
0.310543821628375));
#30739=CARTESIAN_POINT('Ctrl Pts',(-7.97222236609799,-15.4904713670923,
0.403057585596688));
#30740=CARTESIAN_POINT('Ctrl Pts',(-8.00189048816371,-15.405535174049,0.497903494267389));
#30741=CARTESIAN_POINT('Ctrl Pts',(-8.00221557868521,-15.4045954850201,
0.498951748855124));
#30742=CARTESIAN_POINT('Ctrl Pts',(-8.00253786221767,-15.4036548377177,
0.5));
#30743=CARTESIAN_POINT('Origin',(-12.2482946431511,-16.8583313034371,0.5));
#30744=CARTESIAN_POINT('Ctrl Pts',(-17.3143275672679,-2.71461308511347,
98.1029310402112));
#30745=CARTESIAN_POINT('Ctrl Pts',(-17.4636977395246,-2.61423858422028,
98.3435819248339));
#30746=CARTESIAN_POINT('Ctrl Pts',(-17.3857742401592,-2.34690286062856,
98.456536910202));
#30747=CARTESIAN_POINT('Ctrl Pts',(-17.1296512857755,-2.83873298507897,
98.2878840680197));
#30748=CARTESIAN_POINT('Ctrl Pts',(-17.2651608222781,-2.73703317200584,
98.5214982033383));
#30749=CARTESIAN_POINT('Ctrl Pts',(-17.1800764225947,-2.48819271345443,
98.6414834344728));
#30750=CARTESIAN_POINT('Ctrl Pts',(-16.9451136614061,-2.98310069421631,
98.4673409000723));
#30751=CARTESIAN_POINT('Ctrl Pts',(-17.0639661471992,-2.88326764442847,
98.6966806273241));
#30752=CARTESIAN_POINT('Ctrl Pts',(-16.9743943558017,-2.65255720277051,
98.8209468545885));
#30753=CARTESIAN_POINT('Ctrl Pts',(-16.599710139157,-3.30279942760483,98.7866059478771));
#30754=CARTESIAN_POINT('Ctrl Pts',(-16.6878268341941,-3.21163443205236,
99.0079277681159));
#30755=CARTESIAN_POINT('Ctrl Pts',(-16.5890378089614,-3.01654651232763,
99.1402125820154));
#30756=CARTESIAN_POINT('Ctrl Pts',(-16.4374762686563,-3.47698561123553,
98.9284804941285));
#30757=CARTESIAN_POINT('Ctrl Pts',(-16.5106768516081,-3.39212226297961,
99.1468659074355));
#30758=CARTESIAN_POINT('Ctrl Pts',(-16.4078485131273,-3.21487371577898,
99.282087448839));
#30759=CARTESIAN_POINT('Ctrl Pts',(-16.2075579278768,-3.77068327953477,
99.1108598027294));
#30760=CARTESIAN_POINT('Ctrl Pts',(-16.2598042688104,-3.699711420573,99.3254864613232));
#30761=CARTESIAN_POINT('Ctrl Pts',(-16.1506324221157,-3.54922452427082,
99.4644671720467));
#30762=CARTESIAN_POINT('Ctrl Pts',(-16.1328338869384,-3.87465067488062,
99.1667281040793));
#30763=CARTESIAN_POINT('Ctrl Pts',(-16.1785346664591,-3.80861210815923,
99.3801095631261));
#30764=CARTESIAN_POINT('Ctrl Pts',(-16.066957542548,-3.66757422893071,99.5203355960163));
#30765=CARTESIAN_POINT('Ctrl Pts',(-15.9919866048145,-4.0899475674556,99.2638527346786));
#30766=CARTESIAN_POINT('Ctrl Pts',(-16.0257056636234,-4.03466861210512,
99.4749661095219));
#30767=CARTESIAN_POINT('Ctrl Pts',(-15.9090517391358,-3.91261572849114,
99.6174604374821));
#30768=CARTESIAN_POINT('Ctrl Pts',(-15.9254898327248,-4.20166713029529,
99.30543993253));
#30769=CARTESIAN_POINT('Ctrl Pts',(-15.9535873993429,-4.15233969324173,
99.515658214164));
#30770=CARTESIAN_POINT('Ctrl Pts',(-15.834403694553,-4.03975173211336,99.6590477275195));
#30771=CARTESIAN_POINT('Ctrl Pts',(-15.738603988475,-4.55006349017939,99.407174605891));
#30772=CARTESIAN_POINT('Ctrl Pts',(-15.7519852189442,-4.51914563857056,
99.6148745113244));
#30773=CARTESIAN_POINT('Ctrl Pts',(-15.6242698911513,-4.43612723332494,
99.7607826165559));
#30774=CARTESIAN_POINT('Ctrl Pts',(-15.6300705661688,-4.80379339451677,
99.4435386777497));
#30775=CARTESIAN_POINT('Ctrl Pts',(-15.6349263242121,-4.78871307695036,
99.6506668510312));
#30776=CARTESIAN_POINT('Ctrl Pts',(-15.501725341209,-4.72466850699754,99.7971467765044));
#30777=CARTESIAN_POINT('Ctrl Pts',(-15.5059824861585,-5.18799157661508,
99.4425027003972));
#30778=CARTESIAN_POINT('Ctrl Pts',(-15.5033523953773,-5.19622875259016,
99.6496543232893));
#30779=CARTESIAN_POINT('Ctrl Pts',(-15.3607119866153,-5.1611950812275,99.7961107967627));
#30780=CARTESIAN_POINT('Ctrl Pts',(-15.4705223787628,-5.31743764272474,
99.4333242900206));
#30781=CARTESIAN_POINT('Ctrl Pts',(-15.466074874266,-5.33377871102699,99.6406660872409));
#30782=CARTESIAN_POINT('Ctrl Pts',(-15.3202268375058,-5.30821065016262,
99.786932365797));
#30783=CARTESIAN_POINT('Ctrl Pts',(-15.4112870235324,-5.57906517882993,
99.3975703058089));
#30784=CARTESIAN_POINT('Ctrl Pts',(-15.4046994857703,-5.61160402086348,
99.605723827768));
#30785=CARTESIAN_POINT('Ctrl Pts',(-15.2521751775211,-5.60519824976417,
99.7511783033391));
#30786=CARTESIAN_POINT('Ctrl Pts',(-15.3873774999491,-5.71249818528166,
99.370619399419));
#30787=CARTESIAN_POINT('Ctrl Pts',(-15.3804432938941,-5.75346933726169,
99.5793392014518));
#30788=CARTESIAN_POINT('Ctrl Pts',(-15.2244484235508,-5.75658897920125,
99.7242273368566));
#30789=CARTESIAN_POINT('Ctrl Pts',(-15.3346696945248,-6.10616299653759,
99.2668124456042));
#30790=CARTESIAN_POINT('Ctrl Pts',(-15.3287678592426,-6.17236078267475,
99.4777222783444));
#30791=CARTESIAN_POINT('Ctrl Pts',(-15.1624256089298,-6.20298061454582,
99.6204201490477));
#30792=CARTESIAN_POINT('Ctrl Pts',(-15.3240667024475,-6.35937968875464,
99.1683014346688));
#30793=CARTESIAN_POINT('Ctrl Pts',(-15.3219320743537,-6.44185472978044,
99.3809681438969));
#30794=CARTESIAN_POINT('Ctrl Pts',(-15.1483769580277,-6.48977650021881,
99.5219089068377));
#30795=CARTESIAN_POINT('Ctrl Pts',(-15.3423230787144,-6.8517981468712,98.9266153300885));
#30796=CARTESIAN_POINT('Ctrl Pts',(-15.3517693972098,-6.9636263391151,99.1450562468822));
#30797=CARTESIAN_POINT('Ctrl Pts',(-15.1643067184423,-7.04682949241124,
99.2802222813138));
#30798=CARTESIAN_POINT('Ctrl Pts',(-15.3719403060825,-7.09247220631558,
98.7818489409676));
#30799=CARTESIAN_POINT('Ctrl Pts',(-15.389921523533,-7.21841417521539,99.0032991843689));
#30800=CARTESIAN_POINT('Ctrl Pts',(-15.1951156833261,-7.31874252774749,
99.1354555654038));
#30801=CARTESIAN_POINT('Ctrl Pts',(-15.4635565835937,-7.55131386467538,
98.463752920865));
#30802=CARTESIAN_POINT('Ctrl Pts',(-15.5012645827008,-7.70215187775885,
98.693197017485));
#30803=CARTESIAN_POINT('Ctrl Pts',(-15.2930580254491,-7.83652577451189,
98.8173588681435));
#30804=CARTESIAN_POINT('Ctrl Pts',(-15.5265390080494,-7.77132456514675,
98.288422358841));
#30805=CARTESIAN_POINT('Ctrl Pts',(-15.5763509022929,-7.93321211455735,
98.5220290044167));
#30806=CARTESIAN_POINT('Ctrl Pts',(-15.3612680514613,-8.08445864282625,
98.6420342840825));
#30807=CARTESIAN_POINT('Ctrl Pts',(-15.603214142857,-7.98099597085232,98.102881938306));
#30808=CARTESIAN_POINT('Ctrl Pts',(-15.6650624954312,-8.15000252613851,
98.3435328810485));
#30809=CARTESIAN_POINT('Ctrl Pts',(-15.4448833406397,-8.32048399586279,
98.4564865389123));
#30810=CARTESIAN_POINT('Ctrl Pts',(-17.1226665060507,-2.85087466017704,
98.292893219028));
#30811=CARTESIAN_POINT('Ctrl Pts',(-17.1491844558325,-2.83095542391483,
98.310473897128));
#30812=CARTESIAN_POINT('Ctrl Pts',(-17.1736001786359,-2.80849354481796,
98.3279440199927));
#30813=CARTESIAN_POINT('Ctrl Pts',(-17.1956168299013,-2.78379335215336,
98.3450378047718));
#30814=CARTESIAN_POINT('Ctrl Pts',(-17.2156466200124,-2.7613221929924,98.3605889854306));
#30815=CARTESIAN_POINT('Ctrl Pts',(-17.2336921685873,-2.73699581704382,
98.3758286873264));
#30816=CARTESIAN_POINT('Ctrl Pts',(-17.2494951641405,-2.71102785619787,
98.3905567849915));
#30817=CARTESIAN_POINT('Ctrl Pts',(-17.2639409440285,-2.68729011323276,
98.4040199829228));
#30818=CARTESIAN_POINT('Ctrl Pts',(-17.2765129069594,-2.66217890820016,
98.4170556797135));
#30819=CARTESIAN_POINT('Ctrl Pts',(-17.2869749123189,-2.63587291041262,
98.429511010707));
#30820=CARTESIAN_POINT('Ctrl Pts',(-17.2964430397793,-2.61206595070767,
98.4407831002688));
#30821=CARTESIAN_POINT('Ctrl Pts',(-17.3041825761053,-2.58727949046054,
98.4515798544673));
#30822=CARTESIAN_POINT('Ctrl Pts',(-17.3099886550732,-2.56167649681956,
98.461787966872));
#30823=CARTESIAN_POINT('Ctrl Pts',(-17.3128548068309,-2.54903766334346,
98.4668271679356));
#30824=CARTESIAN_POINT('Ctrl Pts',(-17.3152493576056,-2.53620042323942,
98.471722924605));
#30825=CARTESIAN_POINT('Ctrl Pts',(-17.3171452461371,-2.52318856294818,
98.4764616066469));
#30826=CARTESIAN_POINT('Origin',(-15.0469618583258,-7.90408080222984,98.2808650734415));
#30827=CARTESIAN_POINT('Origin',(-16.822369667676,-2.45109746114966,100.));
#30828=CARTESIAN_POINT('Ctrl Pts',(-17.122666505727,-2.85087466042014,0.5));
#30829=CARTESIAN_POINT('Ctrl Pts',(-17.1234615233844,-2.85027747456476,
0.498951748855855));
#30830=CARTESIAN_POINT('Ctrl Pts',(-17.1242547622617,-2.84967791522736,
0.497903494266366));
#30831=CARTESIAN_POINT('Ctrl Pts',(-17.1958659280832,-2.79521512742361,
0.403057585843291));
#30832=CARTESIAN_POINT('Ctrl Pts',(-17.2515645061835,-2.72304942305474,
0.310543821790061));
#30833=CARTESIAN_POINT('Ctrl Pts',(-17.3007393793638,-2.60203756316618,
0.195519413314588));
#30834=CARTESIAN_POINT('Ctrl Pts',(-17.3113366479633,-2.56305412818102,
0.163202546768072));
#30835=CARTESIAN_POINT('Ctrl Pts',(-17.3171452461371,-2.52318856294818,
0.134720657333154));
#30836=CARTESIAN_POINT('Origin',(-15.0503018864028,-7.90496129833282,100.));
#30837=CARTESIAN_POINT('Ctrl Pts',(-15.4929578242382,-8.13746016004849,
0.134720657333154));
#30838=CARTESIAN_POINT('Ctrl Pts',(-15.5116909609204,-8.10179403194155,
0.163202546768232));
#30839=CARTESIAN_POINT('Ctrl Pts',(-15.5260314786975,-8.06402685234187,
0.195519413314936));
#30840=CARTESIAN_POINT('Ctrl Pts',(-15.5573771571874,-7.93722193595586,
0.310543821769176));
#30841=CARTESIAN_POINT('Ctrl Pts',(-15.5547339977031,-7.84609985192745,
0.403057585811652));
#30842=CARTESIAN_POINT('Ctrl Pts',(-15.5288117710302,-7.7599465438431,0.497903494266294));
#30843=CARTESIAN_POINT('Ctrl Pts',(-15.5285224394342,-7.75899523603616,
0.498951748855642));
#30844=CARTESIAN_POINT('Ctrl Pts',(-15.5282302736771,-7.75804480287585,
0.5));
#30845=CARTESIAN_POINT('Origin',(-19.8181570368417,-6.43930956430665,0.5));
#30846=CARTESIAN_POINT('Ctrl Pts',(-17.3656407514415,2.36084587016586,98.4746163542476));
#30847=CARTESIAN_POINT('Ctrl Pts',(-17.4440265737737,2.62644363351055,98.3611663178014));
#30848=CARTESIAN_POINT('Ctrl Pts',(-17.2962665385767,2.72681679293049,98.1210629636544));
#30849=CARTESIAN_POINT('Ctrl Pts',(-16.9690963360076,2.6361363763642,98.8304618827575));
#30850=CARTESIAN_POINT('Ctrl Pts',(-17.0649442889615,2.86366294455722,98.7002300650182));
#30851=CARTESIAN_POINT('Ctrl Pts',(-16.940267897606,2.96864610960449,98.4769098403635));
#30852=CARTESIAN_POINT('Ctrl Pts',(-16.5793520854839,2.99263453638016,99.160238287598));
#30853=CARTESIAN_POINT('Ctrl Pts',(-16.6807262887868,3.18423851866632,99.0255494138259));
#30854=CARTESIAN_POINT('Ctrl Pts',(-16.5907862689845,3.2817310397979,98.8066848982746));
#30855=CARTESIAN_POINT('Ctrl Pts',(-16.06825893873,3.65601467024584,99.5229830380904));
#30856=CARTESIAN_POINT('Ctrl Pts',(-16.1805213417477,3.7965790026359,99.3820315078356));
#30857=CARTESIAN_POINT('Ctrl Pts',(-16.133918665385,3.86446114696819,99.1694296468622));
#30858=CARTESIAN_POINT('Ctrl Pts',(-15.9074663690937,3.90241128133996,99.6234913693271));
#30859=CARTESIAN_POINT('Ctrl Pts',(-16.0241813784637,4.02429095582591,99.480742609552));
#30860=CARTESIAN_POINT('Ctrl Pts',(-15.9904645360932,4.08092818635339,99.2699379792856));
#30861=CARTESIAN_POINT('Ctrl Pts',(-15.6245522069473,4.43521068708326,99.7608048122955));
#30862=CARTESIAN_POINT('Ctrl Pts',(-15.7522284341316,4.51825273440706,99.6149071958598));
#30863=CARTESIAN_POINT('Ctrl Pts',(-15.7388387964642,4.54924202638999,99.4072514211504));
#30864=CARTESIAN_POINT('Ctrl Pts',(-15.504446230321,4.71763971050837,99.7966027452519));
#30865=CARTESIAN_POINT('Ctrl Pts',(-15.637469741455,4.7821404952994,99.6501526042829));
#30866=CARTESIAN_POINT('Ctrl Pts',(-15.6324601989205,4.79760023853937,99.4430493547679));
#30867=CARTESIAN_POINT('Ctrl Pts',(-15.3625803721861,5.15483225994642,99.79636776423));
#30868=CARTESIAN_POINT('Ctrl Pts',(-15.5050490252728,5.19027311193616,99.6499229371967));
#30869=CARTESIAN_POINT('Ctrl Pts',(-15.5076044740504,5.18238705961226,99.442814373582));
#30870=CARTESIAN_POINT('Ctrl Pts',(-15.3211549463132,5.30458937654559,99.7872514480856));
#30871=CARTESIAN_POINT('Ctrl Pts',(-15.4668882655262,5.33038662434119,99.6409952531274));
#30872=CARTESIAN_POINT('Ctrl Pts',(-15.4713150290528,5.31424796399505,99.4336980572382));
#30873=CARTESIAN_POINT('Ctrl Pts',(-15.2524387792612,5.60380285207595,99.7514230350794));
#30874=CARTESIAN_POINT('Ctrl Pts',(-15.4048955461524,5.61029467639245,99.6059800049562));
#30875=CARTESIAN_POINT('Ctrl Pts',(-15.4114951404923,5.57783990353127,99.3978696447402));
#30876=CARTESIAN_POINT('Ctrl Pts',(-15.2252322104212,5.75229303761896,99.7250021223377));
#30877=CARTESIAN_POINT('Ctrl Pts',(-15.3810929371293,5.74943839640557,99.580115086457));
#30878=CARTESIAN_POINT('Ctrl Pts',(-15.3880333336981,5.70871875235814,99.3714487314956));
#30879=CARTESIAN_POINT('Ctrl Pts',(-15.1632690619361,6.19474020261685,99.6227146850678));
#30880=CARTESIAN_POINT('Ctrl Pts',(-15.3293788683914,6.16461669902704,99.4799874409064));
#30881=CARTESIAN_POINT('Ctrl Pts',(-15.3353499887989,6.09890683169306,99.2691612949723));
#30882=CARTESIAN_POINT('Ctrl Pts',(-15.148371564977,6.48916504798086,99.5221656588589));
#30883=CARTESIAN_POINT('Ctrl Pts',(-15.3218719375044,6.44129651453844,99.3812294188918));
#30884=CARTESIAN_POINT('Ctrl Pts',(-15.3240366258068,6.35885837698121,99.1686122675856));
#30885=CARTESIAN_POINT('Ctrl Pts',(-15.1643710385716,7.04782935834292,99.2797533468151));
#30886=CARTESIAN_POINT('Ctrl Pts',(-15.3518153879025,6.96458278973326,99.1446071116388));
#30887=CARTESIAN_POINT('Ctrl Pts',(-15.3423676517735,6.85271014840536,98.9261999569019));
#30888=CARTESIAN_POINT('Ctrl Pts',(-15.1944125118882,7.3137850593314,99.1382521541667));
#30889=CARTESIAN_POINT('Ctrl Pts',(-15.3890461250777,7.21380562024102,99.0060308920463));
#30890=CARTESIAN_POINT('Ctrl Pts',(-15.3712539451641,7.08811389017403,98.7846987631153));
#30891=CARTESIAN_POINT('Ctrl Pts',(-15.2907248901618,7.82511262538337,98.8245648611895));
#30892=CARTESIAN_POINT('Ctrl Pts',(-15.4985537486391,7.69138492458409,98.7003130263029));
#30893=CARTESIAN_POINT('Ctrl Pts',(-15.461363297308,7.54123627293827,98.4710114710543));
#30894=CARTESIAN_POINT('Ctrl Pts',(-15.3574639152262,8.06994831582745,98.6521093612504));
#30895=CARTESIAN_POINT('Ctrl Pts',(-15.5720250893883,7.91951631844514,98.5320184901583));
#30896=CARTESIAN_POINT('Ctrl Pts',(-15.5230000877306,7.75847929885542,98.298561852705));
#30897=CARTESIAN_POINT('Ctrl Pts',(-15.4367365239838,8.29721036780905,98.4746887503082));
#30898=CARTESIAN_POINT('Ctrl Pts',(-15.6562640576654,8.12841791648205,98.3612367156073));
#30899=CARTESIAN_POINT('Ctrl Pts',(-15.5957265901482,7.96036688919461,98.1211353597149));
#30900=CARTESIAN_POINT('Ctrl Pts',(-15.5282302741409,7.75804480438455,98.2928932196501));
#30901=CARTESIAN_POINT('Ctrl Pts',(-15.5379755127708,7.78974666481774,98.3104738977231));
#30902=CARTESIAN_POINT('Ctrl Pts',(-15.5445254860964,7.82226990849227,98.3279440205588));
#30903=CARTESIAN_POINT('Ctrl Pts',(-15.5478189220795,7.85519384700696,98.3450378053077));
#30904=CARTESIAN_POINT('Ctrl Pts',(-15.5508151466501,7.88514661185367,98.3605889859386));
#30905=CARTESIAN_POINT('Ctrl Pts',(-15.5511156170357,7.91543397069313,98.3758286878054));
#30906=CARTESIAN_POINT('Ctrl Pts',(-15.5486369245292,7.94573126001502,98.390556785441));
#30907=CARTESIAN_POINT('Ctrl Pts',(-15.5463711106682,7.97342651383039,98.4040199833497));
#30908=CARTESIAN_POINT('Ctrl Pts',(-15.5417820463004,8.00113151982359,98.4170556801172));
#30909=CARTESIAN_POINT('Ctrl Pts',(-15.5347837088429,8.0285629315143,98.4295110110869));
#30910=CARTESIAN_POINT('Ctrl Pts',(-15.5284502050059,8.05338839216903,98.4407831006321));
#30911=CARTESIAN_POINT('Ctrl Pts',(-15.5201425055928,8.07799024503,98.4515798548133));
#30912=CARTESIAN_POINT('Ctrl Pts',(-15.5097906600338,8.10211622955971,98.4617879672));
#30913=CARTESIAN_POINT('Ctrl Pts',(-15.5046805056801,8.1140259421013,98.4668271681481));
#30914=CARTESIAN_POINT('Ctrl Pts',(-15.4990721976482,8.12581896887833,98.4717229247079));
#30915=CARTESIAN_POINT('Ctrl Pts',(-15.4929578242382,8.13746016004849,98.4764616066469));
#30916=CARTESIAN_POINT('Ctrl Pts',(-17.3171452461371,2.52318856294819,98.4764616066469));
#30917=CARTESIAN_POINT('Ctrl Pts',(-17.3132089417596,2.55020420325263,98.4666230035038));
#30918=CARTESIAN_POINT('Ctrl Pts',(-17.3071132371149,2.57652769355676,98.4560730110189));
#30919=CARTESIAN_POINT('Ctrl Pts',(-17.2990811363583,2.60191581423307,98.4449543865016));
#30920=CARTESIAN_POINT('Ctrl Pts',(-17.2902502712358,2.62982869483543,98.4327300536111));
#30921=CARTESIAN_POINT('Ctrl Pts',(-17.279079410547,2.65661115931325,98.4198183682014));
#30922=CARTESIAN_POINT('Ctrl Pts',(-17.2658576960657,2.6820051671168,98.4064090535706));
#30923=CARTESIAN_POINT('Ctrl Pts',(-17.2516730980718,2.70924851688491,98.3920231932739));
#30924=CARTESIAN_POINT('Ctrl Pts',(-17.2351284858644,2.73489473600463,98.3770645839114));
#30925=CARTESIAN_POINT('Ctrl Pts',(-17.2165633719882,2.75868699848906,98.3617674910388));
#30926=CARTESIAN_POINT('Ctrl Pts',(-17.1948268080254,2.78654365688397,98.343857219123));
#30927=CARTESIAN_POINT('Ctrl Pts',(-17.17032059483,2.81185976437969,98.3254829407031));
#30928=CARTESIAN_POINT('Ctrl Pts',(-17.1435596962152,2.83429057899883,98.3070206561438));
#30929=CARTESIAN_POINT('Ctrl Pts',(-17.1367405896413,2.84000631065752,98.3023161696533));
#30930=CARTESIAN_POINT('Ctrl Pts',(-17.1297749579741,2.84553494376039,98.2976059688167));
#30931=CARTESIAN_POINT('Ctrl Pts',(-17.1226711151596,2.85087119795497,98.2928962747546));
#30932=CARTESIAN_POINT('Origin',(-15.0503018864028,7.90496129833282,100.));
#30933=CARTESIAN_POINT('Ctrl Pts',(-15.5282302736771,7.75804480287585,0.5));
#30934=CARTESIAN_POINT('Ctrl Pts',(-15.5285224394341,7.75899523603604,0.498951748855783));
#30935=CARTESIAN_POINT('Ctrl Pts',(-15.5288117710301,7.75994654384298,0.497903494266496));
#30936=CARTESIAN_POINT('Ctrl Pts',(-15.5547339977038,7.84609985192962,0.403057585807818));
#30937=CARTESIAN_POINT('Ctrl Pts',(-15.5573771571867,7.93722193595853,0.310543821766792));
#30938=CARTESIAN_POINT('Ctrl Pts',(-15.5260314786975,8.06402685234172,0.195519413315069));
#30939=CARTESIAN_POINT('Ctrl Pts',(-15.5116909609204,8.10179403194149,0.163202546768283));
#30940=CARTESIAN_POINT('Ctrl Pts',(-15.4929578242382,8.13746016004849,0.134720657333155));
#30941=CARTESIAN_POINT('Origin',(-16.822369667676,2.45109746114966,100.));
#30942=CARTESIAN_POINT('Ctrl Pts',(-17.3171452461371,2.52318856294819,0.134720657333156));
#30943=CARTESIAN_POINT('Ctrl Pts',(-17.3113366479633,2.56305412818148,0.163202546768402));
#30944=CARTESIAN_POINT('Ctrl Pts',(-17.3007393793636,2.60203756316703,0.195519413315302));
#30945=CARTESIAN_POINT('Ctrl Pts',(-17.2515645061962,2.72304942302292,0.310543821760042));
#30946=CARTESIAN_POINT('Ctrl Pts',(-17.1958659281084,2.79521512740442,0.403057585797637));
#30947=CARTESIAN_POINT('Ctrl Pts',(-17.124254762262,2.84967791522717,0.497903494266591));
#30948=CARTESIAN_POINT('Ctrl Pts',(-17.1234615233845,2.85027747456468,0.498951748855702));
#30949=CARTESIAN_POINT('Ctrl Pts',(-17.122666505727,2.85087466042014,0.5));
#30950=CARTESIAN_POINT('Origin',(-19.8181570368417,6.43930956430665,0.5));
#30951=CARTESIAN_POINT('Ctrl Pts',(-7.9321719283244,15.6280424815024,98.1029310403532));
#30952=CARTESIAN_POINT('Ctrl Pts',(-7.88286802685643,15.8011193837335,98.3435819249719));
#30953=CARTESIAN_POINT('Ctrl Pts',(-7.6045369593422,15.809621013675,98.4565369103438));
#30954=CARTESIAN_POINT('Ctrl Pts',(-7.99314885854456,15.4140497422028,98.2878840681093));
#30955=CARTESIAN_POINT('Ctrl Pts',(-7.93830133829255,15.5743539404689,98.521498203427));
#30956=CARTESIAN_POINT('Ctrl Pts',(-7.67534747321984,15.5703297982934,98.6414834345645));
#30957=CARTESIAN_POINT('Ctrl Pts',(-8.07342544701438,15.1939319565419,98.4673409001115));
#30958=CARTESIAN_POINT('Ctrl Pts',(-8.01520601240624,15.337817496613,98.696680627363));
#30959=CARTESIAN_POINT('Ctrl Pts',(-7.76810813773555,15.3239231079797,98.8209468546291));
#30960=CARTESIAN_POINT('Ctrl Pts',(-8.27074145233702,14.7666413443144,98.786605947879));
#30961=CARTESIAN_POINT('Ctrl Pts',(-8.21126794551343,14.8786168342417,99.0079277681179));
#30962=CARTESIAN_POINT('Ctrl Pts',(-7.99520082055387,14.8449483706469,99.1402125820163));
#30963=CARTESIAN_POINT('Ctrl Pts',(-8.38626933427948,14.5585212736839,98.9284804941305));
#30964=CARTESIAN_POINT('Ctrl Pts',(-8.32817971805768,14.6543633819072,99.1468659074353));
#30965=CARTESIAN_POINT('Ctrl Pts',(-8.12783062814333,14.6113406338476,99.2820874488399));
#30966=CARTESIAN_POINT('Ctrl Pts',(-8.59454374091723,14.2490983667564,99.1108598027282));
#30967=CARTESIAN_POINT('Ctrl Pts',(-8.54319049921983,14.3207191002957,99.325486461323));
#30968=CARTESIAN_POINT('Ctrl Pts',(-8.3663329999394,14.2633935124894,99.4644671720462));
#30969=CARTESIAN_POINT('Ctrl Pts',(-8.67033161120472,14.1459038886755,99.1667281040791));
#30970=CARTESIAN_POINT('Ctrl Pts',(-8.62164751952555,14.2097749522394,99.380109563126));
#30971=CARTESIAN_POINT('Ctrl Pts',(-8.45303329796889,14.1472419030066,99.5203355960162));
#30972=CARTESIAN_POINT('Ctrl Pts',(-8.83156692003832,13.9454197645674,99.2638527346784));
#30973=CARTESIAN_POINT('Ctrl Pts',(-8.78941327154469,13.9945706318057,99.4749661095217));
#30974=CARTESIAN_POINT('Ctrl Pts',(-8.63728603612372,13.9213425720195,99.617460437482));
#30975=CARTESIAN_POINT('Ctrl Pts',(-8.91726990562776,13.8476543326374,99.3054399325309));
#30976=CARTESIAN_POINT('Ctrl Pts',(-8.87903935077148,13.8896197228001,99.515658214165));
#30977=CARTESIAN_POINT('Ctrl Pts',(-8.73513204645105,13.8110608770737,99.6590477275199));
#30978=CARTESIAN_POINT('Ctrl Pts',(-9.19086363206821,13.5622549366773,99.4071746058888));
#30979=CARTESIAN_POINT('Ctrl Pts',(-9.16559403544637,13.5845353846879,99.6148745113222));
#30980=CARTESIAN_POINT('Ctrl Pts',(-9.04717263343547,13.4887249880274,99.7607826165548));
#30981=CARTESIAN_POINT('Ctrl Pts',(-9.3986364390167,13.3806266657361,99.4435386777496));
#30982=CARTESIAN_POINT('Ctrl Pts',(-9.38579471648355,13.3899048404738,99.6506668510311));
#30983=CARTESIAN_POINT('Ctrl Pts',(-9.2837233434811,13.2830140381241,99.7971467765042));
#30984=CARTESIAN_POINT('Ctrl Pts',(-9.72568529812736,13.1438881211714,99.442502700397));
#30985=CARTESIAN_POINT('Ctrl Pts',(-9.73270657526614,13.1388413288334,99.6496543232892));
#30986=CARTESIAN_POINT('Ctrl Pts',(-9.65530926343492,13.0140082384199,99.7961107967627));
#30987=CARTESIAN_POINT('Ctrl Pts',(-9.83783804700205,13.0701625206814,99.4333242900205));
#30988=CARTESIAN_POINT('Ctrl Pts',(-9.85200497202217,13.0608830247369,99.6406660872407));
#30989=CARTESIAN_POINT('Ctrl Pts',(-9.78261877917289,12.9300742643075,99.7869323657969));
#30990=CARTESIAN_POINT('Ctrl Pts',(-10.0683558886233,12.9329789952414,99.3975703058088));
#30991=CARTESIAN_POINT('Ctrl Pts',(-10.0972665052523,12.9166588193608,99.6057238277679));
#30992=CARTESIAN_POINT('Ctrl Pts',(-10.0440416516022,12.7735790742388,99.751178303339));
#30993=CARTESIAN_POINT('Ctrl Pts',(-10.1878697697834,12.8690066204319,99.3706193994188));
#30994=CARTESIAN_POINT('Ctrl Pts',(-10.2246928633405,12.849751016337,99.5793392014517));
#30995=CARTESIAN_POINT('Ctrl Pts',(-10.1794547531643,12.7004270560128,99.7242273368565));
#30996=CARTESIAN_POINT('Ctrl Pts',(-10.5459796461518,12.6972294018582,99.2668124456041));
#30997=CARTESIAN_POINT('Ctrl Pts',(-10.6071137146221,12.6711601820488,99.4777222783443));
#30998=CARTESIAN_POINT('Ctrl Pts',(-10.5848323230216,12.5034972525403,99.6204201490476));
#30999=CARTESIAN_POINT('Ctrl Pts',(-10.7835265265761,12.6088970959964,99.1683014346687));
#31000=CARTESIAN_POINT('Ctrl Pts',(-10.8613053154178,12.581380754749,99.3809681438947));
#31001=CARTESIAN_POINT('Ctrl Pts',(-10.8532501470603,12.4015113889649,99.5219089068378));
#31002=CARTESIAN_POINT('Ctrl Pts',(-11.2574858404351,12.4740942697068,98.9266153300884));
#31003=CARTESIAN_POINT('Ctrl Pts',(-11.3667598443235,12.4485214406135,99.1450562468842));
#31004=CARTESIAN_POINT('Ctrl Pts',(-11.3879615918918,12.2445226500553,99.2802222813136));
#31005=CARTESIAN_POINT('Ctrl Pts',(-11.4955326995551,12.4278895523164,98.7818489409675));
#31006=CARTESIAN_POINT('Ctrl Pts',(-11.6208671315238,12.4060724976491,99.0032991843688));
#31007=CARTESIAN_POINT('Ctrl Pts',(-11.6560867497414,12.1897979679579,99.1354555654036));
#31008=CARTESIAN_POINT('Ctrl Pts',(-11.9602280353382,12.3732319398888,98.4637529209062));
#31009=CARTESIAN_POINT('Ctrl Pts',(-12.1153359231296,12.3624828687138,98.6931970175259));
#31010=CARTESIAN_POINT('Ctrl Pts',(-12.1787937287228,12.1229428480101,98.8173588681849));
#31011=CARTESIAN_POINT('Ctrl Pts',(-12.188933285124,12.3651447396865,98.2884223589317));
#31012=CARTESIAN_POINT('Ctrl Pts',(-12.3582902157324,12.3624926623483,98.5220290045064));
#31013=CARTESIAN_POINT('Ctrl Pts',(-12.4356699558978,12.1111989679492,98.6420342841727));
#31014=CARTESIAN_POINT('Ctrl Pts',(-12.4120365614475,12.3732750986753,98.1028819384482));
#31015=CARTESIAN_POINT('Ctrl Pts',(-12.5918835391586,12.3798704796615,98.3435328811866));
#31016=CARTESIAN_POINT('Ctrl Pts',(-12.6859819511989,12.1177859883826,98.4564865390546));
#31017=CARTESIAN_POINT('Ctrl Pts',(-8.00253786208647,15.4036548381006,98.292893219028));
#31018=CARTESIAN_POINT('Ctrl Pts',(-7.99178803978736,15.4350302895329,98.3104738971094));
#31019=CARTESIAN_POINT('Ctrl Pts',(-7.97797039659482,15.4651921241464,98.3279440199573));
#31020=CARTESIAN_POINT('Ctrl Pts',(-7.9612826368274,15.4937639830745,98.3450378047213));
#31021=CARTESIAN_POINT('Ctrl Pts',(-7.94610084002526,15.5197574155394,98.3605889853761));
#31022=CARTESIAN_POINT('Ctrl Pts',(-7.92854146285382,15.5444370156778,98.375828687269));
#31023=CARTESIAN_POINT('Ctrl Pts',(-7.90872785867543,15.5674910987838,98.3905567849321));
#31024=CARTESIAN_POINT('Ctrl Pts',(-7.89061591503621,15.5885652178644,98.4040199828634));
#31025=CARTESIAN_POINT('Ctrl Pts',(-7.8706186900642,15.6082816542381,98.4170556796548));
#31026=CARTESIAN_POINT('Ctrl Pts',(-7.84883313691036,15.6263606129814,98.4295110106493));
#31027=CARTESIAN_POINT('Ctrl Pts',(-7.82911718504767,15.642722092435,98.4407831002118));
#31028=CARTESIAN_POINT('Ctrl Pts',(-7.80793550877505,15.6577422663405,98.4515798544113));
#31029=CARTESIAN_POINT('Ctrl Pts',(-7.78537979191595,15.6711759357228,98.4617879668172));
#31030=CARTESIAN_POINT('Ctrl Pts',(-7.77424523654401,15.6778074223884,98.4668271679002));
#31031=CARTESIAN_POINT('Ctrl Pts',(-7.76277625253494,15.6840517008834,98.471722924588));
#31032=CARTESIAN_POINT('Ctrl Pts',(-7.75098709974896,15.6898756840048,98.4764616066469));
#31033=CARTESIAN_POINT('Origin',(-12.1669944801976,11.8680158329566,98.2808650734384));
#31034=CARTESIAN_POINT('Origin',(-7.52953032547042,15.2415935216047,100.));
#31035=CARTESIAN_POINT('Ctrl Pts',(-8.00253786221766,15.4036548377177,0.5));
#31036=CARTESIAN_POINT('Ctrl Pts',(-8.00221557868536,15.4045954850197,0.498951748855652));
#31037=CARTESIAN_POINT('Ctrl Pts',(-8.00189048816431,15.4055351740473,0.497903494266625));
#31038=CARTESIAN_POINT('Ctrl Pts',(-7.97222236614597,15.490471366956,0.40305758580859));
#31039=CARTESIAN_POINT('Ctrl Pts',(-7.92080050993637,15.5657442916618,0.310543821767294));
#31040=CARTESIAN_POINT('Ctrl Pts',(-7.82090726356976,15.6499070964475,0.195519413315074));
#31041=CARTESIAN_POINT('Ctrl Pts',(-7.78710654979053,15.6720322417137,0.163202546768292));
#31042=CARTESIAN_POINT('Ctrl Pts',(-7.75098709974896,15.6898756840048,0.134720657333156));
#31043=CARTESIAN_POINT('Origin',(-12.1688640072122,11.8709203002115,100.));
#31044=CARTESIAN_POINT('Ctrl Pts',(-12.5267717721302,12.2200650149237,0.134720657333156));
#31045=CARTESIAN_POINT('Ctrl Pts',(-12.4986401261759,12.2489027263445,0.163202546768228));
#31046=CARTESIAN_POINT('Ctrl Pts',(-12.4671528676167,12.2742120695494,0.195519413314942));
#31047=CARTESIAN_POINT('Ctrl Pts',(-12.3562405729316,12.3432084554757,0.310543821781225));
#31048=CARTESIAN_POINT('Ctrl Pts',(-12.2687615399374,12.3688529339454,0.403057585829754));
#31049=CARTESIAN_POINT('Ctrl Pts',(-12.1788144663217,12.3708222676705,0.497903494266489));
#31050=CARTESIAN_POINT('Ctrl Pts',(-12.1778203104527,12.37084106725,0.498951748856102));
#31051=CARTESIAN_POINT('Ctrl Pts',(-12.1768261106186,12.3708569011015,0.5));
#31052=CARTESIAN_POINT('Origin',(-12.2482946431511,16.8583313034371,0.5));
#31053=CARTESIAN_POINT('Ctrl Pts',(-3.12098026161583,17.2452472912803,98.4746163542476));
#31054=CARTESIAN_POINT('Ctrl Pts',(-2.89260432929213,17.4018708609359,98.3611663178014));
#31055=CARTESIAN_POINT('Ctrl Pts',(-2.75148341999934,17.2923597286537,98.1210629636544));
#31056=CARTESIAN_POINT('Ctrl Pts',(-2.73662446842834,16.9531805857873,98.830461882757));
#31057=CARTESIAN_POINT('Ctrl Pts',(-2.54985248945774,17.1146469822629,98.7002300650194));
#31058=CARTESIAN_POINT('Ctrl Pts',(-2.41148044251214,17.0285142699576,98.4769098403642));
#31059=CARTESIAN_POINT('Ctrl Pts',(-2.27713697342544,16.6926757665454,99.1602382875986));
#31060=CARTESIAN_POINT('Ctrl Pts',(-2.1262371091358,16.8482972498952,99.025549413826));
#31061=CARTESIAN_POINT('Ctrl Pts',(-2.00572321702971,16.7928860538427,98.8066848982746));
#31062=CARTESIAN_POINT('Ctrl Pts',(-1.48828850627704,16.4115930339874,99.5229830380901));
#31063=CARTESIAN_POINT('Ctrl Pts',(-1.38929487236062,16.5617976914248,99.3820315078356));
#31064=CARTESIAN_POINT('Ctrl Pts',(-1.31033409767418,16.5384526486055,99.1694296468622));
#31065=CARTESIAN_POINT('Ctrl Pts',(-1.20426376711567,16.3348109530474,99.6234913693268));
#31066=CARTESIAN_POINT('Ctrl Pts',(-1.12441622988599,16.4834764139428,99.4807426095521));
#31067=CARTESIAN_POINT('Ctrl Pts',(-1.06013194543873,16.4689116580449,99.2699379792856));
#31068=CARTESIAN_POINT('Ctrl Pts',(-0.610116136352994,16.2303876665528,
99.7608048122958));
#31069=CARTESIAN_POINT('Ctrl Pts',(-0.570592580096672,16.3774763782636,
99.6149071958598));
#31070=CARTESIAN_POINT('Ctrl Pts',(-0.536982386433238,16.3743182939755,
99.4072514211504));
#31071=CARTESIAN_POINT('Ctrl Pts',(-0.30439538532984,16.2034354627788,99.7966027452528));
#31072=CARTESIAN_POINT('Ctrl Pts',(-0.284158019240097,16.349880178516,99.6501526042807));
#31073=CARTESIAN_POINT('Ctrl Pts',(-0.267906895914236,16.3498931438339,
99.44304935477));
#31074=CARTESIAN_POINT('Ctrl Pts',(0.15523839877392,16.2036129415517,99.7963677642295));
#31075=CARTESIAN_POINT('Ctrl Pts',(0.144919417032302,16.3500605079967,99.6499229371978));
#31076=CARTESIAN_POINT('Ctrl Pts',(0.136629658481294,16.3500539600225,99.442814373581));
#31077=CARTESIAN_POINT('Ctrl Pts',(0.310467040971329,16.2104925143924,99.7872514480855));
#31078=CARTESIAN_POINT('Ctrl Pts',(0.289967609306312,16.3570649252483,99.6409952531274));
#31079=CARTESIAN_POINT('Ctrl Pts',(0.273250886060001,16.3562879072327,99.4336980572382));
#31080=CARTESIAN_POINT('Ctrl Pts',(0.616270430044837,16.2376016048274,99.7514230350795));
#31081=CARTESIAN_POINT('Ctrl Pts',(0.575332789986894,16.3846026904707,99.6059800049562));
#31082=CARTESIAN_POINT('Ctrl Pts',(0.542427079965384,16.3808502013102,99.3978696447402));
#31083=CARTESIAN_POINT('Ctrl Pts',(0.765900280741983,16.2576126110769,99.7250021223377));
#31084=CARTESIAN_POINT('Ctrl Pts',(0.715021742305763,16.4049628381998,99.580115086457));
#31085=CARTESIAN_POINT('Ctrl Pts',(0.67415035900587,16.3989804855663,99.3714487314956));
#31086=CARTESIAN_POINT('Ctrl Pts',(1.20584020603573,16.3354058480374,99.6227146850678));
#31087=CARTESIAN_POINT('Ctrl Pts',(1.12586029852619,16.4840769873469,99.4799874409063));
#31088=CARTESIAN_POINT('Ctrl Pts',(1.06152132333173,16.4694503946166,99.2691612949723));
#31089=CARTESIAN_POINT('Ctrl Pts',(1.4904584535125,16.4122197672618,99.5221656588587));
#31090=CARTESIAN_POINT('Ctrl Pts',(1.39131820921548,16.5624362368043,99.3812294188917));
#31091=CARTESIAN_POINT('Ctrl Pts',(1.31224595582737,16.5390201922298,99.1686122675856));
#31092=CARTESIAN_POINT('Ctrl Pts',(2.01683567706278,16.6000729369334,99.2797533468153));
#31093=CARTESIAN_POINT('Ctrl Pts',(1.87973999608435,16.7526185023833,99.1446071116388));
#31094=CARTESIAN_POINT('Ctrl Pts',(1.7762623025766,16.7090626239981,98.9261999569019));
#31095=CARTESIAN_POINT('Ctrl Pts',(2.2604912537429,16.7108289072469,99.1382521541666));
#31096=CARTESIAN_POINT('Ctrl Pts',(2.10526006254853,16.865041127594,99.0060308920483));
#31097=CARTESIAN_POINT('Ctrl Pts',(1.9912182095838,16.8092788783049,98.7846987631153));
#31098=CARTESIAN_POINT('Ctrl Pts',(2.71703050574192,16.9604363298062,98.8245648611896));
#31099=CARTESIAN_POINT('Ctrl Pts',(2.52562525529636,17.1167691877694,98.7003130263007));
#31100=CARTESIAN_POINT('Ctrl Pts',(2.39431788322584,17.035000481646,98.4710114710543));
#31101=CARTESIAN_POINT('Ctrl Pts',(2.92925959162593,17.0995673036633,98.6521093612491));
#31102=CARTESIAN_POINT('Ctrl Pts',(2.71988721110643,17.2571410628035,98.5320184901564));
#31103=CARTESIAN_POINT('Ctrl Pts',(2.58188146292243,17.1607523397371,98.298561852701));
#31104=CARTESIAN_POINT('Ctrl Pts',(3.12090206377706,17.2451878710232,98.4746887503082));
#31105=CARTESIAN_POINT('Ctrl Pts',(2.89253316440024,17.4018112264551,98.3612367156073));
#31106=CARTESIAN_POINT('Ctrl Pts',(2.75141424608767,17.2923060501388,98.1211353597149));
#31107=CARTESIAN_POINT('Ctrl Pts',(2.57985201764259,17.1655922764305,98.2928932196501));
#31108=CARTESIAN_POINT('Ctrl Pts',(2.60699083419288,17.1846569627295,98.3104738976888));
#31109=CARTESIAN_POINT('Ctrl Pts',(2.635898223901,17.2009365925282,98.3279440204933));
#31110=CARTESIAN_POINT('Ctrl Pts',(2.66619302242479,17.2142428927914,98.3450378052143));
#31111=CARTESIAN_POINT('Ctrl Pts',(2.69375391028467,17.2263483850626,98.3605889858378));
#31112=CARTESIAN_POINT('Ctrl Pts',(2.72246604979616,17.2359934579821,98.3758286876993));
#31113=CARTESIAN_POINT('Ctrl Pts',(2.75204644232091,17.2429984586142,98.3905567853312));
#31114=CARTESIAN_POINT('Ctrl Pts',(2.77908636891128,17.2494018456788,98.40401998324));
#31115=CARTESIAN_POINT('Ctrl Pts',(2.80685349426263,17.2535987038001,98.4170556800087));
#31116=CARTESIAN_POINT('Ctrl Pts',(2.83510492229913,17.2554196617626,98.4295110109802));
#31117=CARTESIAN_POINT('Ctrl Pts',(2.86067249873503,17.2570676309142,98.4407831005269));
#31118=CARTESIAN_POINT('Ctrl Pts',(2.88663747150523,17.256768929892,98.45157985471));
#31119=CARTESIAN_POINT('Ctrl Pts',(2.91278154249718,17.2543790789575,98.4617879670986));
#31120=CARTESIAN_POINT('Ctrl Pts',(2.9256874768416,17.2531993369325,98.4668271680826));
#31121=CARTESIAN_POINT('Ctrl Pts',(2.93863637438248,17.2515097647149,98.4717229246763));
#31122=CARTESIAN_POINT('Ctrl Pts',(2.95159725048241,17.2492919759318,98.4764616066469));
#31123=CARTESIAN_POINT('Ctrl Pts',(-2.95159725048241,17.2492919759318,98.4764616066469));
#31124=CARTESIAN_POINT('Ctrl Pts',(-2.92468746478162,17.2538966199714,98.4666230035039));
#31125=CARTESIAN_POINT('Ctrl Pts',(-2.89776866146892,17.2562336662028,98.4560730110185));
#31126=CARTESIAN_POINT('Ctrl Pts',(-2.8711410682296,17.256440045183,98.4449543865007));
#31127=CARTESIAN_POINT('Ctrl Pts',(-2.84186545383984,17.256666947832,98.4327300536064));
#31128=CARTESIAN_POINT('Ctrl Pts',(-2.81294183067497,17.2543190646552,98.4198183681925));
#31129=CARTESIAN_POINT('Ctrl Pts',(-2.78470495960319,17.2495916469058,98.4064090535574));
#31130=CARTESIAN_POINT('Ctrl Pts',(-2.75441171242718,17.2445199506112,98.3920231932519));
#31131=CARTESIAN_POINT('Ctrl Pts',(-2.7249081422635,17.2367102069049,98.3770645838805));
#31132=CARTESIAN_POINT('Ctrl Pts',(-2.69654342028693,17.2264059478107,98.3617674909993));
#31133=CARTESIAN_POINT('Ctrl Pts',(-2.66333319608111,17.2143414278385,98.343857219053));
#31134=CARTESIAN_POINT('Ctrl Pts',(-2.63168331068654,17.1988577415015,98.3254829406024));
#31135=CARTESIAN_POINT('Ctrl Pts',(-2.60208076577926,17.1803381173616,98.3070206560147));
#31136=CARTESIAN_POINT('Ctrl Pts',(-2.59453756219189,17.1756190198757,98.3023161695671));
#31137=CARTESIAN_POINT('Ctrl Pts',(-2.58712702115892,17.1707027521152,98.2976059687736));
#31138=CARTESIAN_POINT('Ctrl Pts',(-2.57985673374437,17.1655955893937,98.2928962747547));
#31139=CARTESIAN_POINT('Origin',(2.86726590046863,16.7564550623337,100.));
#31140=CARTESIAN_POINT('Ctrl Pts',(2.57985201635105,17.1655922755232,0.5));
#31141=CARTESIAN_POINT('Ctrl Pts',(2.58066564781748,17.1661638416689,0.498951748855505));
#31142=CARTESIAN_POINT('Ctrl Pts',(2.58148098692646,17.1667329826481,0.497903494266865));
#31143=CARTESIAN_POINT('Ctrl Pts',(2.6554072434575,17.2180093215973,0.403057585720023));
#31144=CARTESIAN_POINT('Ctrl Pts',(2.74125271406851,17.2486813881449,0.310543821709137));
#31145=CARTESIAN_POINT('Ctrl Pts',(2.87153770337927,17.2580547504886,0.195519413316264));
#31146=CARTESIAN_POINT('Ctrl Pts',(2.91188788934173,17.2560868079356,0.163202546768814));
#31147=CARTESIAN_POINT('Ctrl Pts',(2.95159725048241,17.2492919759318,0.13472065733316));
#31148=CARTESIAN_POINT('Origin',(-2.86726590046863,16.7564550623337,100.));
#31149=CARTESIAN_POINT('Ctrl Pts',(-2.95159725048241,17.2492919759318,0.134720657333159));
#31150=CARTESIAN_POINT('Ctrl Pts',(-2.91188788934176,17.2560868079356,0.163202546768789));
#31151=CARTESIAN_POINT('Ctrl Pts',(-2.87153770337939,17.2580547504885,0.19551941331617));
#31152=CARTESIAN_POINT('Ctrl Pts',(-2.74125271406348,17.2486813881446,0.310543821713542));
#31153=CARTESIAN_POINT('Ctrl Pts',(-2.65540724345347,17.2180093215945,0.403057585726612));
#31154=CARTESIAN_POINT('Ctrl Pts',(-2.58148098692643,17.1667329826481,0.497903494266832));
#31155=CARTESIAN_POINT('Ctrl Pts',(-2.58066564781746,17.1661638416689,0.49895174885553));
#31156=CARTESIAN_POINT('Ctrl Pts',(-2.57985201635105,17.1655922755232,0.5));
#31157=CARTESIAN_POINT('Origin',(0.,20.8380434782609,0.5));
#32976=UNCERTAINTY_MEASURE_WITH_UNIT(LENGTH_MEASURE(0.01),#33017,
'DISTANCE_ACCURACY_VALUE',
'Maximum model space distance between geometric entities at asserted c
onnectivities');
#32984=UNCERTAINTY_MEASURE_WITH_UNIT(LENGTH_MEASURE(0.01),#33017,
'DISTANCE_ACCURACY_VALUE',
'Maximum model space distance between geometric entities at asserted c
onnectivities');
#33008=(
GEOMETRIC_REPRESENTATION_CONTEXT(3)
GLOBAL_UNCERTAINTY_ASSIGNED_CONTEXT((#32976))
GLOBAL_UNIT_ASSIGNED_CONTEXT((#33017,#33019,#33020))
REPRESENTATION_CONTEXT('','3D')
);
#33016=(
GEOMETRIC_REPRESENTATION_CONTEXT(3)
GLOBAL_UNCERTAINTY_ASSIGNED_CONTEXT((#32984))
GLOBAL_UNIT_ASSIGNED_CONTEXT((#33017,#33019,#33020))
REPRESENTATION_CONTEXT('','3D')
);
#33017=(
LENGTH_UNIT()
NAMED_UNIT(*)
SI_UNIT(.MILLI.,.METRE.)
);
#33019=(
NAMED_UNIT(*)
PLANE_ANGLE_UNIT()
SI_UNIT($,.RADIAN.)
);
#33020=(
NAMED_UNIT(*)
SI_UNIT($,.STERADIAN.)
SOLID_ANGLE_UNIT()
);
#33044=SHAPE_DEFINITION_REPRESENTATION(#33097,#33147);
#33097=PRODUCT_DEFINITION_SHAPE('',$,#33179);
#33147=SHAPE_REPRESENTATION('',(#10923),#33008);
#33155=PRODUCT_DEFINITION_CONTEXT('part definition',#33250,'design');
#33179=PRODUCT_DEFINITION(
'P_Torque Wrench_Hand Grip_PRT-TQ-1012-03_M_Rev01','PRT-TQ-1012-03',#33210,
#33155);
#33210=PRODUCT_DEFINITION_FORMATION('',$,#33275);
#33250=APPLICATION_CONTEXT(
'Core Data for Automotive Mechanical Design Process');
#33251=PRODUCT_CONTEXT('part definition',#33250,'mechanical');
#33275=PRODUCT('P_Torque Wrench_Hand Grip_PRT-TQ-1012-03_M_Rev01',
'PRT-TQ-1012-03',$,(#33251));
#33284=PRESENTATION_STYLE_ASSIGNMENT((#33291));
#33291=SURFACE_STYLE_USAGE(.BOTH.,#33298);
#33298=SURFACE_SIDE_STYLE('',(#33305));
#33305=SURFACE_STYLE_FILL_AREA(#33312);
#33312=FILL_AREA_STYLE('Opaque(186,91,6)',(#33319));
#33319=FILL_AREA_STYLE_COLOUR('Opaque(186,91,6)',#33326);
#33326=COLOUR_RGB('Opaque(186,91,6)', 0.09019608, 0.27058824, 0.51372549);
ENDSEC;
END-ISO-10303-21;
